ISO-10303-21;
HEADER;
FILE_DESCRIPTION (('STEP AP214'),
    '1' );
FILE_NAME ('fast gear_ISO - Spur gear 2M 40T 20PA 10FW ---S40A75H50L38.0N.step',
    '2026-10-08T09:53:37',
    ( '' ),
    ( '' ),
    'SwSTEP 2.0',
    'SolidWorks 2026',
    '' );
FILE_SCHEMA (( 'AUTOMOTIVE_DESIGN' ));
ENDSEC;

DATA;
#24=CARTESIAN_POINT ( 'NONE',  ( 0.000000000000000000, -37.22597642581153821, 10.79786254984320415 ) ) ;
#40=VECTOR ( 'NONE', #42271, 1000.000000000000000 ) ;
#50=EDGE_CURVE ( 'NONE', #4438, #10838, #58395, .T. ) ;
#55=ORIENTED_EDGE ( 'NONE', *, *, #2305, .T. ) ;
#61=EDGE_LOOP ( 'NONE', ( #56429, #49717, #59358, #37465 ) ) ;
#67=EDGE_LOOP ( 'NONE', ( #2457, #71707, #71945, #64726 ) ) ;
#82=ORIENTED_EDGE ( 'NONE', *, *, #60544, .T. ) ;
#88=EDGE_CURVE ( 'NONE', #20645, #66879, #14982, .T. ) ;
#89=CARTESIAN_POINT ( 'NONE',  ( -3.000000000000000000, 0.000000000000000000, 0.000000000000000000 ) ) ;
#99=CARTESIAN_POINT ( 'NONE',  ( 0.000000000000000000, -0.9646360437375307573, 23.52805723605590060 ) ) ;
#109=PLANE ( 'NONE',  #37048 ) ;
#110=DIRECTION ( 'NONE',  ( 1.000000000000000000, -0.000000000000000000, -0.000000000000000000 ) ) ;
#124=EDGE_LOOP ( 'NONE', ( #72657, #17646, #60225, #7667 ) ) ;
#130=DIRECTION ( 'NONE',  ( 0.000000000000000000, -0.7071067811865389130, -0.7071067811865563435 ) ) ;
#139=LINE ( 'NONE', #40307, #28824 ) ;
#144=AXIS2_PLACEMENT_3D ( 'NONE', #36569, #42969, #48233 ) ;
#153=EDGE_CURVE ( 'NONE', #68796, #47180, #52421, .T. ) ;
#197=DIRECTION ( 'NONE',  ( 0.000000000000000000, -6.938893903907228378E-15, 1.000000000000000000 ) ) ;
#198=AXIS2_PLACEMENT_3D ( 'NONE', #15360, #39055, #27767 ) ;
#200=CARTESIAN_POINT ( 'NONE',  ( 10.00000000000000000, -27.13269053701114331, 25.88420570971391754 ) ) ;
#220=ORIENTED_EDGE ( 'NONE', *, *, #37863, .T. ) ;
#227=AXIS2_PLACEMENT_3D ( 'NONE', #25295, #66623, #48591 ) ;
#233=ORIENTED_EDGE ( 'NONE', *, *, #65058, .T. ) ;
#238=ORIENTED_EDGE ( 'NONE', *, *, #67114, .T. ) ;
#252=CARTESIAN_POINT ( 'NONE',  ( 0.000000000000000000, 5.835314593368772229, -22.81335362449846826 ) ) ;
#270=DIRECTION ( 'NONE',  ( 0.000000000000000000, 1.000000000000000000, -0.000000000000000000 ) ) ;
#275=CARTESIAN_POINT ( 'NONE',  ( -3.000000000000000000, 0.000000000000000000, 0.000000000000000000 ) ) ;
#280=CYLINDRICAL_SURFACE ( 'NONE', #16286, 42.00000000000000000 ) ;
#281=CARTESIAN_POINT ( 'NONE',  ( 0.000000000000000000, -22.67460108101774807, -6.353146135318215038 ) ) ;
#285=FACE_OUTER_BOUND ( 'NONE', #21532, .T. ) ;
#291=AXIS2_PLACEMENT_3D ( 'NONE', #10658, #61809, #43781 ) ;
#341=ORIENTED_EDGE ( 'NONE', *, *, #54773, .T. ) ;
#345=AXIS2_PLACEMENT_3D ( 'NONE', #23518, #51340, #45354 ) ;
#358=ORIENTED_EDGE ( 'NONE', *, *, #28754, .T. ) ;
#391=CIRCLE ( 'NONE', #51961, 16.00000000000000000 ) ;
#398=AXIS2_PLACEMENT_3D ( 'NONE', #46012, #71039, #28703 ) ;
#402=ORIENTED_EDGE ( 'NONE', *, *, #38350, .F. ) ;
#433=AXIS2_PLACEMENT_3D ( 'NONE', #66115, #14212, #26606 ) ;
#453=CARTESIAN_POINT ( 'NONE',  ( -3.000000000000000000, -4.261787119644969479, -26.19803753235780519 ) ) ;
#458=DIRECTION ( 'NONE',  ( 0.000000000000000000, 0.3090169943749410120, 0.9510565162951557516 ) ) ;
#459=ADVANCED_FACE ( 'NONE', ( #27119 ), #44445, .F. ) ;
#469=LINE ( 'NONE', #45568, #28611 ) ;
#471=FACE_OUTER_BOUND ( 'NONE', #38259, .T. ) ;
#474=AXIS2_PLACEMENT_3D ( 'NONE', #29907, #2130, #12619 ) ;
#476=EDGE_CURVE ( 'NONE', #51153, #68962, #28239, .T. ) ;
#482=CARTESIAN_POINT ( 'NONE',  ( 10.00000000000000000, 22.64427369931169309, 30.00120703465213623 ) ) ;
#483=DIRECTION ( 'NONE',  ( -1.000000000000000000, 0.000000000000000000, 0.000000000000000000 ) ) ;
#487=ADVANCED_FACE ( 'NONE', ( #68858 ), #74107, .T. ) ;
#495=ORIENTED_EDGE ( 'NONE', *, *, #68774, .T. ) ;
#499=DIRECTION ( 'NONE',  ( -1.000000000000000000, -0.000000000000000000, -0.000000000000000000 ) ) ;
#500=ORIENTED_EDGE ( 'NONE', *, *, #22914, .F. ) ;
#505=ORIENTED_EDGE ( 'NONE', *, *, #50, .F. ) ;
#514=ORIENTED_EDGE ( 'NONE', *, *, #11366, .F. ) ;
#533=FACE_OUTER_BOUND ( 'NONE', #53175, .T. ) ;
#538=DIRECTION ( 'NONE',  ( 1.000000000000000000, -0.000000000000000000, -0.000000000000000000 ) ) ;
#546=EDGE_CURVE ( 'NONE', #43524, #52685, #44810, .T. ) ;
#548=CARTESIAN_POINT ( 'NONE',  ( 5.000000000000000000, 15.48615015657637706, -39.04073710021327770 ) ) ;
#554=EDGE_LOOP ( 'NONE', ( #59546, #61872, #69236, #1698 ) ) ;
#583=EDGE_LOOP ( 'NONE', ( #10070, #55687, #11544, #43388 ) ) ;
#584=CYLINDRICAL_SURFACE ( 'NONE', #16618, 16.00000000000000000 ) ;
#585=CIRCLE ( 'NONE', #53347, 42.00000000000000000 ) ;
#586=EDGE_LOOP ( 'NONE', ( #41362, #43184, #19887, #37146 ) ) ;
#613=DIRECTION ( 'NONE',  ( 0.000000000000000000, -0.4539904997395540764, 0.8910065241883642351 ) ) ;
#629=DIRECTION ( 'NONE',  ( -1.000000000000000000, 0.000000000000000000, -0.000000000000000000 ) ) ;
#630=CARTESIAN_POINT ( 'NONE',  ( 0.000000000000000000, -37.48860685352290290, -0.8828120875904512665 ) ) ;
#632=EDGE_CURVE ( 'NONE', #62228, #65777, #28151, .T. ) ;
#634=EDGE_CURVE ( 'NONE', #41342, #12738, #7756, .T. ) ;
#635=CARTESIAN_POINT ( 'NONE',  ( 10.00000000000000000, -16.23288003029473359, -33.80338159004301701 ) ) ;
#657=DIRECTION ( 'NONE',  ( 0.000000000000000000, 0.4539904997395477482, -0.8910065241883673437 ) ) ;
#691=VECTOR ( 'NONE', #33949, 1000.000000000000000 ) ;
#720=VECTOR ( 'NONE', #25751, 1000.000000000000000 ) ;
#744=DIRECTION ( 'NONE',  ( -1.000000000000000000, -0.000000000000000000, -0.000000000000000000 ) ) ;
#746=CARTESIAN_POINT ( 'NONE',  ( 10.00000000000000000, 17.67226234102874116, -33.17418723428288274 ) ) ;
#752=EDGE_CURVE ( 'NONE', #15096, #60587, #35726, .T. ) ;
#758=AXIS2_PLACEMENT_3D ( 'NONE', #12505, #70010, #6510 ) ;
#762=CYLINDRICAL_SURFACE ( 'NONE', #9243, 16.00000000000000000 ) ;
#765=VECTOR ( 'NONE', #15129, 1000.000000000000000 ) ;
#766=VERTEX_POINT ( 'NONE', #25933 ) ;
#770=AXIS2_PLACEMENT_3D ( 'NONE', #9925, #56553, #16690 ) ;
#779=VERTEX_POINT ( 'NONE', #26670 ) ;
#784=DIRECTION ( 'NONE',  ( 0.000000000000000000, 0.000000000000000000, 1.000000000000000000 ) ) ;
#794=ORIENTED_EDGE ( 'NONE', *, *, #4900, .T. ) ;
#799=ORIENTED_EDGE ( 'NONE', *, *, #19594, .F. ) ;
#816=CIRCLE ( 'NONE', #59598, 16.00000000000000000 ) ;
#822=VECTOR ( 'NONE', #46720, 1000.000000000000000 ) ;
#823=LINE ( 'NONE', #22987, #58907 ) ;
#831=DIRECTION ( 'NONE',  ( 0.000000000000000000, 0.8090169943749487835, -0.5877852522924713607 ) ) ;
#832=DIRECTION ( 'NONE',  ( -1.000000000000000000, 0.000000000000000000, 0.000000000000000000 ) ) ;
#846=ORIENTED_EDGE ( 'NONE', *, *, #38350, .T. ) ;
#847=CARTESIAN_POINT ( 'NONE',  ( 0.000000000000000000, -31.52238457039579345, -27.75498641678775158 ) ) ;
#857=CARTESIAN_POINT ( 'NONE',  ( -3.000000000000000000, -13.04903810567647682, -19.60159698893442481 ) ) ;
#880=ORIENTED_EDGE ( 'NONE', *, *, #55750, .F. ) ;
#894=CARTESIAN_POINT ( 'NONE',  ( 0.000000000000000000, 0.000000000000000000, 21.00000000000000000 ) ) ;
#909=DIRECTION ( 'NONE',  ( -1.000000000000000000, 0.000000000000000000, -0.000000000000000000 ) ) ;
#913=VERTEX_POINT ( 'NONE', #15021 ) ;
#924=ORIENTED_EDGE ( 'NONE', *, *, #26109, .T. ) ;
#941=CARTESIAN_POINT ( 'NONE',  ( 0.000000000000000000, -32.34446384429951138, -26.79245525562750530 ) ) ;
#952=ORIENTED_EDGE ( 'NONE', *, *, #36133, .T. ) ;
#969=ADVANCED_FACE ( 'NONE', ( #55990 ), #68023, .T. ) ;
#980=DIRECTION ( 'NONE',  ( 0.000000000000000000, 0.1045284632676570791, -0.9945218953682730678 ) ) ;
#993=EDGE_CURVE ( 'NONE', #12738, #35320, #23278, .T. ) ;
#996=CARTESIAN_POINT ( 'NONE',  ( 0.000000000000000000, 37.22597642581150268, 5.202137450157037435 ) ) ;
#997=DIRECTION ( 'NONE',  ( 0.000000000000000000, 0.000000000000000000, 1.000000000000000000 ) ) ;
#1042=EDGE_CURVE ( 'NONE', #26594, #50602, #50718, .T. ) ;
#1064=CARTESIAN_POINT ( 'NONE',  ( -3.000000000000000000, -26.23277895567245821, -4.042438405570103477 ) ) ;
#1071=ORIENTED_EDGE ( 'NONE', *, *, #70363, .T. ) ;
#1084=AXIS2_PLACEMENT_3D ( 'NONE', #26024, #31296, #60267 ) ;
#1105=CYLINDRICAL_SURFACE ( 'NONE', #41654, 37.49900000000000233 ) ;
#1119=DIRECTION ( 'NONE',  ( 0.000000000000000000, 0.000000000000000000, 1.000000000000000000 ) ) ;
#1128=CARTESIAN_POINT ( 'NONE',  ( 0.000000000000000000, 37.16516213103277266, 4.992566952385114831 ) ) ;
#1132=ADVANCED_FACE ( 'NONE', ( #70214 ), #70959, .T. ) ;
#1133=EDGE_CURVE ( 'NONE', #26842, #70819, #32431, .T. ) ;
#1149=CIRCLE ( 'NONE', #29913, 16.00000000000000000 ) ;
#1154=CARTESIAN_POINT ( 'NONE',  ( 0.000000000000000000, 37.58145647212455032, -0.6853352020786441789 ) ) ;
#1156=VECTOR ( 'NONE', #16470, 1000.000000000000000 ) ;
#1158=AXIS2_PLACEMENT_3D ( 'NONE', #11271, #69884, #51869 ) ;
#1168=ORIENTED_EDGE ( 'NONE', *, *, #43119, .T. ) ;
#1179=ORIENTED_EDGE ( 'NONE', *, *, #14136, .T. ) ;
#1196=CARTESIAN_POINT ( 'NONE',  ( 10.00000000000000000, -36.13751322684434797, 21.40280677340358295 ) ) ;
#1201=DIRECTION ( 'NONE',  ( 0.000000000000000000, 0.000000000000000000, 1.000000000000000000 ) ) ;
#1203=DIRECTION ( 'NONE',  ( -1.000000000000000000, -0.000000000000000000, -0.000000000000000000 ) ) ;
#1215=FACE_OUTER_BOUND ( 'NONE', #8701, .T. ) ;
#1224=ORIENTED_EDGE ( 'NONE', *, *, #42313, .F. ) ;
#1235=EDGE_CURVE ( 'NONE', #19038, #52874, #22855, .T. ) ;
#1254=EDGE_CURVE ( 'NONE', #32004, #20003, #26430, .T. ) ;
#1270=CARTESIAN_POINT ( 'NONE',  ( -10.00000000000000000, 0.000000000000000000, 0.000000000000000000 ) ) ;
#1321=CARTESIAN_POINT ( 'NONE',  ( 0.000000000000000000, -27.13269053701114331, 25.88420570971391754 ) ) ;
#1323=CARTESIAN_POINT ( 'NONE',  ( 0.000000000000000000, 30.00120703465205452, 22.64427369931179967 ) ) ;
#1324=CIRCLE ( 'NONE', #39714, 15.99999999999999822 ) ;
#1344=ORIENTED_EDGE ( 'NONE', *, *, #2745, .F. ) ;
#1361=DIRECTION ( 'NONE',  ( 0.000000000000000000, -0.9876883405951361050, -0.1564344650402419989 ) ) ;
#1363=ORIENTED_EDGE ( 'NONE', *, *, #47890, .T. ) ;
#1365=VERTEX_POINT ( 'NONE', #26209 ) ;
#1370=CARTESIAN_POINT ( 'NONE',  ( 10.00000000000000000, 0.000000000000000000, 0.000000000000000000 ) ) ;
#1375=VERTEX_POINT ( 'NONE', #43538 ) ;
#1391=CARTESIAN_POINT ( 'NONE',  ( 10.00000000000000000, 37.01155633439068282, -6.555932627142014191 ) ) ;
#1398=EDGE_CURVE ( 'NONE', #55375, #766, #45384, .T. ) ;
#1403=ORIENTED_EDGE ( 'NONE', *, *, #50554, .F. ) ;
#1406=AXIS2_PLACEMENT_3D ( 'NONE', #47553, #28778, #47185 ) ;
#1414=ORIENTED_EDGE ( 'NONE', *, *, #22167, .T. ) ;
#1417=EDGE_LOOP ( 'NONE', ( #24724, #55404, #20548, #16275 ) ) ;
#1418=VECTOR ( 'NONE', #74185, 1000.000000000000000 ) ;
#1420=AXIS2_PLACEMENT_3D ( 'NONE', #24353, #57095, #29979 ) ;
#1434=DIRECTION ( 'NONE',  ( 0.000000000000000000, -0.7071067811865535679, 0.7071067811865413555 ) ) ;
#1439=VERTEX_POINT ( 'NONE', #45008 ) ;
#1454=CARTESIAN_POINT ( 'NONE',  ( 10.00000000000000000, 37.58145647212453611, 16.68533520207917675 ) ) ;
#1465=AXIS2_PLACEMENT_3D ( 'NONE', #47742, #70655, #59776 ) ;
#1466=CARTESIAN_POINT ( 'NONE',  ( 10.00000000000000000, 27.13269053701096922, 25.88420570971410228 ) ) ;
#1475=CIRCLE ( 'NONE', #43468, 37.49900000000000944 ) ;
#1481=CARTESIAN_POINT ( 'NONE',  ( 10.00000000000000000, -29.81001611430991360, -22.74946021919165418 ) ) ;
#1499=EDGE_CURVE ( 'NONE', #11081, #22472, #23824, .T. ) ;
#1503=DIRECTION ( 'NONE',  ( -1.000000000000000000, 0.000000000000000000, 0.000000000000000000 ) ) ;
#1527=ORIENTED_EDGE ( 'NONE', *, *, #52461, .F. ) ;
#1541=LINE ( 'NONE', #45898, #64524 ) ;
#1542=CARTESIAN_POINT ( 'NONE',  ( 0.000000000000000000, -4.261787119644969479, -26.19803753235780519 ) ) ;
#1546=DIRECTION ( 'NONE',  ( 0.000000000000000000, 0.7431448254773862505, 0.6691306063588672304 ) ) ;
#1551=CARTESIAN_POINT ( 'NONE',  ( 10.00000000000000000, 26.79245525562761188, -32.34446384429941901 ) ) ;
#1555=ORIENTED_EDGE ( 'NONE', *, *, #26109, .F. ) ;
#1559=PLANE ( 'NONE',  #50671 ) ;
#1562=FACE_OUTER_BOUND ( 'NONE', #21689, .T. ) ;
#1563=EDGE_CURVE ( 'NONE', #57100, #11579, #47135, .T. ) ;
#1572=CARTESIAN_POINT ( 'NONE',  ( -10.00000000000000000, 0.000000000000000000, 0.000000000000000000 ) ) ;
#1578=LINE ( 'NONE', #69587, #65841 ) ;
#1588=EDGE_CURVE ( 'NONE', #7308, #26594, #25659, .T. ) ;
#1591=CARTESIAN_POINT ( 'NONE',  ( 0.000000000000000000, -19.89357724624987256, -12.59942793731086041 ) ) ;
#1620=ORIENTED_EDGE ( 'NONE', *, *, #10264, .F. ) ;
#1648=CARTESIAN_POINT ( 'NONE',  ( 10.00000000000000000, 35.38097989696528600, -12.42422080174602605 ) ) ;
#1657=ADVANCED_FACE ( 'NONE', ( #53506 ), #65168, .T. ) ;
#1687=EDGE_CURVE ( 'NONE', #32720, #39781, #6457, .T. ) ;
#1690=ORIENTED_EDGE ( 'NONE', *, *, #30848, .T. ) ;
#1695=VERTEX_POINT ( 'NONE', #33516 ) ;
#1698=ORIENTED_EDGE ( 'NONE', *, *, #43746, .T. ) ;
#1703=AXIS2_PLACEMENT_3D ( 'NONE', #54205, #42188, #65489 ) ;
#1731=DIRECTION ( 'NONE',  ( -1.000000000000000000, 0.000000000000000000, -0.000000000000000000 ) ) ;
#1736=VERTEX_POINT ( 'NONE', #38800 ) ;
#1737=EDGE_CURVE ( 'NONE', #62140, #50450, #9856, .T. ) ;
#1747=DIRECTION ( 'NONE',  ( 1.000000000000000000, -0.000000000000000000, -0.000000000000000000 ) ) ;
#1752=CIRCLE ( 'NONE', #55740, 16.00000000000000000 ) ;
#1757=DIRECTION ( 'NONE',  ( 0.000000000000000000, 0.000000000000000000, 1.000000000000000000 ) ) ;
#1763=DIRECTION ( 'NONE',  ( 0.000000000000000000, 0.000000000000000000, 1.000000000000000000 ) ) ;
#1773=ADVANCED_FACE ( 'NONE', ( #15493 ), #56091, .T. ) ;
#1778=EDGE_LOOP ( 'NONE', ( #27540, #48936, #26434, #34433 ) ) ;
#1780=AXIS2_PLACEMENT_3D ( 'NONE', #62501, #62116, #27521 ) ;
#1786=EDGE_LOOP ( 'NONE', ( #59836, #5307, #25692, #57159 ) ) ;
#1793=CARTESIAN_POINT ( 'NONE',  ( 5.000000000000000000, -22.48208911017474065, -35.47612816024548721 ) ) ;
#1794=CARTESIAN_POINT ( 'NONE',  ( 0.000000000000000000, -16.45098606841149902, 33.79645857604508308 ) ) ;
#1813=ORIENTED_EDGE ( 'NONE', *, *, #40779, .T. ) ;
#1816=VERTEX_POINT ( 'NONE', #35018 ) ;
#1819=LINE ( 'NONE', #64944, #43412 ) ;
#1827=ORIENTED_EDGE ( 'NONE', *, *, #69328, .T. ) ;
#1855=CARTESIAN_POINT ( 'NONE',  ( 10.00000000000000000, -22.64427369931191336, 30.00120703465197280 ) ) ;
#1865=DIRECTION ( 'NONE',  ( -1.000000000000000000, 0.000000000000000000, 0.000000000000000000 ) ) ;
#1877=AXIS2_PLACEMENT_3D ( 'NONE', #45743, #47200, #70113 ) ;
#1889=ORIENTED_EDGE ( 'NONE', *, *, #3175, .T. ) ;
#1894=ORIENTED_EDGE ( 'NONE', *, *, #44039, .F. ) ;
#1898=ORIENTED_EDGE ( 'NONE', *, *, #35296, .F. ) ;
#1906=EDGE_CURVE ( 'NONE', #31995, #22414, #45941, .T. ) ;
#1913=ORIENTED_EDGE ( 'NONE', *, *, #2534, .F. ) ;
#1958=CARTESIAN_POINT ( 'NONE',  ( 0.000000000000000000, -10.45096189432344147, 21.10159698893425784 ) ) ;
#1960=CARTESIAN_POINT ( 'NONE',  ( -3.000000000000000000, 23.50000000000000000, 1.499999999999997780 ) ) ;
#1973=EDGE_CURVE ( 'NONE', #17553, #64952, #13551, .T. ) ;
#1978=ORIENTED_EDGE ( 'NONE', *, *, #60682, .T. ) ;
#1979=CARTESIAN_POINT ( 'NONE',  ( 0.000000000000000000, -21.40280677340398086, 36.13751322684410638 ) ) ;
#1980=ORIENTED_EDGE ( 'NONE', *, *, #50845, .F. ) ;
#2012=FACE_OUTER_BOUND ( 'NONE', #10594, .T. ) ;
#2016=LINE ( 'NONE', #24903, #46301 ) ;
#2018=DIRECTION ( 'NONE',  ( -1.000000000000000000, 0.000000000000000000, 0.000000000000000000 ) ) ;
#2019=ORIENTED_EDGE ( 'NONE', *, *, #57120, .F. ) ;
#2022=CYLINDRICAL_SURFACE ( 'NONE', #15656, 16.00000000000000000 ) ;
#2023=CARTESIAN_POINT ( 'NONE',  ( 0.000000000000000000, 3.925862922256769583, -41.81611651403857621 ) ) ;
#2027=CARTESIAN_POINT ( 'NONE',  ( 0.000000000000000000, 35.95386929396256903, -10.96151621346501237 ) ) ;
#2034=CARTESIAN_POINT ( 'NONE',  ( 10.00000000000000000, -40.98264845739755913, 9.188173127307164734 ) ) ;
#2038=DIRECTION ( 'NONE',  ( 0.000000000000000000, -0.4539904997395542430, 0.8910065241883641241 ) ) ;
#2046=CIRCLE ( 'NONE', #15204, 15.99999999999999822 ) ;
#2052=AXIS2_PLACEMENT_3D ( 'NONE', #46814, #30245, #13325 ) ;
#2090=CARTESIAN_POINT ( 'NONE',  ( -3.000000000000000000, 8.688484142254221609, -21.88630264137359660 ) ) ;
#2092=CARTESIAN_POINT ( 'NONE',  ( 0.000000000000000000, -25.60904388321925396, 6.976881207771170601 ) ) ;
#2099=CARTESIAN_POINT ( 'NONE',  ( 10.00000000000000000, 0.8828120875900632436, 37.48860685352291000 ) ) ;
#2100=CARTESIAN_POINT ( 'NONE',  ( 10.00000000000000000, 21.32104025579158701, -30.84782396557194772 ) ) ;
#2111=ORIENTED_EDGE ( 'NONE', *, *, #67660, .T. ) ;
#2130=DIRECTION ( 'NONE',  ( -1.000000000000000000, 0.000000000000000000, -0.000000000000000000 ) ) ;
#2135=CARTESIAN_POINT ( 'NONE',  ( 10.00000000000000000, 25.88420570971400991, 27.13269053701105449 ) ) ;
#2141=ORIENTED_EDGE ( 'NONE', *, *, #2607, .T. ) ;
#2144=AXIS2_PLACEMENT_3D ( 'NONE', #19810, #54046, #58562 ) ;
#2148=CARTESIAN_POINT ( 'NONE',  ( -3.000000000000000000, 5.835314593368772229, -22.81335362449846826 ) ) ;
#2158=CYLINDRICAL_SURFACE ( 'NONE', #46467, 37.49900000000000233 ) ;
#2176=EDGE_CURVE ( 'NONE', #41055, #54186, #54523, .T. ) ;
#2188=DIRECTION ( 'NONE',  ( 0.000000000000000000, 0.9876883405951372152, 0.1564344650402346160 ) ) ;
#2209=CARTESIAN_POINT ( 'NONE',  ( 0.000000000000000000, 18.84667830672605859, -18.68964196561243796 ) ) ;
#2215=DIRECTION ( 'NONE',  ( -1.000000000000000000, -0.000000000000000000, 0.000000000000000000 ) ) ;
#2239=EDGE_CURVE ( 'NONE', #60337, #68796, #23644, .T. ) ;
#2240=EDGE_LOOP ( 'NONE', ( #3243, #38073, #43114, #12626 ) ) ;
#2246=EDGE_CURVE ( 'NONE', #62834, #3072, #22923, .T. ) ;
#2247=AXIS2_PLACEMENT_3D ( 'NONE', #1064, #40500, #13026 ) ;
#2264=EDGE_LOOP ( 'NONE', ( #67169, #30583, #61452, #35054 ) ) ;
#2265=DIRECTION ( 'NONE',  ( 0.000000000000000000, 0.000000000000000000, 1.000000000000000000 ) ) ;
#2295=DIRECTION ( 'NONE',  ( 0.000000000000000000, 0.000000000000000000, -1.000000000000000000 ) ) ;
#2302=DIRECTION ( 'NONE',  ( -1.000000000000000000, 0.000000000000000000, 0.000000000000000000 ) ) ;
#2305=EDGE_CURVE ( 'NONE', #54905, #49986, #32055, .T. ) ;
#2325=CARTESIAN_POINT ( 'NONE',  ( 10.00000000000000000, -26.79245525562691199, -32.34446384430000876 ) ) ;
#2338=CYLINDRICAL_SURFACE ( 'NONE', #25953, 16.00000000000000000 ) ;
#2339=EDGE_LOOP ( 'NONE', ( #11916, #20613, #39036, #53494 ) ) ;
#2347=VERTEX_POINT ( 'NONE', #51844 ) ;
#2353=CARTESIAN_POINT ( 'NONE',  ( 10.00000000000000000, -30.00120703465189465, -22.64427369931201639 ) ) ;
#2362=AXIS2_PLACEMENT_3D ( 'NONE', #71172, #19677, #41882 ) ;
#2367=ORIENTED_EDGE ( 'NONE', *, *, #58401, .T. ) ;
#2371=CARTESIAN_POINT ( 'NONE',  ( -3.000000000000000000, -19.89357724624987256, -12.59942793731086041 ) ) ;
#2374=FACE_OUTER_BOUND ( 'NONE', #18159, .T. ) ;
#2387=LINE ( 'NONE', #42567, #40371 ) ;
#2400=AXIS2_PLACEMENT_3D ( 'NONE', #34460, #40115, #63068 ) ;
#2412=CARTESIAN_POINT ( 'NONE',  ( -3.000000000000000000, 26.50000000000000000, -1.500000000000001332 ) ) ;
#2426=EDGE_CURVE ( 'NONE', #25590, #50309, #17637, .T. ) ;
#2446=EDGE_CURVE ( 'NONE', #52874, #20645, #42077, .T. ) ;
#2447=AXIS2_PLACEMENT_3D ( 'NONE', #58213, #42406, #6358 ) ;
#2453=VECTOR ( 'NONE', #14953, 999.9999999999998863 ) ;
#2457=ORIENTED_EDGE ( 'NONE', *, *, #56794, .F. ) ;
#2465=VERTEX_POINT ( 'NONE', #18726 ) ;
#2481=CARTESIAN_POINT ( 'NONE',  ( 10.00000000000000000, 37.48860685352291000, 0.8828120875901893649 ) ) ;
#2483=DIRECTION ( 'NONE',  ( -0.000000000000000000, 0.1045284632676436315, 0.9945218953682742891 ) ) ;
#2491=AXIS2_PLACEMENT_3D ( 'NONE', #56724, #28124, #21353 ) ;
#2495=DIRECTION ( 'NONE',  ( 1.000000000000000000, 0.000000000000000000, -0.000000000000000000 ) ) ;
#2498=EDGE_LOOP ( 'NONE', ( #10615, #56014, #68071, #49433 ) ) ;
#2499=EDGE_CURVE ( 'NONE', #22473, #67855, #51677, .T. ) ;
#2502=DIRECTION ( 'NONE',  ( 0.000000000000000000, 0.3090169943749482839, -0.9510565162951533091 ) ) ;
#2503=ADVANCED_FACE ( 'NONE', ( #29631 ), #64246, .F. ) ;
#2509=CARTESIAN_POINT ( 'NONE',  ( -3.000000000000000000, -22.32062822937469804, -14.36278369418829826 ) ) ;
#2514=PLANE ( 'NONE',  #41762 ) ;
#2519=CARTESIAN_POINT ( 'NONE',  ( 10.00000000000000000, 37.22597642581158084, -5.202137450156524068 ) ) ;
#2534=EDGE_CURVE ( 'NONE', #31921, #51229, #7462, .T. ) ;
#2555=AXIS2_PLACEMENT_3D ( 'NONE', #54062, #30372, #42045 ) ;
#2556=PLANE ( 'NONE',  #34190 ) ;
#2562=EDGE_LOOP ( 'NONE', ( #41987, #28970, #17725, #36974 ) ) ;
#2569=ORIENTED_EDGE ( 'NONE', *, *, #52387, .F. ) ;
#2583=AXIS2_PLACEMENT_3D ( 'NONE', #32833, #55782, #22692 ) ;
#2607=EDGE_CURVE ( 'NONE', #61596, #32352, #4060, .T. ) ;
#2608=DIRECTION ( 'NONE',  ( 0.000000000000000000, -0.8090169943749531134, 0.5877852522924653655 ) ) ;
#2614=EDGE_CURVE ( 'NONE', #18110, #44000, #8577, .T. ) ;
#2618=VERTEX_POINT ( 'NONE', #66100 ) ;
#2622=FACE_OUTER_BOUND ( 'NONE', #62454, .T. ) ;
#2623=ORIENTED_EDGE ( 'NONE', *, *, #8125, .T. ) ;
#2642=ORIENTED_EDGE ( 'NONE', *, *, #42778, .T. ) ;
#2653=AXIS2_PLACEMENT_3D ( 'NONE', #69449, #19420, #42368 ) ;
#2657=CIRCLE ( 'NONE', #18226, 16.00000000000000000 ) ;
#2666=ORIENTED_EDGE ( 'NONE', *, *, #47521, .F. ) ;
#2670=CARTESIAN_POINT ( 'NONE',  ( 10.00000000000000000, 4.992566952384984269, 37.16516213103279398 ) ) ;
#2682=DIRECTION ( 'NONE',  ( 0.000000000000000000, 0.000000000000000000, 1.000000000000000000 ) ) ;
#2699=ORIENTED_EDGE ( 'NONE', *, *, #21892, .F. ) ;
#2702=EDGE_CURVE ( 'NONE', #73774, #55313, #72084, .T. ) ;
#2709=ORIENTED_EDGE ( 'NONE', *, *, #42608, .T. ) ;
#2727=EDGE_CURVE ( 'NONE', #57712, #52639, #31859, .T. ) ;
#2732=DIRECTION ( 'NONE',  ( 0.000000000000000000, 0.000000000000000000, 1.000000000000000000 ) ) ;
#2745=EDGE_CURVE ( 'NONE', #32355, #66201, #56675, .T. ) ;
#2760=CARTESIAN_POINT ( 'NONE',  ( 10.00000000000000000, 17.67226234102826510, 33.17418723428314564 ) ) ;
#2792=LINE ( 'NONE', #42986, #27681 ) ;
#2802=AXIS2_PLACEMENT_3D ( 'NONE', #5993, #11237, #68766 ) ;
#2847=DIRECTION ( 'NONE',  ( 0.000000000000000000, 0.9510565162951523099, 0.3090169943749517811 ) ) ;
#2849=DIRECTION ( 'NONE',  ( 0.000000000000000000, 0.9781476007338069101, -0.2079116908177532086 ) ) ;
#2861=CARTESIAN_POINT ( 'NONE',  ( 0.000000000000000000, -2.663952781845850826, -41.91543099594819921 ) ) ;
#2870=DIRECTION ( 'NONE',  ( 0.000000000000000000, -0.9945218953682745111, 0.1045284632676429237 ) ) ;
#2884=VECTOR ( 'NONE', #32891, 1000.000000000000000 ) ;
#2894=VECTOR ( 'NONE', #59999, 1000.000000000000000 ) ;
#2899=ORIENTED_EDGE ( 'NONE', *, *, #49915, .F. ) ;
#2901=VECTOR ( 'NONE', #19819, 1000.000000000000000 ) ;
#2929=VERTEX_POINT ( 'NONE', #5221 ) ;
#2930=CYLINDRICAL_SURFACE ( 'NONE', #55360, 16.00000000000000000 ) ;
#2949=CARTESIAN_POINT ( 'NONE',  ( -3.000000000000000000, -13.04903810567647682, -19.60159698893442481 ) ) ;
#2963=DIRECTION ( 'NONE',  ( -1.000000000000000000, -0.000000000000000000, 0.000000000000000000 ) ) ;
#2974=DIRECTION ( 'NONE',  ( 0.000000000000000000, -0.9510565162951565288, 0.3090169943749382364 ) ) ;
#2985=DIRECTION ( 'NONE',  ( 0.000000000000000000, -0.2079116908177671419, 0.9781476007338040235 ) ) ;
#2986=AXIS2_PLACEMENT_3D ( 'NONE', #72112, #54104, #8222 ) ;
#2996=FACE_OUTER_BOUND ( 'NONE', #32621, .T. ) ;
#3009=AXIS2_PLACEMENT_3D ( 'NONE', #1323, #69322, #24935 ) ;
#3027=DIRECTION ( 'NONE',  ( 0.000000000000000000, -0.1045284632676429099, -0.9945218953682744001 ) ) ;
#3057=CARTESIAN_POINT ( 'NONE',  ( -3.000000000000000000, -13.04903810567647682, -19.60159698893442481 ) ) ;
#3060=ORIENTED_EDGE ( 'NONE', *, *, #18565, .T. ) ;
#3071=DIRECTION ( 'NONE',  ( -1.000000000000000000, 0.000000000000000000, -0.000000000000000000 ) ) ;
#3072=VERTEX_POINT ( 'NONE', #17588 ) ;
#3082=EDGE_CURVE ( 'NONE', #11035, #30392, #7038, .T. ) ;
#3092=CYLINDRICAL_SURFACE ( 'NONE', #1703, 16.00000000000000000 ) ;
#3100=LINE ( 'NONE', #65497, #63562 ) ;
#3109=VECTOR ( 'NONE', #31359, 1000.000000000000114 ) ;
#3119=EDGE_CURVE ( 'NONE', #8248, #67112, #13420, .T. ) ;
#3129=VERTEX_POINT ( 'NONE', #29966 ) ;
#3133=DIRECTION ( 'NONE',  ( -1.000000000000000000, -0.000000000000000000, 0.000000000000000000 ) ) ;
#3175=EDGE_CURVE ( 'NONE', #16273, #62438, #39382, .T. ) ;
#3179=VERTEX_POINT ( 'NONE', #42006 ) ;
#3202=DIRECTION ( 'NONE',  ( 1.000000000000000000, -0.000000000000000000, -0.000000000000000000 ) ) ;
#3207=CARTESIAN_POINT ( 'NONE',  ( 10.00000000000000000, 26.08949754953062694, -27.05870788708203989 ) ) ;
#3211=DIRECTION ( 'NONE',  ( 1.000000000000000000, -0.000000000000000000, -0.000000000000000000 ) ) ;
#3212=DIRECTION ( 'NONE',  ( 1.000000000000000000, -0.000000000000000000, 0.000000000000000000 ) ) ;
#3214=CARTESIAN_POINT ( 'NONE',  ( 0.000000000000000000, -35.47612816024506088, -22.48208911017539435 ) ) ;
#3224=CARTESIAN_POINT ( 'NONE',  ( 0.000000000000000000, 0.000000000000000000, 0.000000000000000000 ) ) ;
#3232=VECTOR ( 'NONE', #63871, 1000.000000000000000 ) ;
#3240=AXIS2_PLACEMENT_3D ( 'NONE', #7476, #24760, #40578 ) ;
#3243=ORIENTED_EDGE ( 'NONE', *, *, #55243, .F. ) ;
#3247=DIRECTION ( 'NONE',  ( 0.000000000000000000, 0.9135454576426063067, -0.4067366430757881068 ) ) ;
#3248=EDGE_LOOP ( 'NONE', ( #1894, #52391, #11295, #71249 ) ) ;
#3274=DIRECTION ( 'NONE',  ( -1.000000000000000000, -0.000000000000000000, 0.000000000000000000 ) ) ;
#3283=VERTEX_POINT ( 'NONE', #43125 ) ;
#3304=EDGE_LOOP ( 'NONE', ( #7755, #15074, #34763, #514 ) ) ;
#3309=LINE ( 'NONE', #54414, #17262 ) ;
#3314=DIRECTION ( 'NONE',  ( -1.000000000000000000, 0.000000000000000000, 0.000000000000000000 ) ) ;
#3323=DIRECTION ( 'NONE',  ( -1.000000000000000000, 0.000000000000000000, 0.000000000000000000 ) ) ;
#3329=VERTEX_POINT ( 'NONE', #54389 ) ;
#3330=DIRECTION ( 'NONE',  ( 1.000000000000000000, 0.000000000000000000, 0.000000000000000000 ) ) ;
#3343=CARTESIAN_POINT ( 'NONE',  ( -10.00000000000000000, 0.000000000000000000, 0.000000000000000000 ) ) ;
#3350=EDGE_CURVE ( 'NONE', #19670, #60432, #68257, .T. ) ;
#3353=FACE_OUTER_BOUND ( 'NONE', #57335, .T. ) ;
#3354=VERTEX_POINT ( 'NONE', #49111 ) ;
#3368=LINE ( 'NONE', #71745, #33612 ) ;
#3385=DIRECTION ( 'NONE',  ( -1.000000000000000000, 0.000000000000000000, -0.000000000000000000 ) ) ;
#3391=CYLINDRICAL_SURFACE ( 'NONE', #42381, 42.00000000000000000 ) ;
#3421=ORIENTED_EDGE ( 'NONE', *, *, #2614, .T. ) ;
#3434=EDGE_CURVE ( 'NONE', #64359, #61324, #13010, .T. ) ;
#3440=CARTESIAN_POINT ( 'NONE',  ( -3.000000000000000000, -10.45096189432314837, -21.10159698893440350 ) ) ;
#3448=EDGE_CURVE ( 'NONE', #53520, #54954, #56247, .T. ) ;
#3449=ORIENTED_EDGE ( 'NONE', *, *, #73309, .T. ) ;
#3452=ORIENTED_EDGE ( 'NONE', *, *, #7714, .F. ) ;
#3455=FACE_OUTER_BOUND ( 'NONE', #45313, .T. ) ;
#3456=ORIENTED_EDGE ( 'NONE', *, *, #11366, .T. ) ;
#3480=CARTESIAN_POINT ( 'NONE',  ( -3.000000000000000000, -3.948201729842348850, 23.21447184625293048 ) ) ;
#3481=DIRECTION ( 'NONE',  ( 0.000000000000000000, 0.000000000000000000, 1.000000000000000000 ) ) ;
#3483=CYLINDRICAL_SURFACE ( 'NONE', #28666, 16.00000000000000000 ) ;
#3485=ORIENTED_EDGE ( 'NONE', *, *, #55841, .F. ) ;
#3487=AXIS2_PLACEMENT_3D ( 'NONE', #58012, #13255, #70754 ) ;
#3488=AXIS2_PLACEMENT_3D ( 'NONE', #55970, #14996, #61618 ) ;
#3489=CARTESIAN_POINT ( 'NONE',  ( 5.000000000000000000, -16.65560815589439159, 38.55633173627004595 ) ) ;
#3503=DIRECTION ( 'NONE',  ( 0.000000000000000000, 0.000000000000000000, 1.000000000000000000 ) ) ;
#3512=ORIENTED_EDGE ( 'NONE', *, *, #53638, .T. ) ;
#3518=AXIS2_PLACEMENT_3D ( 'NONE', #59122, #19618, #7247 ) ;
#3520=LINE ( 'NONE', #54994, #37599 ) ;
#3534=EDGE_LOOP ( 'NONE', ( #9717, #49196, #61310, #60382 ) ) ;
#3539=CARTESIAN_POINT ( 'NONE',  ( 0.000000000000000000, -38.55633173626998911, -16.65560815589452304 ) ) ;
#3560=ORIENTED_EDGE ( 'NONE', *, *, #32899, .F. ) ;
#3565=CARTESIAN_POINT ( 'NONE',  ( 10.00000000000000000, -10.96151621346461447, -35.95386929396268272 ) ) ;
#3578=EDGE_CURVE ( 'NONE', #53383, #63709, #51752, .T. ) ;
#3590=CYLINDRICAL_SURFACE ( 'NONE', #58274, 16.00000000000000000 ) ;
#3618=CARTESIAN_POINT ( 'NONE',  ( 0.000000000000000000, -11.95096189432345390, 23.69967320028757385 ) ) ;
#3620=CYLINDRICAL_SURFACE ( 'NONE', #44325, 16.00000000000000000 ) ;
#3633=DIRECTION ( 'NONE',  ( -1.000000000000000000, -0.000000000000000000, -0.000000000000000000 ) ) ;
#3637=CIRCLE ( 'NONE', #34847, 37.49900000000000944 ) ;
#3662=EDGE_LOOP ( 'NONE', ( #41472, #31624, #59306, #41796 ) ) ;
#3668=ADVANCED_FACE ( 'NONE', ( #12596 ), #58456, .T. ) ;
#3673=DIRECTION ( 'NONE',  ( -1.000000000000000000, -0.000000000000000000, -0.000000000000000000 ) ) ;
#3674=ORIENTED_EDGE ( 'NONE', *, *, #6333, .T. ) ;
#3675=EDGE_CURVE ( 'NONE', #56198, #49339, #56591, .T. ) ;
#3676=DIRECTION ( 'NONE',  ( 0.000000000000000000, -0.9510565162951544194, 0.3090169943749450088 ) ) ;
#3681=DIRECTION ( 'NONE',  ( -1.000000000000000000, 0.000000000000000000, 0.000000000000000000 ) ) ;
#3685=DIRECTION ( 'NONE',  ( -1.000000000000000000, 0.000000000000000000, -0.000000000000000000 ) ) ;
#3686=EDGE_CURVE ( 'NONE', #12875, #7056, #52079, .T. ) ;
#3702=CIRCLE ( 'NONE', #34924, 42.00000000000000000 ) ;
#3748=ORIENTED_EDGE ( 'NONE', *, *, #13332, .T. ) ;
#3763=DIRECTION ( 'NONE',  ( 0.000000000000000000, 0.000000000000000000, 1.000000000000000000 ) ) ;
#3770=EDGE_CURVE ( 'NONE', #3354, #73774, #12137, .T. ) ;
#3773=CARTESIAN_POINT ( 'NONE',  ( 10.00000000000000000, 35.38097989696512968, 12.42422080174651100 ) ) ;
#3785=CARTESIAN_POINT ( 'NONE',  ( -3.000000000000000000, 0.000000000000000000, 0.000000000000000000 ) ) ;
#3789=AXIS2_PLACEMENT_3D ( 'NONE', #20001, #65893, #54961 ) ;
#3791=VERTEX_POINT ( 'NONE', #54310 ) ;
#3806=ORIENTED_EDGE ( 'NONE', *, *, #39083, .F. ) ;
#3811=FACE_OUTER_BOUND ( 'NONE', #61527, .T. ) ;
#3834=CARTESIAN_POINT ( 'NONE',  ( 10.00000000000000000, 0.000000000000000000, 0.000000000000000000 ) ) ;
#3835=CARTESIAN_POINT ( 'NONE',  ( 0.000000000000000000, 22.48208911017500355, 35.47612816024530957 ) ) ;
#3855=AXIS2_PLACEMENT_3D ( 'NONE', #66042, #14514, #8882 ) ;
#3860=EDGE_CURVE ( 'NONE', #15417, #51502, #68564, .T. ) ;
#3874=PLANE ( 'NONE',  #22596 ) ;
#3886=EDGE_LOOP ( 'NONE', ( #8169, #58773, #8952, #62257 ) ) ;
#3904=CARTESIAN_POINT ( 'NONE',  ( 10.00000000000000000, 0.000000000000000000, 0.000000000000000000 ) ) ;
#3933=CARTESIAN_POINT ( 'NONE',  ( 10.00000000000000000, 27.05870788708267582, -26.08949754952995903 ) ) ;
#3940=ADVANCED_FACE ( 'NONE', ( #33207 ), #45640, .F. ) ;
#3944=CARTESIAN_POINT ( 'NONE',  ( 10.00000000000000000, 5.202137450156389953, 37.22597642581160216 ) ) ;
#3949=DIRECTION ( 'NONE',  ( 0.000000000000000000, -0.8910065241883627918, -0.4539904997395568520 ) ) ;
#3978=CYLINDRICAL_SURFACE ( 'NONE', #60827, 42.00000000000000000 ) ;
#4000=LINE ( 'NONE', #39691, #71492 ) ;
#4005=LINE ( 'NONE', #66413, #10388 ) ;
#4013=VECTOR ( 'NONE', #72739, 1000.000000000000000 ) ;
#4039=DIRECTION ( 'NONE',  ( 0.000000000000000000, 0.000000000000000000, 1.000000000000000000 ) ) ;
#4040=ORIENTED_EDGE ( 'NONE', *, *, #26910, .F. ) ;
#4044=CARTESIAN_POINT ( 'NONE',  ( 0.000000000000000000, 0.000000000000000000, 0.000000000000000000 ) ) ;
#4048=DIRECTION ( 'NONE',  ( -1.000000000000000000, 0.000000000000000000, -0.000000000000000000 ) ) ;
#4051=CARTESIAN_POINT ( 'NONE',  ( 10.00000000000000000, -16.45098606841102651, -33.79645857604531045 ) ) ;
#4053=ORIENTED_EDGE ( 'NONE', *, *, #60375, .F. ) ;
#4056=ORIENTED_EDGE ( 'NONE', *, *, #28445, .T. ) ;
#4060=LINE ( 'NONE', #43543, #52267 ) ;
#4078=CARTESIAN_POINT ( 'NONE',  ( -3.000000000000000000, 5.835314593368772229, -22.81335362449846826 ) ) ;
#4080=( NAMED_UNIT ( * ) PLANE_ANGLE_UNIT ( ) SI_UNIT ( $, .RADIAN. ) );
#4096=CARTESIAN_POINT ( 'NONE',  ( 0.000000000000000000, -18.13022148937263012, 15.02647892043544608 ) ) ;
#4107=DIRECTION ( 'NONE',  ( -1.000000000000000000, 0.000000000000000000, -0.000000000000000000 ) ) ;
#4108=ORIENTED_EDGE ( 'NONE', *, *, #30953, .T. ) ;
#4118=DIRECTION ( 'NONE',  ( 0.000000000000000000, 0.000000000000000000, 1.000000000000000000 ) ) ;
#4120=DIRECTION ( 'NONE',  ( -0.000000000000000000, -0.9135454576426059736, 0.4067366430757887730 ) ) ;
#4130=CARTESIAN_POINT ( 'NONE',  ( 10.00000000000000000, 9.188173127307297960, 40.98264845739753071 ) ) ;
#4136=LINE ( 'NONE', #50338, #9954 ) ;
#4151=CARTESIAN_POINT ( 'NONE',  ( -10.00000000000000000, 0.000000000000000000, 0.000000000000000000 ) ) ;
#4159=EDGE_CURVE ( 'NONE', #17752, #15096, #18200, .T. ) ;
#4172=ORIENTED_EDGE ( 'NONE', *, *, #48042, .T. ) ;
#4189=EDGE_LOOP ( 'NONE', ( #13945, #38307, #39494, #6690 ) ) ;
#4222=CARTESIAN_POINT ( 'NONE',  ( 10.00000000000000000, -5.202137450156129717, -37.22597642581163768 ) ) ;
#4224=AXIS2_PLACEMENT_3D ( 'NONE', #43272, #54892, #47772 ) ;
#4243=DIRECTION ( 'NONE',  ( 0.000000000000000000, 0.000000000000000000, 1.000000000000000000 ) ) ;
#4257=DIRECTION ( 'NONE',  ( 0.000000000000000000, -0.1045284632676570791, 0.9945218953682730678 ) ) ;
#4265=ORIENTED_EDGE ( 'NONE', *, *, #55749, .F. ) ;
#4274=AXIS2_PLACEMENT_3D ( 'NONE', #30254, #17869, #47186 ) ;
#4287=CARTESIAN_POINT ( 'NONE',  ( 10.00000000000000000, -0.8828120875898013420, -37.48860685352291711 ) ) ;
#4305=AXIS2_PLACEMENT_3D ( 'NONE', #15931, #17416, #16305 ) ;
#4307=ADVANCED_FACE ( 'NONE', ( #21089 ), #43686, .T. ) ;
#4321=EDGE_LOOP ( 'NONE', ( #45299, #29200, #72111, #52967 ) ) ;
#4326=PLANE ( 'NONE',  #72878 ) ;
#4329=FACE_OUTER_BOUND ( 'NONE', #41240, .T. ) ;
#4339=CIRCLE ( 'NONE', #25938, 37.49900000000000944 ) ;
#4367=CLOSED_SHELL ( 'NONE', ( #25388, #28567, #60637, #50250, #27416, #7301, #42177, #42548, #11987, #70442, #66033, #19959, #65638, #15108, #25792, #9334, #18733, #49473, #54238, #29272, #36587, #60870, #61668, #41937, #52385, #28921, #67624, #57032, #26316, #20773, #39146, #21995, #26792, #33722, #1773, #15820, #22720, #49421, #6485, #45364, #27395, #36906, #20292, #23971, #50768, #30057, #41315, #44432, #61945, #28448, #43966, #67494, #10806, #1657, #29456, #18250, #50142, #40580, #22057, #55922, #28579, #41491, #43375, #42536, #63668, #51958, #63318, #71549, #36842, #20966, #5146, #73667, #71017, #49614, #69432, #62769, #53229, #46463, #49480, #19537, #6930, #32403, #68929, #13002, #9789, #11445, #69342, #65724, #24938, #18691, #19450, #38989, #67194, #7209, #17178, #19852, #32062, #64163, #3668, #29851, #52649, #44833, #12285, #43426, #69781, #22231, #53047, #48181, #44744, #66709, #42711, #71081, #61915, #11988, #29026, #61626, #31080, #49282, #37467, #487, #15020, #18823, #64615, #20119, #17410, #18648, #1132, #40142, #65689, #44395, #35983, #29036, #4307, #30028, #40470, #22471, #10195, #66638, #10938, #47313, #6208, #37851, #7241, #26292, #7125, #31705, #67839, #62025, #23128, #65013, #26225, #41693, #38731, #10714, #26669, #24719, #72870, #16905, #54160, #9058, #62036, #61651, #10089, #51762, #11717, #71372, #969, #70695, #31468, #2503, #51277, #23349, #47561, #18085, #56877, #52276, #50767, #30058, #29753, #54691, #44938, #69863, #21189, #53273, #459, #68232, #47144, #6712, #56440, #40554, #71431, #36845, #57143, #15469, #35963, #52130, #51344, #53414, #69279, #23827, #7079, #59588, #52596, #23293, #69105, #42461, #39080, #26149, #3940, #62220, #62570, #12799, #66817, #22480, #16630, #11624, #21700, #21477, #4429, #47783, #72705, #19102, #71456, #20729, #28710, #7329, #29938, #23433, #52873, #55513, #15120, #17466, #53457, #49657, #41756, #60849, #67165, #63980, #25860, #41971, #36396, #41736, #11783, #25626 ) ) ;
#4377=EDGE_CURVE ( 'NONE', #69721, #16255, #57925, .T. ) ;
#4388=LINE ( 'NONE', #69654, #37159 ) ;
#4395=ORIENTED_EDGE ( 'NONE', *, *, #6229, .F. ) ;
#4408=FACE_BOUND ( 'NONE', #61031, .T. ) ;
#4415=CARTESIAN_POINT ( 'NONE',  ( 10.00000000000000000, -30.84782396557201878, -21.32104025579148399 ) ) ;
#4429=ADVANCED_FACE ( 'NONE', ( #57557 ), #29694, .F. ) ;
#4437=CIRCLE ( 'NONE', #44033, 37.49900000000001654 ) ;
#4438=VERTEX_POINT ( 'NONE', #12048 ) ;
#4449=AXIS2_PLACEMENT_3D ( 'NONE', #52576, #63881, #7088 ) ;
#4465=EDGE_LOOP ( 'NONE', ( #58724, #69348, #48995, #19993 ) ) ;
#4467=ORIENTED_EDGE ( 'NONE', *, *, #48547, .T. ) ;
#4477=DIRECTION ( 'NONE',  ( -1.000000000000000000, -0.000000000000000000, 0.000000000000000000 ) ) ;
#4482=EDGE_LOOP ( 'NONE', ( #60567, #58334, #36925, #2709 ) ) ;
#4492=CARTESIAN_POINT ( 'NONE',  ( 0.000000000000000000, 16.65560815589411092, 38.55633173627015253 ) ) ;
#4534=EDGE_LOOP ( 'NONE', ( #47252, #6336, #57708, #44476 ) ) ;
#4563=CIRCLE ( 'NONE', #44206, 16.00000000000000000 ) ;
#4588=DIRECTION ( 'NONE',  ( -1.000000000000000000, 0.000000000000000000, 0.000000000000000000 ) ) ;
#4591=EDGE_CURVE ( 'NONE', #66007, #3283, #55451, .T. ) ;
#4610=DIRECTION ( 'NONE',  ( -1.000000000000000000, -0.000000000000000000, -0.000000000000000000 ) ) ;
#4615=FACE_OUTER_BOUND ( 'NONE', #18932, .T. ) ;
#4624=ORIENTED_EDGE ( 'NONE', *, *, #32987, .T. ) ;
#4626=LINE ( 'NONE', #15507, #62479 ) ;
#4629=CIRCLE ( 'NONE', #43054, 37.49900000000000233 ) ;
#4640=VERTEX_POINT ( 'NONE', #10478 ) ;
#4649=VECTOR ( 'NONE', #69948, 1000.000000000000000 ) ;
#4662=FACE_OUTER_BOUND ( 'NONE', #24144, .T. ) ;
#4676=PLANE ( 'NONE',  #26590 ) ;
#4693=ORIENTED_EDGE ( 'NONE', *, *, #27120, .F. ) ;
#4695=EDGE_CURVE ( 'NONE', #59768, #27866, #73254, .T. ) ;
#4697=CARTESIAN_POINT ( 'NONE',  ( 10.00000000000000000, 6.555932627142952995, -37.01155633439051940 ) ) ;
#4702=AXIS2_PLACEMENT_3D ( 'NONE', #39515, #74078, #66952 ) ;
#4716=CIRCLE ( 'NONE', #34682, 16.00000000000000000 ) ;
#4735=ORIENTED_EDGE ( 'NONE', *, *, #8430, .T. ) ;
#4746=CARTESIAN_POINT ( 'NONE',  ( 10.00000000000000000, 21.32104025579114648, 30.84782396557224970 ) ) ;
#4772=DIRECTION ( 'NONE',  ( -0.000000000000000000, 0.1045284632676559550, -0.9945218953682731788 ) ) ;
#4784=EDGE_CURVE ( 'NONE', #36276, #32331, #35053, .T. ) ;
#4792=VECTOR ( 'NONE', #58107, 1000.000000000000000 ) ;
#4812=EDGE_CURVE ( 'NONE', #5732, #30754, #5607, .T. ) ;
#4818=VECTOR ( 'NONE', #15183, 1000.000000000000000 ) ;
#4828=FACE_OUTER_BOUND ( 'NONE', #65834, .T. ) ;
#4836=CARTESIAN_POINT ( 'NONE',  ( 0.000000000000000000, -27.75498641678764855, 31.52238457039590358 ) ) ;
#4845=AXIS2_PLACEMENT_3D ( 'NONE', #32784, #54988, #49350 ) ;
#4860=ORIENTED_EDGE ( 'NONE', *, *, #45851, .F. ) ;
#4880=CARTESIAN_POINT ( 'NONE',  ( 0.000000000000000000, -35.92658777277502935, -10.74501242461320594 ) ) ;
#4885=DIRECTION ( 'NONE',  ( 1.000000000000000000, 0.000000000000000000, -0.000000000000000000 ) ) ;
#4895=AXIS2_PLACEMENT_3D ( 'NONE', #50606, #51731, #10389 ) ;
#4900=EDGE_CURVE ( 'NONE', #71560, #20201, #53085, .T. ) ;
#4919=CARTESIAN_POINT ( 'NONE',  ( 10.00000000000000000, 0.000000000000000000, 0.000000000000000000 ) ) ;
#4937=CIRCLE ( 'NONE', #33732, 16.00000000000000000 ) ;
#4948=EDGE_CURVE ( 'NONE', #52639, #15350, #7469, .T. ) ;
#4974=LINE ( 'NONE', #44066, #35230 ) ;
#4995=DIRECTION ( 'NONE',  ( 1.000000000000000000, 0.000000000000000000, 0.000000000000000000 ) ) ;
#5012=EDGE_CURVE ( 'NONE', #23404, #8315, #71552, .T. ) ;
#5027=AXIS2_PLACEMENT_3D ( 'NONE', #69938, #34253, #69581 ) ;
#5032=CARTESIAN_POINT ( 'NONE',  ( 10.00000000000000000, 0.000000000000000000, 0.000000000000000000 ) ) ;
#5047=DIRECTION ( 'NONE',  ( 0.000000000000000000, 0.5877852522924683631, 0.8090169943749510040 ) ) ;
#5057=EDGE_CURVE ( 'NONE', #66402, #69599, #37412, .T. ) ;
#5061=DIRECTION ( 'NONE',  ( -1.000000000000000000, 0.000000000000000000, 0.000000000000000000 ) ) ;
#5064=EDGE_CURVE ( 'NONE', #12875, #64628, #26844, .T. ) ;
#5103=VERTEX_POINT ( 'NONE', #55425 ) ;
#5113=VERTEX_POINT ( 'NONE', #32847 ) ;
#5117=CYLINDRICAL_SURFACE ( 'NONE', #69036, 42.00000000000000000 ) ;
#5123=ORIENTED_EDGE ( 'NONE', *, *, #33243, .T. ) ;
#5127=ORIENTED_EDGE ( 'NONE', *, *, #3434, .T. ) ;
#5138=DIRECTION ( 'NONE',  ( 0.000000000000000000, 0.000000000000000000, -1.000000000000000000 ) ) ;
#5139=EDGE_LOOP ( 'NONE', ( #14067, #9558, #45126, #27072 ) ) ;
#5146=ADVANCED_FACE ( 'NONE', ( #27956 ), #16315, .T. ) ;
#5147=DIRECTION ( 'NONE',  ( 0.000000000000000000, 0.000000000000000000, 1.000000000000000000 ) ) ;
#5152=DIRECTION ( 'NONE',  ( 0.000000000000000000, 0.000000000000000000, 1.000000000000000000 ) ) ;
#5156=AXIS2_PLACEMENT_3D ( 'NONE', #61720, #20384, #26749 ) ;
#5158=DIRECTION ( 'NONE',  ( 0.000000000000000000, 0.000000000000000000, 1.000000000000000000 ) ) ;
#5174=EDGE_CURVE ( 'NONE', #1439, #47477, #65567, .T. ) ;
#5177=CARTESIAN_POINT ( 'NONE',  ( -3.000000000000000000, 23.59884966291538078, -12.14883922797231541 ) ) ;
#5193=CIRCLE ( 'NONE', #17197, 42.00000000000000000 ) ;
#5197=ORIENTED_EDGE ( 'NONE', *, *, #25289, .T. ) ;
#5221=CARTESIAN_POINT ( 'NONE',  ( 10.00000000000000000, 16.65560815589464028, -38.55633173626993937 ) ) ;
#5240=DIRECTION ( 'NONE',  ( 0.000000000000000000, 0.000000000000000000, 1.000000000000000000 ) ) ;
#5249=DIRECTION ( 'NONE',  ( 0.000000000000000000, 0.9945218953682730678, 0.1045284632676570929 ) ) ;
#5267=CARTESIAN_POINT ( 'NONE',  ( 0.000000000000000000, 0.000000000000000000, 0.000000000000000000 ) ) ;
#5283=AXIS2_PLACEMENT_3D ( 'NONE', #34153, #52176, #51072 ) ;
#5295=CARTESIAN_POINT ( 'NONE',  ( 10.00000000000000000, 30.00120703465205452, 22.64427369931179967 ) ) ;
#5296=ORIENTED_EDGE ( 'NONE', *, *, #28508, .T. ) ;
#5307=ORIENTED_EDGE ( 'NONE', *, *, #68793, .F. ) ;
#5308=CIRCLE ( 'NONE', #14886, 16.00000000000000355 ) ;
#5312=AXIS2_PLACEMENT_3D ( 'NONE', #30093, #42874, #65070 ) ;
#5322=ORIENTED_EDGE ( 'NONE', *, *, #53876, .T. ) ;
#5323=DIRECTION ( 'NONE',  ( 0.000000000000000000, 0.000000000000000000, 1.000000000000000000 ) ) ;
#5328=LINE ( 'NONE', #34992, #18842 ) ;
#5359=EDGE_CURVE ( 'NONE', #16188, #70424, #46746, .T. ) ;
#5373=EDGE_LOOP ( 'NONE', ( #8314, #19514, #952, #13113 ) ) ;
#5383=CARTESIAN_POINT ( 'NONE',  ( 0.000000000000000000, 9.615535125379096826, -24.73947219025904687 ) ) ;
#5391=ORIENTED_EDGE ( 'NONE', *, *, #70773, .F. ) ;
#5402=CARTESIAN_POINT ( 'NONE',  ( 0.000000000000000000, 22.48208911017551515, -35.47612816024499693 ) ) ;
#5414=VECTOR ( 'NONE', #55886, 1000.000000000000000 ) ;
#5417=LINE ( 'NONE', #58007, #27215 ) ;
#5435=AXIS2_PLACEMENT_3D ( 'NONE', #29881, #46449, #64481 ) ;
#5438=DIRECTION ( 'NONE',  ( 0.000000000000000000, 0.2079116908177664480, -0.9781476007338041345 ) ) ;
#5439=CYLINDRICAL_SURFACE ( 'NONE', #36880, 37.49900000000000233 ) ;
#5450=CARTESIAN_POINT ( 'NONE',  ( 10.00000000000000000, -37.01155633439063308, 6.555932627142289526 ) ) ;
#5484=ORIENTED_EDGE ( 'NONE', *, *, #28477, .F. ) ;
#5503=CYLINDRICAL_SURFACE ( 'NONE', #45826, 42.00000000000000000 ) ;
#5518=VERTEX_POINT ( 'NONE', #48939 ) ;
#5533=DIRECTION ( 'NONE',  ( -1.000000000000000000, -0.000000000000000000, 0.000000000000000000 ) ) ;
#5539=EDGE_CURVE ( 'NONE', #71364, #29066, #29577, .T. ) ;
#5544=CARTESIAN_POINT ( 'NONE',  ( -3.000000000000000000, 20.85821328998756385, -10.92862929874494959 ) ) ;
#5557=VERTEX_POINT ( 'NONE', #70765 ) ;
#5585=AXIS2_PLACEMENT_3D ( 'NONE', #73344, #10566, #68475 ) ;
#5586=CARTESIAN_POINT ( 'NONE',  ( 0.000000000000000000, 16.45098606841126454, 33.79645857604518966 ) ) ;
#5603=CARTESIAN_POINT ( 'NONE',  ( 0.000000000000000000, 33.79645857604513992, 16.45098606841138178 ) ) ;
#5607=LINE ( 'NONE', #51441, #21851 ) ;
#5622=LINE ( 'NONE', #51835, #49122 ) ;
#5623=DIRECTION ( 'NONE',  ( 1.000000000000000000, 0.000000000000000000, 0.000000000000000000 ) ) ;
#5661=DIRECTION ( 'NONE',  ( -1.000000000000000000, 0.000000000000000000, -0.000000000000000000 ) ) ;
#5677=ORIENTED_EDGE ( 'NONE', *, *, #55930, .F. ) ;
#5678=AXIS2_PLACEMENT_3D ( 'NONE', #58444, #70087, #1361 ) ;
#5686=EDGE_LOOP ( 'NONE', ( #29391, #17111, #23076, #28497 ) ) ;
#5689=ORIENTED_EDGE ( 'NONE', *, *, #22921, .T. ) ;
#5692=CYLINDRICAL_SURFACE ( 'NONE', #56103, 42.00000000000000000 ) ;
#5699=DIRECTION ( 'NONE',  ( -1.000000000000000000, -0.000000000000000000, -0.000000000000000000 ) ) ;
#5700=EDGE_CURVE ( 'NONE', #39132, #24073, #44805, .T. ) ;
#5705=CARTESIAN_POINT ( 'NONE',  ( -3.000000000000000000, -13.04903810567675038, 19.60159698893425428 ) ) ;
#5732=VERTEX_POINT ( 'NONE', #23715 ) ;
#5733=LINE ( 'NONE', #29370, #66072 ) ;
#5744=AXIS2_PLACEMENT_3D ( 'NONE', #37905, #60835, #9317 ) ;
#5779=DIRECTION ( 'NONE',  ( 0.000000000000000000, 0.2079116908177664758, -0.9781476007338042455 ) ) ;
#5795=DIRECTION ( 'NONE',  ( 1.000000000000000000, -0.000000000000000000, 0.000000000000000000 ) ) ;
#5797=CYLINDRICAL_SURFACE ( 'NONE', #398, 42.00000000000000000 ) ;
#5803=CARTESIAN_POINT ( 'NONE',  ( 0.000000000000000000, 23.59884966291538433, -12.14883922797231719 ) ) ;
#5808=CARTESIAN_POINT ( 'NONE',  ( -3.000000000000000000, 22.07842321921481243, 8.187992925817422218 ) ) ;
#5868=CARTESIAN_POINT ( 'NONE',  ( -3.000000000000000000, 5.835314593368477354, 22.81335362449854642 ) ) ;
#5884=FACE_OUTER_BOUND ( 'NONE', #17690, .T. ) ;
#5893=AXIS2_PLACEMENT_3D ( 'NONE', #69937, #11679, #831 ) ;
#5896=VECTOR ( 'NONE', #50448, 1000.000000000000000 ) ;
#5901=DIRECTION ( 'NONE',  ( 0.000000000000000000, -0.9876883405951358830, -0.1564344650402420822 ) ) ;
#5902=EDGE_CURVE ( 'NONE', #23253, #37124, #24823, .T. ) ;
#5917=CIRCLE ( 'NONE', #47917, 42.00000000000000000 ) ;
#5920=DIRECTION ( 'NONE',  ( 0.000000000000000000, -0.5877852522924689183, -0.8090169943749504489 ) ) ;
#5932=VECTOR ( 'NONE', #15839, 1000.000000000000000 ) ;
#5945=DIRECTION ( 'NONE',  ( -1.000000000000000000, 0.000000000000000000, 0.000000000000000000 ) ) ;
#5946=AXIS2_PLACEMENT_3D ( 'NONE', #11992, #34933, #52213 ) ;
#5951=EDGE_CURVE ( 'NONE', #17707, #62900, #53398, .T. ) ;
#5954=ORIENTED_EDGE ( 'NONE', *, *, #56561, .T. ) ;
#5963=FACE_OUTER_BOUND ( 'NONE', #2498, .T. ) ;
#5970=AXIS2_PLACEMENT_3D ( 'NONE', #54397, #21272, #10013 ) ;
#5979=FACE_OUTER_BOUND ( 'NONE', #25092, .T. ) ;
#5993=CARTESIAN_POINT ( 'NONE',  ( 0.000000000000000000, 0.000000000000000000, 0.000000000000000000 ) ) ;
#6004=AXIS2_PLACEMENT_3D ( 'NONE', #66961, #26733, #54946 ) ;
#6006=CARTESIAN_POINT ( 'NONE',  ( -3.000000000000000000, 6.762365576493310826, 25.66652317338401090 ) ) ;
#6008=CARTESIAN_POINT ( 'NONE',  ( 10.00000000000000000, 21.32104025579114648, 30.84782396557224970 ) ) ;
#6023=EDGE_LOOP ( 'NONE', ( #15414, #37830, #40484, #13524 ) ) ;
#6024=CARTESIAN_POINT ( 'NONE',  ( -3.000000000000000000, 9.615535125379096826, -24.73947219025905042 ) ) ;
#6071=CARTESIAN_POINT ( 'NONE',  ( 10.00000000000000000, 0.000000000000000000, 0.000000000000000000 ) ) ;
#6079=EDGE_CURVE ( 'NONE', #46417, #11359, #34428, .T. ) ;
#6086=DIRECTION ( 'NONE',  ( -1.000000000000000000, -0.000000000000000000, -0.000000000000000000 ) ) ;
#6088=DIRECTION ( 'NONE',  ( 0.000000000000000000, 0.9135454576426005335, 0.4067366430758010409 ) ) ;
#6102=ORIENTED_EDGE ( 'NONE', *, *, #47024, .T. ) ;
#6107=DIRECTION ( 'NONE',  ( 0.000000000000000000, 0.000000000000000000, -1.000000000000000000 ) ) ;
#6115=AXIS2_PLACEMENT_3D ( 'NONE', #34803, #629, #41547 ) ;
#6121=ORIENTED_EDGE ( 'NONE', *, *, #14142, .T. ) ;
#6129=ORIENTED_EDGE ( 'NONE', *, *, #36563, .T. ) ;
#6149=CARTESIAN_POINT ( 'NONE',  ( 0.000000000000000000, -41.91543099594816368, -2.663952781846588014 ) ) ;
#6151=EDGE_CURVE ( 'NONE', #65031, #20728, #33802, .T. ) ;
#6156=CIRCLE ( 'NONE', #13313, 37.49900000000000233 ) ;
#6157=CARTESIAN_POINT ( 'NONE',  ( 10.00000000000000000, 0.000000000000000000, 0.000000000000000000 ) ) ;
#6160=EDGE_CURVE ( 'NONE', #53009, #64628, #68015, .T. ) ;
#6161=EDGE_CURVE ( 'NONE', #30392, #55889, #55985, .T. ) ;
#6162=DIRECTION ( 'NONE',  ( 0.000000000000000000, 0.9510565162951546414, -0.3090169943749442871 ) ) ;
#6177=CARTESIAN_POINT ( 'NONE',  ( 10.00000000000000000, 0.000000000000000000, 0.000000000000000000 ) ) ;
#6181=FACE_OUTER_BOUND ( 'NONE', #554, .T. ) ;
#6187=ORIENTED_EDGE ( 'NONE', *, *, #46121, .T. ) ;
#6193=ORIENTED_EDGE ( 'NONE', *, *, #57591, .F. ) ;
#6197=ORIENTED_EDGE ( 'NONE', *, *, #7880, .F. ) ;
#6204=ORIENTED_EDGE ( 'NONE', *, *, #17311, .T. ) ;
#6208=ADVANCED_FACE ( 'NONE', ( #27405 ), #50340, .T. ) ;
#6225=DIRECTION ( 'NONE',  ( 0.000000000000000000, 0.000000000000000000, 1.000000000000000000 ) ) ;
#6229=EDGE_CURVE ( 'NONE', #72554, #24755, #46204, .T. ) ;
#6246=FACE_OUTER_BOUND ( 'NONE', #60862, .T. ) ;
#6250=ORIENTED_EDGE ( 'NONE', *, *, #6151, .F. ) ;
#6253=CARTESIAN_POINT ( 'NONE',  ( 10.00000000000000000, -27.05870788708213226, -26.08949754953053102 ) ) ;
#6259=DIRECTION ( 'NONE',  ( 0.000000000000000000, 0.000000000000000000, 1.000000000000000000 ) ) ;
#6268=CARTESIAN_POINT ( 'NONE',  ( 10.00000000000000000, -35.53030884539094103, 12.26510123303246935 ) ) ;
#6269=CARTESIAN_POINT ( 'NONE',  ( 0.000000000000000000, 10.96151621346487914, 35.95386929396260456 ) ) ;
#6283=DIRECTION ( 'NONE',  ( 0.000000000000000000, -0.9510565162951506446, -0.3090169943749562775 ) ) ;
#6290=EDGE_LOOP ( 'NONE', ( #58941, #34022, #35259, #48466 ) ) ;
#6291=EDGE_CURVE ( 'NONE', #20918, #33855, #63501, .T. ) ;
#6293=CARTESIAN_POINT ( 'NONE',  ( 10.00000000000000000, -33.80338159004273280, -16.23288003029533044 ) ) ;
#6298=DIRECTION ( 'NONE',  ( -1.000000000000000000, 0.000000000000000000, 0.000000000000000000 ) ) ;
#6314=DIRECTION ( 'NONE',  ( -1.000000000000000000, 0.000000000000000000, -0.000000000000000000 ) ) ;
#6328=ORIENTED_EDGE ( 'NONE', *, *, #42689, .T. ) ;
#6332=CIRCLE ( 'NONE', #36306, 37.49900000000000233 ) ;
#6333=EDGE_CURVE ( 'NONE', #24241, #7257, #69853, .T. ) ;
#6336=ORIENTED_EDGE ( 'NONE', *, *, #19594, .T. ) ;
#6355=DIRECTION ( 'NONE',  ( -1.000000000000000000, 0.000000000000000000, 0.000000000000000000 ) ) ;
#6358=DIRECTION ( 'NONE',  ( 0.000000000000000000, 0.000000000000000000, 1.000000000000000000 ) ) ;
#6363=EDGE_CURVE ( 'NONE', #27461, #26343, #27222, .T. ) ;
#6365=CARTESIAN_POINT ( 'NONE',  ( 10.00000000000000000, 0.8828120875900632436, 37.48860685352291000 ) ) ;
#6369=CARTESIAN_POINT ( 'NONE',  ( 10.00000000000000000, -17.67226234102849958, 33.17418723428301774 ) ) ;
#6372=EDGE_CURVE ( 'NONE', #48989, #35036, #60832, .T. ) ;
#6384=DIRECTION ( 'NONE',  ( -1.000000000000000000, 0.000000000000000000, 0.000000000000000000 ) ) ;
#6401=AXIS2_PLACEMENT_3D ( 'NONE', #6623, #63406, #52471 ) ;
#6404=ORIENTED_EDGE ( 'NONE', *, *, #12033, .F. ) ;
#6416=DIRECTION ( 'NONE',  ( -0.000000000000000000, -0.9135454576426004225, -0.4067366430758009854 ) ) ;
#6417=DIRECTION ( 'NONE',  ( -1.000000000000000000, 0.000000000000000000, 0.000000000000000000 ) ) ;
#6426=ORIENTED_EDGE ( 'NONE', *, *, #32725, .F. ) ;
#6427=VECTOR ( 'NONE', #7182, 1000.000000000000000 ) ;
#6440=FACE_OUTER_BOUND ( 'NONE', #66156, .T. ) ;
#6450=EDGE_CURVE ( 'NONE', #11255, #53009, #36376, .T. ) ;
#6455=CARTESIAN_POINT ( 'NONE',  ( 0.000000000000000000, 24.81905959214274660, -9.408202855044498492 ) ) ;
#6457=CIRCLE ( 'NONE', #12446, 37.49900000000000944 ) ;
#6459=PRODUCT_DEFINITION_FORMATION_WITH_SPECIFIED_SOURCE ( 'ANY', '', #68031, .NOT_KNOWN. ) ;
#6462=CARTESIAN_POINT ( 'NONE',  ( 10.00000000000000000, 0.000000000000000000, 0.000000000000000000 ) ) ;
#6476=LINE ( 'NONE', #29739, #14253 ) ;
#6485=ADVANCED_FACE ( 'NONE', ( #48041 ), #70955, .T. ) ;
#6510=DIRECTION ( 'NONE',  ( 0.000000000000000000, 0.000000000000000000, 1.000000000000000000 ) ) ;
#6516=DIRECTION ( 'NONE',  ( 0.000000000000000000, 0.3090169943749442316, 0.9510565162951545304 ) ) ;
#6535=CARTESIAN_POINT ( 'NONE',  ( 10.00000000000000000, 0.000000000000000000, 0.000000000000000000 ) ) ;
#6537=DIRECTION ( 'NONE',  ( 1.000000000000000000, -0.000000000000000000, -0.000000000000000000 ) ) ;
#6540=DIRECTION ( 'NONE',  ( 0.000000000000000000, -0.5877852522924689183, -0.8090169943749504489 ) ) ;
#6541=AXIS2_PLACEMENT_3D ( 'NONE', #13481, #30756, #53705 ) ;
#6546=EDGE_LOOP ( 'NONE', ( #5677, #17010, #64304, #65458 ) ) ;
#6572=AXIS2_PLACEMENT_3D ( 'NONE', #27684, #16784, #5147 ) ;
#6575=DIRECTION ( 'NONE',  ( 0.000000000000000000, -0.1564344650402170744, -0.9876883405951398798 ) ) ;
#6580=DIRECTION ( 'NONE',  ( -1.000000000000000000, 0.000000000000000000, -0.000000000000000000 ) ) ;
#6606=ORIENTED_EDGE ( 'NONE', *, *, #31120, .F. ) ;
#6607=LINE ( 'NONE', #8734, #12052 ) ;
#6623=CARTESIAN_POINT ( 'NONE',  ( -3.000000000000000000, 14.60985201121729737, -18.46759930825687945 ) ) ;
#6652=CARTESIAN_POINT ( 'NONE',  ( 0.000000000000000000, -0.8828120875903202602, 37.48860685352291000 ) ) ;
#6668=VERTEX_POINT ( 'NONE', #44637 ) ;
#6677=ORIENTED_EDGE ( 'NONE', *, *, #34922, .T. ) ;
#6686=VERTEX_POINT ( 'NONE', #10407 ) ;
#6690=ORIENTED_EDGE ( 'NONE', *, *, #25117, .F. ) ;
#6691=DIRECTION ( 'NONE',  ( 0.000000000000000000, 0.000000000000000000, 1.000000000000000000 ) ) ;
#6712=ADVANCED_FACE ( 'NONE', ( #40848 ), #23915, .F. ) ;
#6713=DIRECTION ( 'NONE',  ( -0.000000000000000000, -0.4067366430757898277, -0.9135454576426055295 ) ) ;
#6719=DIRECTION ( 'NONE',  ( -0.000000000000000000, -0.3090169943749573878, 0.9510565162951503115 ) ) ;
#6729=CARTESIAN_POINT ( 'NONE',  ( 10.00000000000000000, 0.6853352020790449695, 37.58145647212454321 ) ) ;
#6752=LINE ( 'NONE', #40601, #19747 ) ;
#6765=CARTESIAN_POINT ( 'NONE',  ( 10.00000000000000000, -10.74501242461258244, -35.92658777277521409 ) ) ;
#6771=EDGE_CURVE ( 'NONE', #12946, #3354, #71195, .T. ) ;
#6774=EDGE_CURVE ( 'NONE', #35754, #26913, #35200, .T. ) ;
#6775=CARTESIAN_POINT ( 'NONE',  ( -3.000000000000000000, 22.07842321921481243, 8.187992925817422218 ) ) ;
#6790=CARTESIAN_POINT ( 'NONE',  ( 10.00000000000000000, 22.48208911017500355, 35.47612816024531668 ) ) ;
#6792=LINE ( 'NONE', #8266, #45936 ) ;
#6796=FACE_OUTER_BOUND ( 'NONE', #5373, .T. ) ;
#6799=ORIENTED_EDGE ( 'NONE', *, *, #63586, .T. ) ;
#6802=DIRECTION ( 'NONE',  ( -1.000000000000000000, -0.000000000000000000, 0.000000000000000000 ) ) ;
#6807=EDGE_CURVE ( 'NONE', #5113, #61245, #8803, .T. ) ;
#6808=CARTESIAN_POINT ( 'NONE',  ( 10.00000000000000000, -36.88895765772637247, 6.736453364083436313 ) ) ;
#6822=CARTESIAN_POINT ( 'NONE',  ( 0.000000000000000000, -37.22597642581153821, -5.202137450156795850 ) ) ;
#6823=VECTOR ( 'NONE', #40176, 1000.000000000000000 ) ;
#6828=CARTESIAN_POINT ( 'NONE',  ( 0.000000000000000000, 38.55633173627034438, -16.65560815589369881 ) ) ;
#6832=VECTOR ( 'NONE', #20872, 1000.000000000000000 ) ;
#6840=ORIENTED_EDGE ( 'NONE', *, *, #68105, .F. ) ;
#6854=AXIS2_PLACEMENT_3D ( 'NONE', #28837, #23210, #52884 ) ;
#6870=CARTESIAN_POINT ( 'NONE',  ( 0.000000000000000000, 0.000000000000000000, 0.000000000000000000 ) ) ;
#6879=ORIENTED_EDGE ( 'NONE', *, *, #28754, .F. ) ;
#6909=CARTESIAN_POINT ( 'NONE',  ( 0.000000000000000000, 27.13269053701096922, 25.88420570971410228 ) ) ;
#6912=EDGE_LOOP ( 'NONE', ( #43721, #32938, #12694, #4735 ) ) ;
#6914=EDGE_LOOP ( 'NONE', ( #17202, #9152, #57698, #31329 ) ) ;
#6922=EDGE_LOOP ( 'NONE', ( #39250, #7519, #61602, #500 ) ) ;
#6928=ORIENTED_EDGE ( 'NONE', *, *, #65558, .T. ) ;
#6930=ADVANCED_FACE ( 'NONE', ( #42683 ), #35922, .T. ) ;
#6932=CARTESIAN_POINT ( 'NONE',  ( 0.000000000000000000, 40.68715046381927891, 10.41901085202092858 ) ) ;
#6952=CARTESIAN_POINT ( 'NONE',  ( 10.00000000000000000, 0.000000000000000000, 0.000000000000000000 ) ) ;
#6955=CYLINDRICAL_SURFACE ( 'NONE', #51023, 42.00000000000000000 ) ;
#6965=AXIS2_PLACEMENT_3D ( 'NONE', #34726, #52007, #197 ) ;
#6977=CYLINDRICAL_SURFACE ( 'NONE', #40073, 16.00000000000000000 ) ;
#7002=FACE_OUTER_BOUND ( 'NONE', #16624, .T. ) ;
#7006=VECTOR ( 'NONE', #54632, 1000.000000000000000 ) ;
#7016=EDGE_CURVE ( 'NONE', #60338, #26546, #11266, .T. ) ;
#7021=FACE_OUTER_BOUND ( 'NONE', #53424, .T. ) ;
#7038=LINE ( 'NONE', #40519, #23756 ) ;
#7039=AXIS2_PLACEMENT_3D ( 'NONE', #6535, #42589, #20756 ) ;
#7052=CYLINDRICAL_SURFACE ( 'NONE', #1420, 42.00000000000000000 ) ;
#7053=CARTESIAN_POINT ( 'NONE',  ( 10.00000000000000000, -33.79645857604525361, 16.45098606841114730 ) ) ;
#7056=VERTEX_POINT ( 'NONE', #49053 ) ;
#7061=ORIENTED_EDGE ( 'NONE', *, *, #48033, .T. ) ;
#7074=CIRCLE ( 'NONE', #55046, 16.00000000000000000 ) ;
#7076=DIRECTION ( 'NONE',  ( -1.000000000000000000, -0.000000000000000000, 0.000000000000000000 ) ) ;
#7079=ADVANCED_FACE ( 'NONE', ( #4329 ), #44162, .F. ) ;
#7088=DIRECTION ( 'NONE',  ( 0.000000000000000000, 0.000000000000000000, 1.000000000000000000 ) ) ;
#7096=CARTESIAN_POINT ( 'NONE',  ( 4.999999999999999112, -40.98264845739755202, 9.188173127307159405 ) ) ;
#7103=ORIENTED_EDGE ( 'NONE', *, *, #6363, .F. ) ;
#7110=ORIENTED_EDGE ( 'NONE', *, *, #37391, .F. ) ;
#7113=EDGE_LOOP ( 'NONE', ( #6102, #61489, #13011, #14790 ) ) ;
#7125=ADVANCED_FACE ( 'NONE', ( #30509 ), #3092, .T. ) ;
#7147=EDGE_CURVE ( 'NONE', #34118, #41638, #25984, .T. ) ;
#7153=DIRECTION ( 'NONE',  ( 0.000000000000000000, -0.9510565162951543083, 0.3090169943749449533 ) ) ;
#7156=AXIS2_PLACEMENT_3D ( 'NONE', #70281, #13881, #36820 ) ;
#7180=DIRECTION ( 'NONE',  ( 0.000000000000000000, 0.000000000000000000, 1.000000000000000000 ) ) ;
#7182=DIRECTION ( 'NONE',  ( 1.000000000000000000, -0.000000000000000000, -0.000000000000000000 ) ) ;
#7190=DIRECTION ( 'NONE',  ( 0.000000000000000000, 0.7071067811865437980, 0.7071067811865512365 ) ) ;
#7203=AXIS2_PLACEMENT_3D ( 'NONE', #27596, #44151, #49776 ) ;
#7206=ORIENTED_EDGE ( 'NONE', *, *, #25740, .T. ) ;
#7208=EDGE_LOOP ( 'NONE', ( #56918, #29271, #51051, #8144 ) ) ;
#7209=ADVANCED_FACE ( 'NONE', ( #36524 ), #24880, .T. ) ;
#7238=CARTESIAN_POINT ( 'NONE',  ( 0.000000000000000000, 33.80338159004307386, -16.23288003029461279 ) ) ;
#7239=CIRCLE ( 'NONE', #14415, 37.49900000000000944 ) ;
#7241=ADVANCED_FACE ( 'NONE', ( #42547 ), #59105, .T. ) ;
#7247=DIRECTION ( 'NONE',  ( 0.000000000000000000, 0.000000000000000000, -1.000000000000000000 ) ) ;
#7253=DIRECTION ( 'NONE',  ( -1.000000000000000000, -0.000000000000000000, -0.000000000000000000 ) ) ;
#7257=VERTEX_POINT ( 'NONE', #60227 ) ;
#7276=DIRECTION ( 'NONE',  ( 0.000000000000000000, -0.9135454576426005335, -0.4067366430758010409 ) ) ;
#7288=VECTOR ( 'NONE', #6416, 1000.000000000000114 ) ;
#7291=VECTOR ( 'NONE', #10130, 1000.000000000000000 ) ;
#7301=ADVANCED_FACE ( 'NONE', ( #22510 ), #45076, .T. ) ;
#7308=VERTEX_POINT ( 'NONE', #67998 ) ;
#7324=FACE_OUTER_BOUND ( 'NONE', #39487, .T. ) ;
#7327=CARTESIAN_POINT ( 'NONE',  ( 0.000000000000000000, -6.736453364083290651, -36.88895765772640090 ) ) ;
#7329=ADVANCED_FACE ( 'NONE', ( #5979 ), #10855, .F. ) ;
#7342=AXIS2_PLACEMENT_3D ( 'NONE', #18794, #12787, #60164 ) ;
#7355=CARTESIAN_POINT ( 'NONE',  ( 10.00000000000000000, 16.23288003029497162, 33.80338159004289622 ) ) ;
#7361=FACE_OUTER_BOUND ( 'NONE', #66051, .T. ) ;
#7385=EDGE_CURVE ( 'NONE', #14108, #68714, #30465, .T. ) ;
#7390=ORIENTED_EDGE ( 'NONE', *, *, #37935, .T. ) ;
#7391=CIRCLE ( 'NONE', #33797, 16.00000000000000355 ) ;
#7397=DIRECTION ( 'NONE',  ( 0.000000000000000000, -0.8660254037844363761, -0.5000000000000039968 ) ) ;
#7404=ORIENTED_EDGE ( 'NONE', *, *, #4948, .F. ) ;
#7412=EDGE_LOOP ( 'NONE', ( #69840, #40993, #1827, #3512 ) ) ;
#7418=EDGE_CURVE ( 'NONE', #71534, #62834, #24524, .T. ) ;
#7439=VERTEX_POINT ( 'NONE', #52541 ) ;
#7462=LINE ( 'NONE', #30376, #72064 ) ;
#7464=ORIENTED_EDGE ( 'NONE', *, *, #752, .F. ) ;
#7469=CIRCLE ( 'NONE', #49487, 42.00000000000000000 ) ;
#7476=CARTESIAN_POINT ( 'NONE',  ( 10.00000000000000000, 35.95386929396256903, -10.96151621346501237 ) ) ;
#7478=EDGE_CURVE ( 'NONE', #8315, #32534, #31089, .T. ) ;
#7481=LINE ( 'NONE', #41684, #18410 ) ;
#7495=CARTESIAN_POINT ( 'NONE',  ( 10.00000000000000000, 29.81001611431041098, -22.74946021919100403 ) ) ;
#7501=CYLINDRICAL_SURFACE ( 'NONE', #8096, 42.00000000000000000 ) ;
#7506=ORIENTED_EDGE ( 'NONE', *, *, #39463, .T. ) ;
#7515=ORIENTED_EDGE ( 'NONE', *, *, #38555, .T. ) ;
#7519=ORIENTED_EDGE ( 'NONE', *, *, #6774, .T. ) ;
#7532=AXIS2_PLACEMENT_3D ( 'NONE', #42642, #59948, #36252 ) ;
#7540=FACE_OUTER_BOUND ( 'NONE', #18123, .T. ) ;
#7551=CARTESIAN_POINT ( 'NONE',  ( 0.000000000000000000, 0.000000000000000000, 0.000000000000000000 ) ) ;
#7572=ORIENTED_EDGE ( 'NONE', *, *, #44389, .T. ) ;
#7574=ORIENTED_EDGE ( 'NONE', *, *, #26619, .T. ) ;
#7592=AXIS2_PLACEMENT_3D ( 'NONE', #68395, #10488, #17251 ) ;
#7595=AXIS2_PLACEMENT_3D ( 'NONE', #15863, #38794, #61729 ) ;
#7596=CARTESIAN_POINT ( 'NONE',  ( 5.000000000000000000, -32.34446384429989507, 26.79245525562703278 ) ) ;
#7598=LINE ( 'NONE', #2371, #24593 ) ;
#7606=ORIENTED_EDGE ( 'NONE', *, *, #45768, .T. ) ;
#7617=CARTESIAN_POINT ( 'NONE',  ( -3.000000000000000000, 5.835314593368477354, 22.81335362449854642 ) ) ;
#7622=CARTESIAN_POINT ( 'NONE',  ( 10.00000000000000000, 33.79645857604513992, -16.45098606841138178 ) ) ;
#7634=EDGE_CURVE ( 'NONE', #60432, #36593, #61166, .T. ) ;
#7642=VECTOR ( 'NONE', #36477, 1000.000000000000000 ) ;
#7667=ORIENTED_EDGE ( 'NONE', *, *, #23459, .T. ) ;
#7677=VERTEX_POINT ( 'NONE', #68662 ) ;
#7698=LINE ( 'NONE', #37011, #39634 ) ;
#7714=EDGE_CURVE ( 'NONE', #11647, #47006, #71302, .T. ) ;
#7716=LINE ( 'NONE', #13351, #29345 ) ;
#7726=DIRECTION ( 'NONE',  ( -1.000000000000000000, 0.000000000000000000, 0.000000000000000000 ) ) ;
#7727=DIRECTION ( 'NONE',  ( 0.000000000000000000, 0.000000000000000000, 1.000000000000000000 ) ) ;
#7753=CARTESIAN_POINT ( 'NONE',  ( 10.00000000000000000, 30.84782396557218931, 21.32104025579126017 ) ) ;
#7754=VERTEX_POINT ( 'NONE', #40082 ) ;
#7755=ORIENTED_EDGE ( 'NONE', *, *, #65848, .F. ) ;
#7756=CIRCLE ( 'NONE', #66579, 15.99999999999999645 ) ;
#7761=LINE ( 'NONE', #47243, #65241 ) ;
#7763=DIRECTION ( 'NONE',  ( 0.000000000000000000, 0.000000000000000000, -1.000000000000000000 ) ) ;
#7785=CARTESIAN_POINT ( 'NONE',  ( 4.999999999999999112, 21.40280677340371795, 36.13751322684426270 ) ) ;
#7789=CARTESIAN_POINT ( 'NONE',  ( 0.000000000000000000, 5.835314593368477354, 22.81335362449854642 ) ) ;
#7792=EDGE_LOOP ( 'NONE', ( #61292, #32926, #66037, #71907 ) ) ;
#7794=FACE_OUTER_BOUND ( 'NONE', #47633, .T. ) ;
#7795=EDGE_CURVE ( 'NONE', #8585, #39671, #23359, .T. ) ;
#7806=ORIENTED_EDGE ( 'NONE', *, *, #69005, .F. ) ;
#7815=LINE ( 'NONE', #29996, #19554 ) ;
#7827=CARTESIAN_POINT ( 'NONE',  ( 10.00000000000000000, -33.79645857604501913, -16.45098606841161626 ) ) ;
#7841=DIRECTION ( 'NONE',  ( -0.000000000000000000, 0.8660254037844368202, 0.5000000000000031086 ) ) ;
#7845=AXIS2_PLACEMENT_3D ( 'NONE', #34413, #39330, #11122 ) ;
#7849=ORIENTED_EDGE ( 'NONE', *, *, #24936, .T. ) ;
#7862=VERTEX_POINT ( 'NONE', #69755 ) ;
#7880=EDGE_CURVE ( 'NONE', #19238, #67909, #52456, .T. ) ;
#7890=DIRECTION ( 'NONE',  ( -1.000000000000000000, 0.000000000000000000, 0.000000000000000000 ) ) ;
#7891=CARTESIAN_POINT ( 'NONE',  ( -3.000000000000000000, 20.85821328998756385, -10.92862929874494959 ) ) ;
#7894=PLANE ( 'NONE',  #18115 ) ;
#7932=ORIENTED_EDGE ( 'NONE', *, *, #2305, .F. ) ;
#7934=ORIENTED_EDGE ( 'NONE', *, *, #546, .F. ) ;
#7936=ORIENTED_EDGE ( 'NONE', *, *, #24354, .T. ) ;
#7938=EDGE_LOOP ( 'NONE', ( #34410, #30228, #72645, #8142 ) ) ;
#7951=EDGE_CURVE ( 'NONE', #65031, #27079, #7716, .T. ) ;
#7958=EDGE_CURVE ( 'NONE', #57048, #66402, #52157, .T. ) ;
#7959=LINE ( 'NONE', #70354, #14850 ) ;
#7962=EDGE_CURVE ( 'NONE', #5557, #26897, #29890, .T. ) ;
#7975=VERTEX_POINT ( 'NONE', #18616 ) ;
#7984=CARTESIAN_POINT ( 'NONE',  ( 5.000000000000000000, -15.48615015657610705, 39.04073710021338428 ) ) ;
#7993=DIRECTION ( 'NONE',  ( -1.000000000000000000, 0.000000000000000000, -0.000000000000000000 ) ) ;
#7997=EDGE_CURVE ( 'NONE', #26343, #18301, #35906, .T. ) ;
#8008=DIRECTION ( 'NONE',  ( -1.000000000000000000, 0.000000000000000000, 0.000000000000000000 ) ) ;
#8038=ORIENTED_EDGE ( 'NONE', *, *, #53131, .T. ) ;
#8074=ORIENTED_EDGE ( 'NONE', *, *, #1235, .T. ) ;
#8086=CARTESIAN_POINT ( 'NONE',  ( 0.000000000000000000, -33.00180498840060039, 17.80606268964528027 ) ) ;
#8090=AXIS2_PLACEMENT_3D ( 'NONE', #67119, #62904, #11361 ) ;
#8096=AXIS2_PLACEMENT_3D ( 'NONE', #42087, #28655, #25520 ) ;
#8114=AXIS2_PLACEMENT_3D ( 'NONE', #7551, #46296, #69949 ) ;
#8125=EDGE_CURVE ( 'NONE', #39121, #67207, #54689, .T. ) ;
#8142=ORIENTED_EDGE ( 'NONE', *, *, #16455, .T. ) ;
#8143=CARTESIAN_POINT ( 'NONE',  ( -3.000000000000000000, 22.07842321921492612, -8.187992925817130896 ) ) ;
#8144=ORIENTED_EDGE ( 'NONE', *, *, #24462, .T. ) ;
#8146=CIRCLE ( 'NONE', #26172, 16.00000000000000355 ) ;
#8168=AXIS2_PLACEMENT_3D ( 'NONE', #56179, #21585, #67833 ) ;
#8169=ORIENTED_EDGE ( 'NONE', *, *, #34640, .T. ) ;
#8172=AXIS2_PLACEMENT_3D ( 'NONE', #54600, #7993, #8371 ) ;
#8175=CIRCLE ( 'NONE', #23803, 16.00000000000000000 ) ;
#8192=VECTOR ( 'NONE', #19752, 1000.000000000000000 ) ;
#8199=EDGE_CURVE ( 'NONE', #42329, #53520, #21956, .T. ) ;
#8203=VERTEX_POINT ( 'NONE', #39998 ) ;
#8210=AXIS2_PLACEMENT_3D ( 'NONE', #64055, #18900, #41846 ) ;
#8213=VERTEX_POINT ( 'NONE', #45276 ) ;
#8217=FACE_OUTER_BOUND ( 'NONE', #586, .T. ) ;
#8218=AXIS2_PLACEMENT_3D ( 'NONE', #5705, #41020, #40641 ) ;
#8222=DIRECTION ( 'NONE',  ( 0.000000000000000000, -0.9876883405951393247, 0.1564344650402204329 ) ) ;
#8225=ORIENTED_EDGE ( 'NONE', *, *, #32602, .T. ) ;
#8248=VERTEX_POINT ( 'NONE', #62955 ) ;
#8251=AXIS2_PLACEMENT_3D ( 'NONE', #51672, #52032, #51294 ) ;
#8260=LINE ( 'NONE', #36826, #74126 ) ;
#8262=FACE_OUTER_BOUND ( 'NONE', #72015, .T. ) ;
#8266=CARTESIAN_POINT ( 'NONE',  ( 10.00000000000000000, 6.736453364083557105, 36.88895765772635826 ) ) ;
#8268=AXIS2_PLACEMENT_3D ( 'NONE', #31630, #67334, #50403 ) ;
#8292=DIRECTION ( 'NONE',  ( 0.000000000000000000, -0.4999999999999920064, -0.8660254037844432595 ) ) ;
#8299=AXIS2_PLACEMENT_3D ( 'NONE', #57497, #33815, #22544 ) ;
#8312=ORIENTED_EDGE ( 'NONE', *, *, #10796, .T. ) ;
#8314=ORIENTED_EDGE ( 'NONE', *, *, #54736, .T. ) ;
#8315=VERTEX_POINT ( 'NONE', #22333 ) ;
#8318=CARTESIAN_POINT ( 'NONE',  ( 10.00000000000000000, 0.000000000000000000, 0.000000000000000000 ) ) ;
#8319=DIRECTION ( 'NONE',  ( 0.000000000000000000, -0.9510565162951500895, -0.3090169943749583314 ) ) ;
#8342=DIRECTION ( 'NONE',  ( -1.000000000000000000, 0.000000000000000000, 0.000000000000000000 ) ) ;
#8352=CARTESIAN_POINT ( 'NONE',  ( 10.00000000000000000, 27.05870788708231700, 26.08949754953034272 ) ) ;
#8354=CARTESIAN_POINT ( 'NONE',  ( 0.000000000000000000, -23.29833615347109443, 3.418703333116492438 ) ) ;
#8371=DIRECTION ( 'NONE',  ( 0.000000000000000000, 0.9510565162951544194, -0.3090169943749446757 ) ) ;
#8382=DIRECTION ( 'NONE',  ( 0.000000000000000000, 0.000000000000000000, 1.000000000000000000 ) ) ;
#8396=AXIS2_PLACEMENT_3D ( 'NONE', #44658, #9684, #67573 ) ;
#8397=EDGE_CURVE ( 'NONE', #70426, #43951, #68567, .T. ) ;
#8402=ORIENTED_EDGE ( 'NONE', *, *, #12589, .T. ) ;
#8419=EDGE_CURVE ( 'NONE', #11350, #38975, #12519, .T. ) ;
#8426=ORIENTED_EDGE ( 'NONE', *, *, #4591, .F. ) ;
#8430=EDGE_CURVE ( 'NONE', #71727, #69710, #69671, .T. ) ;
#8441=DIRECTION ( 'NONE',  ( -1.000000000000000000, 0.000000000000000000, -0.000000000000000000 ) ) ;
#8455=AXIS2_PLACEMENT_3D ( 'NONE', #13724, #70482, #29904 ) ;
#8496=CARTESIAN_POINT ( 'NONE',  ( -3.000000000000000000, -11.95096189432345390, 23.69967320028757385 ) ) ;
#8498=EDGE_CURVE ( 'NONE', #27250, #24265, #67640, .T. ) ;
#8503=CARTESIAN_POINT ( 'NONE',  ( 10.00000000000000000, 0.000000000000000000, 0.000000000000000000 ) ) ;
#8512=VERTEX_POINT ( 'NONE', #44340 ) ;
#8551=VERTEX_POINT ( 'NONE', #43613 ) ;
#8552=ORIENTED_EDGE ( 'NONE', *, *, #68105, .T. ) ;
#8558=LINE ( 'NONE', #71314, #2901 ) ;
#8559=CARTESIAN_POINT ( 'NONE',  ( 10.00000000000000000, 29.81001611431041098, -22.74946021919100403 ) ) ;
#8563=CARTESIAN_POINT ( 'NONE',  ( 0.000000000000000000, 35.47612816024556537, -22.48208911017461631 ) ) ;
#8571=AXIS2_PLACEMENT_3D ( 'NONE', #6157, #58010, #11401 ) ;
#8577=LINE ( 'NONE', #66461, #19836 ) ;
#8585=VERTEX_POINT ( 'NONE', #16136 ) ;
#8611=AXIS2_PLACEMENT_3D ( 'NONE', #56632, #21654, #32558 ) ;
#8614=EDGE_LOOP ( 'NONE', ( #61440, #8985, #27997, #33826 ) ) ;
#8618=ORIENTED_EDGE ( 'NONE', *, *, #46698, .F. ) ;
#8628=DIRECTION ( 'NONE',  ( 0.000000000000000000, -0.1564344650402170744, -0.9876883405951398798 ) ) ;
#8659=CARTESIAN_POINT ( 'NONE',  ( 10.00000000000000000, 27.13269053701132094, -25.88420570971372570 ) ) ;
#8662=AXIS2_PLACEMENT_3D ( 'NONE', #746, #57857, #35284 ) ;
#8679=CARTESIAN_POINT ( 'NONE',  ( 0.000000000000000000, -5.202137450156655518, 37.22597642581156663 ) ) ;
#8695=ORIENTED_EDGE ( 'NONE', *, *, #752, .T. ) ;
#8700=ORIENTED_EDGE ( 'NONE', *, *, #12569, .T. ) ;
#8701=EDGE_LOOP ( 'NONE', ( #60452, #64169, #44944, #65366 ) ) ;
#8712=CYLINDRICAL_SURFACE ( 'NONE', #8268, 37.49900000000000233 ) ;
#8734=CARTESIAN_POINT ( 'NONE',  ( 0.000000000000000000, 24.81905959214261514, 9.408202855044825341 ) ) ;
#8777=VERTEX_POINT ( 'NONE', #29614 ) ;
#8778=ORIENTED_EDGE ( 'NONE', *, *, #47523, .F. ) ;
#8780=ORIENTED_EDGE ( 'NONE', *, *, #37665, .T. ) ;
#8803=CIRCLE ( 'NONE', #37626, 15.99999999999999645 ) ;
#8816=FACE_OUTER_BOUND ( 'NONE', #14791, .T. ) ;
#8819=CIRCLE ( 'NONE', #433, 16.00000000000000000 ) ;
#8822=CARTESIAN_POINT ( 'NONE',  ( -3.000000000000000000, 5.835314593368477354, 22.81335362449854642 ) ) ;
#8824=DIRECTION ( 'NONE',  ( 0.000000000000000000, -0.2079116908177532363, -0.9781476007338070211 ) ) ;
#8836=FACE_BOUND ( 'NONE', #13590, .T. ) ;
#8847=VECTOR ( 'NONE', #34138, 1000.000000000000000 ) ;
#8850=ORIENTED_EDGE ( 'NONE', *, *, #2426, .T. ) ;
#8864=VECTOR ( 'NONE', #11538, 1000.000000000000000 ) ;
#8867=LINE ( 'NONE', #31780, #35659 ) ;
#8880=AXIS2_PLACEMENT_3D ( 'NONE', #14287, #37236, #36472 ) ;
#8882=DIRECTION ( 'NONE',  ( 0.000000000000000000, 0.000000000000000000, 1.000000000000000000 ) ) ;
#8907=ORIENTED_EDGE ( 'NONE', *, *, #12719, .F. ) ;
#8909=EDGE_CURVE ( 'NONE', #7754, #3179, #52940, .T. ) ;
#8911=VECTOR ( 'NONE', #30350, 1000.000000000000000 ) ;
#8925=DIRECTION ( 'NONE',  ( 1.000000000000000000, -0.000000000000000000, 0.000000000000000000 ) ) ;
#8930=AXIS2_PLACEMENT_3D ( 'NONE', #72995, #15879, #16612 ) ;
#8952=ORIENTED_EDGE ( 'NONE', *, *, #60130, .F. ) ;
#8979=EDGE_LOOP ( 'NONE', ( #68718, #68039, #14338, #53202 ) ) ;
#8984=CIRCLE ( 'NONE', #51016, 37.49900000000000233 ) ;
#8985=ORIENTED_EDGE ( 'NONE', *, *, #29586, .F. ) ;
#8987=EDGE_CURVE ( 'NONE', #25052, #60133, #72434, .T. ) ;
#9027=DIRECTION ( 'NONE',  ( 0.000000000000000000, -6.982962677686267499E-15, 1.000000000000000000 ) ) ;
#9029=DIRECTION ( 'NONE',  ( -1.000000000000000000, 0.000000000000000000, 0.000000000000000000 ) ) ;
#9033=ORIENTED_EDGE ( 'NONE', *, *, #44039, .T. ) ;
#9043=AXIS2_PLACEMENT_3D ( 'NONE', #17778, #7253, #34701 ) ;
#9058=ADVANCED_FACE ( 'NONE', ( #72069 ), #14930, .T. ) ;
#9126=ORIENTED_EDGE ( 'NONE', *, *, #61726, .F. ) ;
#9132=ORIENTED_EDGE ( 'NONE', *, *, #22914, .T. ) ;
#9135=ORIENTED_EDGE ( 'NONE', *, *, #24462, .F. ) ;
#9152=ORIENTED_EDGE ( 'NONE', *, *, #33861, .F. ) ;
#9155=ORIENTED_EDGE ( 'NONE', *, *, #38356, .F. ) ;
#9162=DIRECTION ( 'NONE',  ( 0.000000000000000000, 0.000000000000000000, 1.000000000000000000 ) ) ;
#9187=EDGE_CURVE ( 'NONE', #29480, #51502, #22434, .T. ) ;
#9188=CARTESIAN_POINT ( 'NONE',  ( 4.999999999999999112, 38.55633173627034438, -16.65560815589369881 ) ) ;
#9206=VECTOR ( 'NONE', #6355, 1000.000000000000000 ) ;
#9216=ORIENTED_EDGE ( 'NONE', *, *, #16193, .T. ) ;
#9219=CARTESIAN_POINT ( 'NONE',  ( -10.00000000000000000, 0.000000000000000000, 0.000000000000000000 ) ) ;
#9222=LINE ( 'NONE', #8496, #16568 ) ;
#9243=AXIS2_PLACEMENT_3D ( 'NONE', #6729, #23650, #41674 ) ;
#9245=VECTOR ( 'NONE', #36625, 1000.000000000000000 ) ;
#9251=ORIENTED_EDGE ( 'NONE', *, *, #40402, .F. ) ;
#9268=FACE_OUTER_BOUND ( 'NONE', #26072, .T. ) ;
#9302=ORIENTED_EDGE ( 'NONE', *, *, #30570, .T. ) ;
#9304=FACE_OUTER_BOUND ( 'NONE', #41574, .T. ) ;
#9317=DIRECTION ( 'NONE',  ( 0.000000000000000000, 0.8090169943749426773, 0.5877852522924797984 ) ) ;
#9328=CARTESIAN_POINT ( 'NONE',  ( 0.000000000000000000, 27.05870788708267582, -26.08949754952995903 ) ) ;
#9334=ADVANCED_FACE ( 'NONE', ( #53970 ), #12253, .T. ) ;
#9353=VECTOR ( 'NONE', #48232, 1000.000000000000000 ) ;
#9357=CARTESIAN_POINT ( 'NONE',  ( -3.000000000000000000, -11.95096189432312350, -23.69967320028773372 ) ) ;
#9360=CARTESIAN_POINT ( 'NONE',  ( 0.000000000000000000, 22.07842321921481243, 8.187992925817422218 ) ) ;
#9382=DIRECTION ( 'NONE',  ( -0.000000000000000000, 0.5000000000000039968, -0.8660254037844363761 ) ) ;
#9396=CIRCLE ( 'NONE', #51432, 16.00000000000000000 ) ;
#9400=EDGE_CURVE ( 'NONE', #7257, #33537, #40866, .T. ) ;
#9405=ORIENTED_EDGE ( 'NONE', *, *, #55841, .T. ) ;
#9410=AXIS2_PLACEMENT_3D ( 'NONE', #17449, #22736, #44926 ) ;
#9426=EDGE_LOOP ( 'NONE', ( #33269, #56608, #19894, #63000 ) ) ;
#9453=LINE ( 'NONE', #21462, #12893 ) ;
#9475=CARTESIAN_POINT ( 'NONE',  ( 10.00000000000000000, 16.23288003029543347, -33.80338159004267595 ) ) ;
#9485=EDGE_CURVE ( 'NONE', #10617, #66007, #14092, .T. ) ;
#9486=CARTESIAN_POINT ( 'NONE',  ( 0.000000000000000000, -31.52238457039619490, 27.75498641678731104 ) ) ;
#9489=CARTESIAN_POINT ( 'NONE',  ( 10.00000000000000000, -3.925862922255855647, -41.81611651403866858 ) ) ;
#9494=EDGE_LOOP ( 'NONE', ( #9302, #63183, #32940, #20057 ) ) ;
#9501=CIRCLE ( 'NONE', #59982, 16.00000000000000000 ) ;
#9510=LINE ( 'NONE', #45216, #68260 ) ;
#9515=ORIENTED_EDGE ( 'NONE', *, *, #63941, .T. ) ;
#9524=DIRECTION ( 'NONE',  ( 0.000000000000000000, 0.000000000000000000, 1.000000000000000000 ) ) ;
#9530=EDGE_LOOP ( 'NONE', ( #19219, #12934, #1813, #60820 ) ) ;
#9553=CARTESIAN_POINT ( 'NONE',  ( 5.000000000000000000, -36.13751322684404244, -21.40280677340410165 ) ) ;
#9558=ORIENTED_EDGE ( 'NONE', *, *, #26884, .F. ) ;
#9559=VERTEX_POINT ( 'NONE', #25756 ) ;
#9574=LINE ( 'NONE', #15585, #63411 ) ;
#9585=EDGE_CURVE ( 'NONE', #11102, #10014, #46025, .T. ) ;
#9588=CIRCLE ( 'NONE', #45614, 42.00000000000000000 ) ;
#9599=ORIENTED_EDGE ( 'NONE', *, *, #17647, .F. ) ;
#9627=CARTESIAN_POINT ( 'NONE',  ( 10.00000000000000000, -16.23288003029521320, 33.80338159004277543 ) ) ;
#9642=EDGE_LOOP ( 'NONE', ( #51211, #12269, #33003, #37061 ) ) ;
#9647=ORIENTED_EDGE ( 'NONE', *, *, #72649, .T. ) ;
#9652=CARTESIAN_POINT ( 'NONE',  ( 10.00000000000000000, 0.000000000000000000, 0.000000000000000000 ) ) ;
#9653=CARTESIAN_POINT ( 'NONE',  ( 5.000000000000000000, 41.91543099594818500, -2.663952781846291362 ) ) ;
#9655=ORIENTED_EDGE ( 'NONE', *, *, #55444, .T. ) ;
#9656=DIRECTION ( 'NONE',  ( 0.000000000000000000, 0.000000000000000000, 1.000000000000000000 ) ) ;
#9684=DIRECTION ( 'NONE',  ( -1.000000000000000000, 0.000000000000000000, 0.000000000000000000 ) ) ;
#9689=ORIENTED_EDGE ( 'NONE', *, *, #58645, .T. ) ;
#9693=EDGE_CURVE ( 'NONE', #20201, #71364, #41842, .T. ) ;
#9695=EDGE_CURVE ( 'NONE', #20645, #44110, #29807, .T. ) ;
#9717=ORIENTED_EDGE ( 'NONE', *, *, #7795, .F. ) ;
#9747=AXIS2_PLACEMENT_3D ( 'NONE', #13339, #37766, #65598 ) ;
#9756=DIRECTION ( 'NONE',  ( 0.000000000000000000, -0.9510565162951543083, 0.3090169943749448977 ) ) ;
#9757=DIRECTION ( 'NONE',  ( -1.000000000000000000, 0.000000000000000000, 0.000000000000000000 ) ) ;
#9784=VERTEX_POINT ( 'NONE', #941 ) ;
#9789=ADVANCED_FACE ( 'NONE', ( #41488 ), #30568, .T. ) ;
#9791=CARTESIAN_POINT ( 'NONE',  ( 0.000000000000000000, -18.13022148937263012, 15.02647892043544608 ) ) ;
#9792=ORIENTED_EDGE ( 'NONE', *, *, #2499, .F. ) ;
#9793=CIRCLE ( 'NONE', #8571, 42.00000000000000000 ) ;
#9794=DIRECTION ( 'NONE',  ( -1.000000000000000000, 0.000000000000000000, 0.000000000000000000 ) ) ;
#9795=ORIENTED_EDGE ( 'NONE', *, *, #73044, .F. ) ;
#9805=CARTESIAN_POINT ( 'NONE',  ( 4.999999999999999112, -2.663952781846440576, 41.91543099594817789 ) ) ;
#9806=ORIENTED_EDGE ( 'NONE', *, *, #31050, .F. ) ;
#9813=EDGE_LOOP ( 'NONE', ( #10811, #43695, #57535, #2642 ) ) ;
#9819=ORIENTED_EDGE ( 'NONE', *, *, #50908, .F. ) ;
#9825=LINE ( 'NONE', #66247, #52491 ) ;
#9836=ORIENTED_EDGE ( 'NONE', *, *, #70170, .F. ) ;
#9843=FACE_OUTER_BOUND ( 'NONE', #61442, .T. ) ;
#9846=ORIENTED_EDGE ( 'NONE', *, *, #68411, .T. ) ;
#9856=LINE ( 'NONE', #38057, #16052 ) ;
#9864=EDGE_CURVE ( 'NONE', #30584, #37124, #47504, .T. ) ;
#9870=LINE ( 'NONE', #20777, #72685 ) ;
#9875=CARTESIAN_POINT ( 'NONE',  ( 10.00000000000000000, -37.22597642581161637, 5.202137450156258502 ) ) ;
#9884=AXIS2_PLACEMENT_3D ( 'NONE', #47566, #74003, #16500 ) ;
#9885=ORIENTED_EDGE ( 'NONE', *, *, #88, .F. ) ;
#9917=EDGE_CURVE ( 'NONE', #55034, #70934, #20412, .T. ) ;
#9925=CARTESIAN_POINT ( 'NONE',  ( 10.00000000000000000, 35.95386929396241271, 10.96151621346552751 ) ) ;
#9954=VECTOR ( 'NONE', #55615, 1000.000000000000000 ) ;
#9960=VERTEX_POINT ( 'NONE', #26037 ) ;
#9988=LINE ( 'NONE', #55112, #53587 ) ;
#10010=CYLINDRICAL_SURFACE ( 'NONE', #39755, 16.00000000000000000 ) ;
#10011=VECTOR ( 'NONE', #55249, 1000.000000000000000 ) ;
#10012=AXIS2_PLACEMENT_3D ( 'NONE', #72436, #61180, #72794 ) ;
#10013=DIRECTION ( 'NONE',  ( 0.000000000000000000, 0.9876883405951372152, 0.1564344650402347547 ) ) ;
#10014=VERTEX_POINT ( 'NONE', #47375 ) ;
#10015=EDGE_CURVE ( 'NONE', #55034, #47629, #12410, .T. ) ;
#10039=CARTESIAN_POINT ( 'NONE',  ( 0.000000000000000000, -40.68715046381937128, 10.41901085202062660 ) ) ;
#10044=CIRCLE ( 'NONE', #65333, 16.00000000000000000 ) ;
#10069=VERTEX_POINT ( 'NONE', #1551 ) ;
#10070=ORIENTED_EDGE ( 'NONE', *, *, #26619, .F. ) ;
#10080=DIRECTION ( 'NONE',  ( 0.000000000000000000, 0.3090169943749580539, -0.9510565162951499785 ) ) ;
#10089=ADVANCED_FACE ( 'NONE', ( #48109 ), #65416, .T. ) ;
#10099=ORIENTED_EDGE ( 'NONE', *, *, #51648, .F. ) ;
#10130=DIRECTION ( 'NONE',  ( -1.000000000000000000, 0.000000000000000000, 0.000000000000000000 ) ) ;
#10131=CARTESIAN_POINT ( 'NONE',  ( 0.000000000000000000, -26.79245525562738095, 32.34446384429961796 ) ) ;
#10139=DIRECTION ( 'NONE',  ( 0.000000000000000000, 0.000000000000000000, 1.000000000000000000 ) ) ;
#10150=AXIS2_PLACEMENT_3D ( 'NONE', #482, #18102, #34643 ) ;
#10166=EDGE_CURVE ( 'NONE', #68072, #11081, #58650, .T. ) ;
#10167=ORIENTED_EDGE ( 'NONE', *, *, #31062, .F. ) ;
#10177=CARTESIAN_POINT ( 'NONE',  ( 0.000000000000000000, 41.81611651403861885, 3.925862922256313503 ) ) ;
#10193=CARTESIAN_POINT ( 'NONE',  ( 0.000000000000000000, -37.58145647212455032, 16.68533520207890319 ) ) ;
#10195=ADVANCED_FACE ( 'NONE', ( #31542 ), #32655, .T. ) ;
#10206=EDGE_CURVE ( 'NONE', #51805, #24766, #27013, .T. ) ;
#10221=VECTOR ( 'NONE', #21766, 1000.000000000000000 ) ;
#10226=LINE ( 'NONE', #56096, #5896 ) ;
#10228=VERTEX_POINT ( 'NONE', #43598 ) ;
#10241=CARTESIAN_POINT ( 'NONE',  ( 0.000000000000000000, -25.60904388321916514, -6.976881207771517879 ) ) ;
#10244=ORIENTED_EDGE ( 'NONE', *, *, #26040, .T. ) ;
#10259=DIRECTION ( 'NONE',  ( 0.000000000000000000, 0.4539904997395414754, 0.8910065241883706744 ) ) ;
#10264=EDGE_CURVE ( 'NONE', #18236, #50093, #46735, .T. ) ;
#10277=DIRECTION ( 'NONE',  ( 0.000000000000000000, 0.2079116908177664758, -0.9781476007338042455 ) ) ;
#10294=DIRECTION ( 'NONE',  ( -0.000000000000000000, 0.1045284632676436315, 0.9945218953682742891 ) ) ;
#10300=ORIENTED_EDGE ( 'NONE', *, *, #10933, .F. ) ;
#10303=EDGE_CURVE ( 'NONE', #6668, #67482, #1149, .T. ) ;
#10306=CARTESIAN_POINT ( 'NONE',  ( 4.999999999999999112, -40.68715046381921496, -10.41901085202121280 ) ) ;
#10309=ORIENTED_EDGE ( 'NONE', *, *, #47890, .F. ) ;
#10327=VECTOR ( 'NONE', #32674, 1000.000000000000000 ) ;
#10338=CIRCLE ( 'NONE', #33141, 16.00000000000000000 ) ;
#10365=VERTEX_POINT ( 'NONE', #59765 ) ;
#10380=CARTESIAN_POINT ( 'NONE',  ( 10.00000000000000000, 35.38097989696512968, 12.42422080174651100 ) ) ;
#10388=VECTOR ( 'NONE', #3274, 1000.000000000000000 ) ;
#10389=DIRECTION ( 'NONE',  ( 0.000000000000000000, -0.8090169943749531134, 0.5877852522924653655 ) ) ;
#10392=CARTESIAN_POINT ( 'NONE',  ( -3.000000000000000000, 20.85821328998756385, -10.92862929874494959 ) ) ;
#10407=CARTESIAN_POINT ( 'NONE',  ( 0.000000000000000000, -17.80606268964516659, -33.00180498840066434 ) ) ;
#10416=CARTESIAN_POINT ( 'NONE',  ( -3.000000000000000000, 22.07842321921492612, -8.187992925817130896 ) ) ;
#10425=VECTOR ( 'NONE', #26876, 1000.000000000000000 ) ;
#10446=CARTESIAN_POINT ( 'NONE',  ( 0.000000000000000000, 16.61724383029390140, -20.69703378468903665 ) ) ;
#10457=CARTESIAN_POINT ( 'NONE',  ( 10.00000000000000000, 0.000000000000000000, 0.000000000000000000 ) ) ;
#10478=CARTESIAN_POINT ( 'NONE',  ( 10.00000000000000000, 0.8828120875905820508, -37.48860685352290290 ) ) ;
#10488=DIRECTION ( 'NONE',  ( -1.000000000000000000, 0.000000000000000000, -0.000000000000000000 ) ) ;
#10502=EDGE_CURVE ( 'NONE', #51690, #67688, #71926, .T. ) ;
#10508=CARTESIAN_POINT ( 'NONE',  ( 10.00000000000000000, 0.000000000000000000, 0.000000000000000000 ) ) ;
#10540=ORIENTED_EDGE ( 'NONE', *, *, #40653, .T. ) ;
#10552=AXIS2_PLACEMENT_3D ( 'NONE', #64903, #13383, #70145 ) ;
#10553=VECTOR ( 'NONE', #37696, 1000.000000000000000 ) ;
#10566=DIRECTION ( 'NONE',  ( -1.000000000000000000, 0.000000000000000000, 0.000000000000000000 ) ) ;
#10568=ORIENTED_EDGE ( 'NONE', *, *, #54671, .F. ) ;
#10576=ORIENTED_EDGE ( 'NONE', *, *, #13754, .F. ) ;
#10594=EDGE_LOOP ( 'NONE', ( #10733, #29419, #4053, #40256 ) ) ;
#10606=DIRECTION ( 'NONE',  ( -1.000000000000000000, -0.000000000000000000, 0.000000000000000000 ) ) ;
#10607=CARTESIAN_POINT ( 'NONE',  ( 0.000000000000000000, -30.00120703465222149, 22.64427369931158296 ) ) ;
#10609=AXIS2_PLACEMENT_3D ( 'NONE', #33431, #27422, #10139 ) ;
#10615=ORIENTED_EDGE ( 'NONE', *, *, #10206, .F. ) ;
#10617=VERTEX_POINT ( 'NONE', #14257 ) ;
#10624=ORIENTED_EDGE ( 'NONE', *, *, #47521, .T. ) ;
#10635=VERTEX_POINT ( 'NONE', #9357 ) ;
#10639=ORIENTED_EDGE ( 'NONE', *, *, #73894, .T. ) ;
#10642=DIRECTION ( 'NONE',  ( 0.000000000000000000, 0.1564344650402312298, -0.9876883405951375483 ) ) ;
#10658=CARTESIAN_POINT ( 'NONE',  ( 10.00000000000000000, 33.17418723428333749, -17.67226234102790272 ) ) ;
#10664=CIRCLE ( 'NONE', #28694, 42.00000000000000000 ) ;
#10665=ORIENTED_EDGE ( 'NONE', *, *, #15292, .T. ) ;
#10704=ORIENTED_EDGE ( 'NONE', *, *, #30068, .T. ) ;
#10705=CARTESIAN_POINT ( 'NONE',  ( 10.00000000000000000, 0.000000000000000000, 0.000000000000000000 ) ) ;
#10707=ORIENTED_EDGE ( 'NONE', *, *, #15452, .F. ) ;
#10714=ADVANCED_FACE ( 'NONE', ( #51816 ), #56354, .T. ) ;
#10715=AXIS2_PLACEMENT_3D ( 'NONE', #72543, #66197, #44371 ) ;
#10718=ORIENTED_EDGE ( 'NONE', *, *, #50307, .F. ) ;
#10733=ORIENTED_EDGE ( 'NONE', *, *, #27237, .T. ) ;
#10752=AXIS2_PLACEMENT_3D ( 'NONE', #54068, #2963, #19831 ) ;
#10756=CARTESIAN_POINT ( 'NONE',  ( 10.00000000000000000, 10.41901085202135668, -40.68715046381917944 ) ) ;
#10757=ORIENTED_EDGE ( 'NONE', *, *, #34830, .F. ) ;
#10764=DIRECTION ( 'NONE',  ( 0.000000000000000000, -0.5877852522924802425, 0.8090169943749422332 ) ) ;
#10775=FACE_BOUND ( 'NONE', #55298, .T. ) ;
#10796=EDGE_CURVE ( 'NONE', #64719, #56201, #45075, .T. ) ;
#10804=VECTOR ( 'NONE', #69672, 1000.000000000000000 ) ;
#10806=ADVANCED_FACE ( 'NONE', ( #52540 ), #59302, .T. ) ;
#10811=ORIENTED_EDGE ( 'NONE', *, *, #70760, .T. ) ;
#10813=CARTESIAN_POINT ( 'NONE',  ( 10.00000000000000000, 36.13751322684449718, -21.40280677340333071 ) ) ;
#10826=VECTOR ( 'NONE', #47909, 1000.000000000000227 ) ;
#10838=VERTEX_POINT ( 'NONE', #1466 ) ;
#10844=CARTESIAN_POINT ( 'NONE',  ( -10.00000000000000000, 0.000000000000000000, 0.000000000000000000 ) ) ;
#10845=CARTESIAN_POINT ( 'NONE',  ( -3.000000000000000000, 24.81905959214275370, -9.408202855044498492 ) ) ;
#10846=LINE ( 'NONE', #15739, #43292 ) ;
#10855=PLANE ( 'NONE',  #47289 ) ;
#10894=CARTESIAN_POINT ( 'NONE',  ( -3.000000000000000000, -3.948201729842038432, -23.21447184625298021 ) ) ;
#10896=DIRECTION ( 'NONE',  ( -1.000000000000000000, 0.000000000000000000, -0.000000000000000000 ) ) ;
#10905=CYLINDRICAL_SURFACE ( 'NONE', #29323, 16.00000000000000000 ) ;
#10909=ORIENTED_EDGE ( 'NONE', *, *, #14453, .T. ) ;
#10910=DIRECTION ( 'NONE',  ( -1.000000000000000000, -0.000000000000000000, -0.000000000000000000 ) ) ;
#10920=DIRECTION ( 'NONE',  ( -1.000000000000000000, 0.000000000000000000, 0.000000000000000000 ) ) ;
#10921=ORIENTED_EDGE ( 'NONE', *, *, #48707, .T. ) ;
#10933=EDGE_CURVE ( 'NONE', #62989, #70987, #9588, .T. ) ;
#10938=ADVANCED_FACE ( 'NONE', ( #23614 ), #13792, .T. ) ;
#10948=DIRECTION ( 'NONE',  ( 1.000000000000000000, -0.000000000000000000, 0.000000000000000000 ) ) ;
#10954=EDGE_CURVE ( 'NONE', #779, #27461, #27614, .T. ) ;
#10955=CARTESIAN_POINT ( 'NONE',  ( 0.000000000000000000, -37.16516213103273714, -4.992566952385376844 ) ) ;
#10965=VECTOR ( 'NONE', #53193, 1000.000000000000114 ) ;
#10977=ORIENTED_EDGE ( 'NONE', *, *, #18160, .F. ) ;
#10978=FACE_OUTER_BOUND ( 'NONE', #11581, .T. ) ;
#10982=DIRECTION ( 'NONE',  ( 0.000000000000000000, -0.3090169943749549453, 0.9510565162951511997 ) ) ;
#10984=VECTOR ( 'NONE', #42386, 1000.000000000000000 ) ;
#10992=LINE ( 'NONE', #857, #38270 ) ;
#10993=EDGE_LOOP ( 'NONE', ( #32548, #7806, #13311, #71495 ) ) ;
#10994=DIRECTION ( 'NONE',  ( 1.000000000000000000, 0.000000000000000000, 0.000000000000000000 ) ) ;
#10997=ORIENTED_EDGE ( 'NONE', *, *, #37550, .T. ) ;
#11012=AXIS2_PLACEMENT_3D ( 'NONE', #89, #62848, #68838 ) ;
#11022=DIRECTION ( 'NONE',  ( 0.000000000000000000, 0.000000000000000000, 1.000000000000000000 ) ) ;
#11035=VERTEX_POINT ( 'NONE', #49127 ) ;
#11037=DIRECTION ( 'NONE',  ( 1.000000000000000000, 0.000000000000000000, 0.000000000000000000 ) ) ;
#11062=CARTESIAN_POINT ( 'NONE',  ( 0.000000000000000000, 23.50000000000000000, -1.500000000000001332 ) ) ;
#11072=LINE ( 'NONE', #39648, #50635 ) ;
#11077=CARTESIAN_POINT ( 'NONE',  ( 10.00000000000000000, -0.6853352020787742971, -37.58145647212455032 ) ) ;
#11081=VERTEX_POINT ( 'NONE', #48386 ) ;
#11102=VERTEX_POINT ( 'NONE', #60791 ) ;
#11115=DIRECTION ( 'NONE',  ( -1.000000000000000000, 0.000000000000000000, 0.000000000000000000 ) ) ;
#11116=ORIENTED_EDGE ( 'NONE', *, *, #73085, .F. ) ;
#11122=DIRECTION ( 'NONE',  ( 0.000000000000000000, 0.3090169943749412340, 0.9510565162951556406 ) ) ;
#11151=CARTESIAN_POINT ( 'NONE',  ( 0.000000000000000000, 0.000000000000000000, 0.000000000000000000 ) ) ;
#11166=DIRECTION ( 'NONE',  ( 0.000000000000000000, -0.8090169943749422332, -0.5877852522924803536 ) ) ;
#11174=ORIENTED_EDGE ( 'NONE', *, *, #32592, .F. ) ;
#11177=FACE_OUTER_BOUND ( 'NONE', #63192, .T. ) ;
#11180=CIRCLE ( 'NONE', #23216, 42.00000000000000000 ) ;
#11181=CARTESIAN_POINT ( 'NONE',  ( -3.000000000000000000, 16.61724383029361718, 20.69703378468926402 ) ) ;
#11186=EDGE_CURVE ( 'NONE', #12067, #48989, #39588, .T. ) ;
#11192=CIRCLE ( 'NONE', #2802, 37.49900000000000944 ) ;
#11205=EDGE_CURVE ( 'NONE', #66879, #42446, #55250, .T. ) ;
#11220=AXIS2_PLACEMENT_3D ( 'NONE', #25842, #53311, #29997 ) ;
#11221=DIRECTION ( 'NONE',  ( 0.000000000000000000, 0.8660254037844368202, 0.5000000000000029976 ) ) ;
#11226=DIRECTION ( 'NONE',  ( 1.000000000000000000, -0.000000000000000000, -0.000000000000000000 ) ) ;
#11229=PLANE ( 'NONE',  #9884 ) ;
#11234=PLANE ( 'NONE',  #29202 ) ;
#11237=DIRECTION ( 'NONE',  ( -1.000000000000000000, 0.000000000000000000, 0.000000000000000000 ) ) ;
#11255=VERTEX_POINT ( 'NONE', #38970 ) ;
#11258=CYLINDRICAL_SURFACE ( 'NONE', #19030, 37.49900000000000233 ) ;
#11266=CIRCLE ( 'NONE', #29235, 15.99999999999999645 ) ;
#11271=CARTESIAN_POINT ( 'NONE',  ( 0.000000000000000000, 0.000000000000000000, 0.000000000000000000 ) ) ;
#11278=DIRECTION ( 'NONE',  ( -1.000000000000000000, -0.000000000000000000, 0.000000000000000000 ) ) ;
#11281=VERTEX_POINT ( 'NONE', #59878 ) ;
#11295=ORIENTED_EDGE ( 'NONE', *, *, #50307, .T. ) ;
#11297=DIRECTION ( 'NONE',  ( -1.000000000000000000, -0.000000000000000000, 0.000000000000000000 ) ) ;
#11328=CARTESIAN_POINT ( 'NONE',  ( -3.000000000000000000, 22.07842321921481243, 8.187992925817422218 ) ) ;
#11330=PLANE ( 'NONE',  #40181 ) ;
#11335=CARTESIAN_POINT ( 'NONE',  ( 0.000000000000000000, 0.000000000000000000, 0.000000000000000000 ) ) ;
#11341=DIRECTION ( 'NONE',  ( -1.000000000000000000, -0.000000000000000000, 0.000000000000000000 ) ) ;
#11350=VERTEX_POINT ( 'NONE', #635 ) ;
#11351=PRODUCT_DEFINITION ( 'UNKNOWN', '', #6459, #43167 ) ;
#11359=VERTEX_POINT ( 'NONE', #31283 ) ;
#11361=DIRECTION ( 'NONE',  ( 0.000000000000000000, 0.000000000000000000, 1.000000000000000000 ) ) ;
#11366=EDGE_CURVE ( 'NONE', #63788, #70934, #6607, .T. ) ;
#11396=AXIS2_PLACEMENT_3D ( 'NONE', #27560, #21167, #10642 ) ;
#11401=DIRECTION ( 'NONE',  ( 0.000000000000000000, 0.000000000000000000, 1.000000000000000000 ) ) ;
#11445=ADVANCED_FACE ( 'NONE', ( #29515 ), #2022, .T. ) ;
#11449=ORIENTED_EDGE ( 'NONE', *, *, #15375, .T. ) ;
#11469=LINE ( 'NONE', #73504, #19441 ) ;
#11473=ORIENTED_EDGE ( 'NONE', *, *, #70773, .T. ) ;
#11476=ORIENTED_EDGE ( 'NONE', *, *, #39083, .T. ) ;
#11488=LINE ( 'NONE', #44610, #55849 ) ;
#11492=CARTESIAN_POINT ( 'NONE',  ( 0.000000000000000000, 0.000000000000000000, 0.000000000000000000 ) ) ;
#11522=AXIS2_PLACEMENT_3D ( 'NONE', #51858, #68428, #16917 ) ;
#11523=EDGE_CURVE ( 'NONE', #7257, #57225, #68473, .T. ) ;
#11526=VERTEX_POINT ( 'NONE', #26748 ) ;
#11538=DIRECTION ( 'NONE',  ( 0.000000000000000000, 0.000000000000000000, 1.000000000000000000 ) ) ;
#11542=DIRECTION ( 'NONE',  ( 0.000000000000000000, 0.000000000000000000, 1.000000000000000000 ) ) ;
#11544=ORIENTED_EDGE ( 'NONE', *, *, #2239, .T. ) ;
#11551=VECTOR ( 'NONE', #49836, 1000.000000000000000 ) ;
#11579=VERTEX_POINT ( 'NONE', #60616 ) ;
#11581=EDGE_LOOP ( 'NONE', ( #36283, #61980, #49377, #3449 ) ) ;
#11582=DIRECTION ( 'NONE',  ( 0.000000000000000000, 0.9876883405951381034, -0.1564344650402276216 ) ) ;
#11595=DIRECTION ( 'NONE',  ( 0.000000000000000000, -0.4067366430758009854, 0.9135454576426004225 ) ) ;
#11618=AXIS2_PLACEMENT_3D ( 'NONE', #74136, #10994, #57966 ) ;
#11620=ORIENTED_EDGE ( 'NONE', *, *, #60544, .F. ) ;
#11622=CARTESIAN_POINT ( 'NONE',  ( 10.00000000000000000, -37.01155633439053361, -6.555932627142825986 ) ) ;
#11624=ADVANCED_FACE ( 'NONE', ( #28231 ), #11674, .F. ) ;
#11631=EDGE_CURVE ( 'NONE', #7862, #19038, #3702, .T. ) ;
#11633=DIRECTION ( 'NONE',  ( 1.000000000000000000, 0.000000000000000000, 0.000000000000000000 ) ) ;
#11641=EDGE_LOOP ( 'NONE', ( #29931, #23328, #26687, #73212 ) ) ;
#11647=VERTEX_POINT ( 'NONE', #45174 ) ;
#11674=PLANE ( 'NONE',  #61273 ) ;
#11675=DIRECTION ( 'NONE',  ( 0.000000000000000000, -0.9945218953682730678, -0.1045284632676570929 ) ) ;
#11679=DIRECTION ( 'NONE',  ( -1.000000000000000000, 0.000000000000000000, -0.000000000000000000 ) ) ;
#11683=EDGE_CURVE ( 'NONE', #47235, #12105, #823, .T. ) ;
#11684=PLANE ( 'NONE',  #67701 ) ;
#11686=DIRECTION ( 'NONE',  ( -1.000000000000000000, 0.000000000000000000, 0.000000000000000000 ) ) ;
#11705=VERTEX_POINT ( 'NONE', #10955 ) ;
#11709=PLANE ( 'NONE',  #59214 ) ;
#11715=EDGE_LOOP ( 'NONE', ( #39295, #19957, #20345, #70538 ) ) ;
#11717=ADVANCED_FACE ( 'NONE', ( #22608 ), #16967, .T. ) ;
#11751=DIRECTION ( 'NONE',  ( -1.000000000000000000, -0.000000000000000000, 0.000000000000000000 ) ) ;
#11766=FACE_OUTER_BOUND ( 'NONE', #41171, .T. ) ;
#11775=AXIS2_PLACEMENT_3D ( 'NONE', #19225, #65480, #13217 ) ;
#11778=LINE ( 'NONE', #200, #33278 ) ;
#11783=ADVANCED_FACE ( 'NONE', ( #14270 ), #7894, .F. ) ;
#11800=PLANE ( 'NONE',  #71154 ) ;
#11807=AXIS2_PLACEMENT_3D ( 'NONE', #56465, #55334, #27872 ) ;
#11812=CARTESIAN_POINT ( 'NONE',  ( 10.00000000000000000, 12.42422080174639021, 35.38097989696516521 ) ) ;
#11813=ORIENTED_EDGE ( 'NONE', *, *, #3119, .T. ) ;
#11826=CARTESIAN_POINT ( 'NONE',  ( -3.000000000000000000, 8.688484142254221609, -21.88630264137359660 ) ) ;
#11835=VERTEX_POINT ( 'NONE', #44719 ) ;
#11858=DIRECTION ( 'NONE',  ( -1.000000000000000000, 0.000000000000000000, -0.000000000000000000 ) ) ;
#11861=AXIS2_PLACEMENT_3D ( 'NONE', #45256, #16673, #39611 ) ;
#11862=VERTEX_POINT ( 'NONE', #38697 ) ;
#11876=PLANE ( 'NONE',  #67656 ) ;
#11882=CARTESIAN_POINT ( 'NONE',  ( 10.00000000000000000, 0.000000000000000000, 0.000000000000000000 ) ) ;
#11886=FACE_OUTER_BOUND ( 'NONE', #35700, .T. ) ;
#11888=CIRCLE ( 'NONE', #44315, 16.00000000000000355 ) ;
#11895=ORIENTED_EDGE ( 'NONE', *, *, #64245, .T. ) ;
#11902=CARTESIAN_POINT ( 'NONE',  ( 0.000000000000000000, 25.88420570971438650, -27.13269053701069566 ) ) ;
#11904=ORIENTED_EDGE ( 'NONE', *, *, #55762, .T. ) ;
#11916=ORIENTED_EDGE ( 'NONE', *, *, #22670, .T. ) ;
#11921=CIRCLE ( 'NONE', #20183, 16.00000000000000000 ) ;
#11923=CARTESIAN_POINT ( 'NONE',  ( 10.00000000000000000, -33.00180498840060039, 17.80606268964528027 ) ) ;
#11925=LINE ( 'NONE', #52513, #49738 ) ;
#11940=CARTESIAN_POINT ( 'NONE',  ( 0.000000000000000000, 26.79245525562714292, 32.34446384429980981 ) ) ;
#11943=CARTESIAN_POINT ( 'NONE',  ( 0.000000000000000000, -13.04903810567647682, -19.60159698893442481 ) ) ;
#11967=PLANE ( 'NONE',  #56002 ) ;
#11975=LINE ( 'NONE', #62395, #32310 ) ;
#11987=ADVANCED_FACE ( 'NONE', ( #40544 ), #51449, .T. ) ;
#11988=ADVANCED_FACE ( 'NONE', ( #34166 ), #57110, .T. ) ;
#11992=CARTESIAN_POINT ( 'NONE',  ( 10.00000000000000000, 10.96151621346487914, 35.95386929396260456 ) ) ;
#11996=LINE ( 'NONE', #34936, #35593 ) ;
#11998=VECTOR ( 'NONE', #55417, 1000.000000000000000 ) ;
#12029=EDGE_LOOP ( 'NONE', ( #8225, #28832, #23306, #68172 ) ) ;
#12033=EDGE_CURVE ( 'NONE', #36560, #47180, #51084, .T. ) ;
#12038=EDGE_CURVE ( 'NONE', #72759, #55034, #57848, .T. ) ;
#12041=ORIENTED_EDGE ( 'NONE', *, *, #37367, .F. ) ;
#12048=CARTESIAN_POINT ( 'NONE',  ( 10.00000000000000000, 25.88420570971400991, 27.13269053701105449 ) ) ;
#12052=VECTOR ( 'NONE', #20381, 999.9999999999998863 ) ;
#12060=CIRCLE ( 'NONE', #4845, 16.00000000000000000 ) ;
#12067=VERTEX_POINT ( 'NONE', #12336 ) ;
#12073=CARTESIAN_POINT ( 'NONE',  ( -10.00000000000000000, 0.000000000000000000, 0.000000000000000000 ) ) ;
#12074=CARTESIAN_POINT ( 'NONE',  ( -3.000000000000000000, 14.60985201121729737, -18.46759930825687945 ) ) ;
#12075=CARTESIAN_POINT ( 'NONE',  ( 10.00000000000000000, 22.74946021919133088, 29.81001611431016229 ) ) ;
#12083=DIRECTION ( 'NONE',  ( -1.000000000000000000, -0.000000000000000000, 0.000000000000000000 ) ) ;
#12086=AXIS2_PLACEMENT_3D ( 'NONE', #52373, #23085, #40361 ) ;
#12105=VERTEX_POINT ( 'NONE', #58568 ) ;
#12107=ORIENTED_EDGE ( 'NONE', *, *, #16066, .T. ) ;
#12137=CIRCLE ( 'NONE', #13314, 16.00000000000000000 ) ;
#12160=DIRECTION ( 'NONE',  ( -1.000000000000000000, 0.000000000000000000, -0.000000000000000000 ) ) ;
#12164=VECTOR ( 'NONE', #49432, 1000.000000000000000 ) ;
#12179=DIRECTION ( 'NONE',  ( 0.000000000000000000, 0.5877852522924684742, 0.8090169943749506709 ) ) ;
#12186=VECTOR ( 'NONE', #53857, 1000.000000000000000 ) ;
#12203=ORIENTED_EDGE ( 'NONE', *, *, #38643, .T. ) ;
#12243=ORIENTED_EDGE ( 'NONE', *, *, #26040, .F. ) ;
#12250=DIRECTION ( 'NONE',  ( -1.000000000000000000, -0.000000000000000000, -0.000000000000000000 ) ) ;
#12251=LINE ( 'NONE', #25008, #39271 ) ;
#12253=CYLINDRICAL_SURFACE ( 'NONE', #38500, 42.00000000000000000 ) ;
#12269=ORIENTED_EDGE ( 'NONE', *, *, #53324, .F. ) ;
#12285=ADVANCED_FACE ( 'NONE', ( #28806 ), #52102, .T. ) ;
#12289=EDGE_LOOP ( 'NONE', ( #26646, #64260, #16529, #73487 ) ) ;
#12290=ORIENTED_EDGE ( 'NONE', *, *, #16027, .T. ) ;
#12299=ORIENTED_EDGE ( 'NONE', *, *, #60105, .T. ) ;
#12303=DIRECTION ( 'NONE',  ( 0.000000000000000000, -0.9781476007338040235, -0.2079116908177671419 ) ) ;
#12326=DIRECTION ( 'NONE',  ( -1.000000000000000000, -0.000000000000000000, -0.000000000000000000 ) ) ;
#12332=FACE_OUTER_BOUND ( 'NONE', #15832, .T. ) ;
#12335=CARTESIAN_POINT ( 'NONE',  ( 0.000000000000000000, 6.555932627142952995, -37.01155633439051940 ) ) ;
#12336=CARTESIAN_POINT ( 'NONE',  ( 0.000000000000000000, -30.84782396557201878, -21.32104025579148399 ) ) ;
#12341=DIRECTION ( 'NONE',  ( -1.000000000000000000, 0.000000000000000000, 0.000000000000000000 ) ) ;
#12360=FACE_OUTER_BOUND ( 'NONE', #30054, .T. ) ;
#12406=VERTEX_POINT ( 'NONE', #68673 ) ;
#12410=LINE ( 'NONE', #6775, #16680 ) ;
#12412=CARTESIAN_POINT ( 'NONE',  ( 0.000000000000000000, 23.59884966291521380, 12.14883922797262805 ) ) ;
#12420=DIRECTION ( 'NONE',  ( 1.000000000000000000, 0.000000000000000000, -0.000000000000000000 ) ) ;
#12435=CARTESIAN_POINT ( 'NONE',  ( -3.000000000000000000, 20.85821328998741109, 10.92862929874522315 ) ) ;
#12437=LINE ( 'NONE', #40279, #4649 ) ;
#12438=DIRECTION ( 'NONE',  ( -1.000000000000000000, 0.000000000000000000, 0.000000000000000000 ) ) ;
#12441=DIRECTION ( 'NONE',  ( 1.000000000000000000, -0.000000000000000000, -0.000000000000000000 ) ) ;
#12446=AXIS2_PLACEMENT_3D ( 'NONE', #32033, #71889, #15119 ) ;
#12448=CARTESIAN_POINT ( 'NONE',  ( 10.00000000000000000, 0.000000000000000000, 0.000000000000000000 ) ) ;
#12449=EDGE_CURVE ( 'NONE', #46611, #70418, #45386, .T. ) ;
#12452=ORIENTED_EDGE ( 'NONE', *, *, #63526, .F. ) ;
#12453=DIRECTION ( 'NONE',  ( -1.000000000000000000, -0.000000000000000000, -0.000000000000000000 ) ) ;
#12456=ORIENTED_EDGE ( 'NONE', *, *, #61890, .F. ) ;
#12464=ORIENTED_EDGE ( 'NONE', *, *, #38356, .T. ) ;
#12471=ORIENTED_EDGE ( 'NONE', *, *, #21384, .F. ) ;
#12484=VERTEX_POINT ( 'NONE', #65251 ) ;
#12503=CARTESIAN_POINT ( 'NONE',  ( -3.000000000000000000, 23.59884966291521380, 12.14883922797262805 ) ) ;
#12505=CARTESIAN_POINT ( 'NONE',  ( 10.00000000000000000, 37.22597642581158084, -5.202137450156524068 ) ) ;
#12514=ORIENTED_EDGE ( 'NONE', *, *, #68793, .T. ) ;
#12518=DIRECTION ( 'NONE',  ( 0.000000000000000000, 0.000000000000000000, 1.000000000000000000 ) ) ;
#12519=LINE ( 'NONE', #46375, #18103 ) ;
#12522=CIRCLE ( 'NONE', #18532, 42.00000000000000000 ) ;
#12537=EDGE_CURVE ( 'NONE', #24073, #11102, #63775, .T. ) ;
#12540=ORIENTED_EDGE ( 'NONE', *, *, #7385, .T. ) ;
#12545=EDGE_CURVE ( 'NONE', #22221, #32803, #53780, .T. ) ;
#12564=VERTEX_POINT ( 'NONE', #42677 ) ;
#12568=LINE ( 'NONE', #16835, #15549 ) ;
#12569=EDGE_CURVE ( 'NONE', #26913, #35679, #33378, .T. ) ;
#12589=EDGE_CURVE ( 'NONE', #2929, #54905, #20101, .T. ) ;
#12596=FACE_OUTER_BOUND ( 'NONE', #1778, .T. ) ;
#12601=DIRECTION ( 'NONE',  ( -1.000000000000000000, 0.000000000000000000, 0.000000000000000000 ) ) ;
#12609=ORIENTED_EDGE ( 'NONE', *, *, #47855, .T. ) ;
#12613=DIRECTION ( 'NONE',  ( 0.000000000000000000, 0.000000000000000000, 1.000000000000000000 ) ) ;
#12619=DIRECTION ( 'NONE',  ( 0.000000000000000000, 0.000000000000000000, 1.000000000000000000 ) ) ;
#12626=ORIENTED_EDGE ( 'NONE', *, *, #476, .T. ) ;
#12659=EDGE_CURVE ( 'NONE', #37934, #39121, #9574, .T. ) ;
#12670=CARTESIAN_POINT ( 'NONE',  ( -3.000000000000000000, -22.67460108101774807, -6.353146135318215038 ) ) ;
#12674=VECTOR ( 'NONE', #16302, 1000.000000000000000 ) ;
#12685=ORIENTED_EDGE ( 'NONE', *, *, #42608, .F. ) ;
#12688=DIRECTION ( 'NONE',  ( 0.000000000000000000, 0.000000000000000000, 1.000000000000000000 ) ) ;
#12689=VECTOR ( 'NONE', #30175, 999.9999999999998863 ) ;
#12694=ORIENTED_EDGE ( 'NONE', *, *, #46121, .F. ) ;
#12719=EDGE_CURVE ( 'NONE', #58159, #11705, #28610, .T. ) ;
#12722=CIRCLE ( 'NONE', #65553, 37.49900000000000233 ) ;
#12738=VERTEX_POINT ( 'NONE', #46022 ) ;
#12761=ORIENTED_EDGE ( 'NONE', *, *, #60130, .T. ) ;
#12762=SURFACE_STYLE_USAGE ( .BOTH. , #64648 ) ;
#12765=LINE ( 'NONE', #1542, #25831 ) ;
#12768=ORIENTED_EDGE ( 'NONE', *, *, #69914, .T. ) ;
#12770=LINE ( 'NONE', #69192, #24143 ) ;
#12775=ORIENTED_EDGE ( 'NONE', *, *, #33979, .T. ) ;
#12777=PLANE ( 'NONE',  #57604 ) ;
#12786=AXIS2_PLACEMENT_3D ( 'NONE', #22301, #38484, #16285 ) ;
#12787=DIRECTION ( 'NONE',  ( -1.000000000000000000, 0.000000000000000000, 0.000000000000000000 ) ) ;
#12790=CIRCLE ( 'NONE', #66836, 42.00000000000000000 ) ;
#12797=VECTOR ( 'NONE', #27029, 1000.000000000000227 ) ;
#12799=ADVANCED_FACE ( 'NONE', ( #68588 ), #45662, .F. ) ;
#12800=DIRECTION ( 'NONE',  ( -1.000000000000000000, 0.000000000000000000, -0.000000000000000000 ) ) ;
#12801=DIRECTION ( 'NONE',  ( -1.000000000000000000, 0.000000000000000000, 0.000000000000000000 ) ) ;
#12811=CARTESIAN_POINT ( 'NONE',  ( -3.000000000000000000, -22.67460108101783334, 6.353146135317912169 ) ) ;
#12836=ORIENTED_EDGE ( 'NONE', *, *, #6079, .F. ) ;
#12851=DIRECTION ( 'NONE',  ( 0.000000000000000000, 0.9510565162951544194, -0.3090169943749446757 ) ) ;
#12854=CARTESIAN_POINT ( 'NONE',  ( 10.00000000000000000, 16.23288003029497162, 33.80338159004289622 ) ) ;
#12866=CARTESIAN_POINT ( 'NONE',  ( 0.000000000000000000, 35.38097989696512968, 12.42422080174651100 ) ) ;
#12875=VERTEX_POINT ( 'NONE', #70393 ) ;
#12893=VECTOR ( 'NONE', #26005, 1000.000000000000114 ) ;
#12908=DIRECTION ( 'NONE',  ( -1.000000000000000000, 0.000000000000000000, 0.000000000000000000 ) ) ;
#12913=EDGE_CURVE ( 'NONE', #38975, #48180, #44285, .T. ) ;
#12918=CARTESIAN_POINT ( 'NONE',  ( 0.000000000000000000, -19.89357724624987256, -12.59942793731086041 ) ) ;
#12924=EDGE_LOOP ( 'NONE', ( #52614, #31377, #9885, #27634 ) ) ;
#12929=AXIS2_PLACEMENT_3D ( 'NONE', #11151, #12250, #13721 ) ;
#12931=ORIENTED_EDGE ( 'NONE', *, *, #61024, .T. ) ;
#12934=ORIENTED_EDGE ( 'NONE', *, *, #12964, .T. ) ;
#12946=VERTEX_POINT ( 'NONE', #57675 ) ;
#12958=CARTESIAN_POINT ( 'NONE',  ( 0.000000000000000000, -3.948201729842348850, 23.21447184625293048 ) ) ;
#12959=CYLINDRICAL_SURFACE ( 'NONE', #56398, 42.00000000000000000 ) ;
#12964=EDGE_CURVE ( 'NONE', #35320, #12946, #52660, .T. ) ;
#12974=DIRECTION ( 'NONE',  ( -1.000000000000000000, 0.000000000000000000, 0.000000000000000000 ) ) ;
#12978=CARTESIAN_POINT ( 'NONE',  ( 10.00000000000000000, 37.58145647212453611, 0.6853352020791767529 ) ) ;
#12990=CIRCLE ( 'NONE', #16650, 16.00000000000000000 ) ;
#12994=DIRECTION ( 'NONE',  ( 0.000000000000000000, -0.7071067811865389130, -0.7071067811865561215 ) ) ;
#12999=VECTOR ( 'NONE', #21687, 1000.000000000000000 ) ;
#13002=ADVANCED_FACE ( 'NONE', ( #23816 ), #17796, .T. ) ;
#13003=ORIENTED_EDGE ( 'NONE', *, *, #55454, .T. ) ;
#13005=EDGE_CURVE ( 'NONE', #12406, #51690, #20225, .T. ) ;
#13009=AXIS2_PLACEMENT_3D ( 'NONE', #44769, #25976, #48904 ) ;
#13010=CIRCLE ( 'NONE', #72999, 16.00000000000000355 ) ;
#13011=ORIENTED_EDGE ( 'NONE', *, *, #10015, .F. ) ;
#13022=ORIENTED_EDGE ( 'NONE', *, *, #47979, .F. ) ;
#13026=DIRECTION ( 'NONE',  ( 0.000000000000000000, -0.2079116908177653100, 0.9781476007338044676 ) ) ;
#13034=ORIENTED_EDGE ( 'NONE', *, *, #19683, .T. ) ;
#13049=DIRECTION ( 'NONE',  ( 0.000000000000000000, 0.3090169943749442316, 0.9510565162951545304 ) ) ;
#13050=LINE ( 'NONE', #35614, #46741 ) ;
#13051=ORIENTED_EDGE ( 'NONE', *, *, #60023, .F. ) ;
#13062=ORIENTED_EDGE ( 'NONE', *, *, #51000, .T. ) ;
#13065=AXIS2_PLACEMENT_3D ( 'NONE', #40726, #2018, #34705 ) ;
#13066=VECTOR ( 'NONE', #14760, 1000.000000000000000 ) ;
#13100=AXIS2_PLACEMENT_3D ( 'NONE', #49594, #20285, #14647 ) ;
#13106=CYLINDRICAL_SURFACE ( 'NONE', #19723, 16.00000000000000000 ) ;
#13113=ORIENTED_EDGE ( 'NONE', *, *, #64585, .T. ) ;
#13133=( NAMED_UNIT ( * ) SI_UNIT ( $, .STERADIAN. ) SOLID_ANGLE_UNIT ( ) );
#13158=CIRCLE ( 'NONE', #55176, 42.00000000000000000 ) ;
#13164=AXIS2_PLACEMENT_3D ( 'NONE', #41868, #74321, #5920 ) ;
#13166=DIRECTION ( 'NONE',  ( -1.000000000000000000, 0.000000000000000000, 0.000000000000000000 ) ) ;
#13167=EDGE_CURVE ( 'NONE', #66514, #39991, #10992, .T. ) ;
#13177=DIRECTION ( 'NONE',  ( 0.000000000000000000, 0.000000000000000000, 1.000000000000000000 ) ) ;
#13196=DIRECTION ( 'NONE',  ( 0.000000000000000000, 0.000000000000000000, 1.000000000000000000 ) ) ;
#13210=CIRCLE ( 'NONE', #2491, 42.00000000000000000 ) ;
#13217=DIRECTION ( 'NONE',  ( 0.000000000000000000, 0.5877852522924744694, -0.8090169943749465631 ) ) ;
#13231=VECTOR ( 'NONE', #42948, 1000.000000000000000 ) ;
#13235=EDGE_CURVE ( 'NONE', #50602, #54476, #25074, .T. ) ;
#13255=DIRECTION ( 'NONE',  ( 0.000000000000000000, -0.7431448254773954654, 0.6691306063588569053 ) ) ;
#13261=EDGE_CURVE ( 'NONE', #30694, #70056, #53896, .T. ) ;
#13290=ORIENTED_EDGE ( 'NONE', *, *, #51398, .T. ) ;
#13297=CARTESIAN_POINT ( 'NONE',  ( -3.000000000000000000, -18.13022148937243472, -15.02647892043568767 ) ) ;
#13298=ORIENTED_EDGE ( 'NONE', *, *, #1499, .T. ) ;
#13301=ORIENTED_EDGE ( 'NONE', *, *, #37358, .F. ) ;
#13311=ORIENTED_EDGE ( 'NONE', *, *, #46371, .F. ) ;
#13313=AXIS2_PLACEMENT_3D ( 'NONE', #55154, #4048, #48771 ) ;
#13314=AXIS2_PLACEMENT_3D ( 'NONE', #3565, #66340, #30612 ) ;
#13317=VECTOR ( 'NONE', #40830, 1000.000000000000000 ) ;
#13322=CARTESIAN_POINT ( 'NONE',  ( 10.00000000000000000, -30.00120703465222149, 22.64427369931158296 ) ) ;
#13325=DIRECTION ( 'NONE',  ( 0.000000000000000000, 0.4539904997395479702, -0.8910065241883673437 ) ) ;
#13332=EDGE_CURVE ( 'NONE', #26331, #36342, #25130, .T. ) ;
#13336=CARTESIAN_POINT ( 'NONE',  ( 0.000000000000000000, 39.04073710021344112, 15.48615015657596672 ) ) ;
#13339=CARTESIAN_POINT ( 'NONE',  ( 0.000000000000000000, 0.000000000000000000, 0.000000000000000000 ) ) ;
#13342=ORIENTED_EDGE ( 'NONE', *, *, #5174, .F. ) ;
#13351=CARTESIAN_POINT ( 'NONE',  ( -3.000000000000000000, -23.29833615347109443, 3.418703333116492438 ) ) ;
#13362=CARTESIAN_POINT ( 'NONE',  ( 10.00000000000000000, 0.000000000000000000, 0.000000000000000000 ) ) ;
#13383=DIRECTION ( 'NONE',  ( -1.000000000000000000, 0.000000000000000000, 0.000000000000000000 ) ) ;
#13385=LINE ( 'NONE', #24668, #36666 ) ;
#13386=VERTEX_POINT ( 'NONE', #39299 ) ;
#13394=DIRECTION ( 'NONE',  ( 1.000000000000000000, 0.000000000000000000, -0.000000000000000000 ) ) ;
#13406=CARTESIAN_POINT ( 'NONE',  ( 0.000000000000000000, 37.58145647212453611, 0.6853352020791767529 ) ) ;
#13412=ORIENTED_EDGE ( 'NONE', *, *, #65183, .F. ) ;
#13420=LINE ( 'NONE', #1454, #32164 ) ;
#13437=CARTESIAN_POINT ( 'NONE',  ( 10.00000000000000000, 6.555932627142418312, 37.01155633439060466 ) ) ;
#13452=DIRECTION ( 'NONE',  ( 0.000000000000000000, -0.9945218953682730678, -0.1045284632676570929 ) ) ;
#13454=CARTESIAN_POINT ( 'NONE',  ( -3.000000000000000000, 8.688484142253939169, 21.88630264137371029 ) ) ;
#13480=VERTEX_POINT ( 'NONE', #11812 ) ;
#13481=CARTESIAN_POINT ( 'NONE',  ( 10.00000000000000000, 0.000000000000000000, 0.000000000000000000 ) ) ;
#13523=DIRECTION ( 'NONE',  ( -1.000000000000000000, 0.000000000000000000, 0.000000000000000000 ) ) ;
#13524=ORIENTED_EDGE ( 'NONE', *, *, #36941, .T. ) ;
#13532=CARTESIAN_POINT ( 'NONE',  ( 10.00000000000000000, -16.45098606841102651, -33.79645857604531045 ) ) ;
#13537=CARTESIAN_POINT ( 'NONE',  ( 0.000000000000000000, -13.04903810567647682, -19.60159698893442481 ) ) ;
#13551=LINE ( 'NONE', #6808, #22465 ) ;
#13561=CARTESIAN_POINT ( 'NONE',  ( 10.00000000000000000, 10.74501242461282757, 35.92658777277515014 ) ) ;
#13566=ORIENTED_EDGE ( 'NONE', *, *, #1687, .F. ) ;
#13588=EDGE_LOOP ( 'NONE', ( #11174, #40881, #17153, #73782 ) ) ;
#13590=EDGE_LOOP ( 'NONE', ( #62819, #69121 ) ) ;
#13600=VERTEX_POINT ( 'NONE', #54639 ) ;
#13602=DIRECTION ( 'NONE',  ( 0.000000000000000000, 0.000000000000000000, -1.000000000000000000 ) ) ;
#13646=DIRECTION ( 'NONE',  ( -1.000000000000000000, -0.000000000000000000, 0.000000000000000000 ) ) ;
#13647=EDGE_LOOP ( 'NONE', ( #8618, #56121, #21425, #24502 ) ) ;
#13648=FACE_OUTER_BOUND ( 'NONE', #6912, .T. ) ;
#13654=ORIENTED_EDGE ( 'NONE', *, *, #51533, .T. ) ;
#13658=CARTESIAN_POINT ( 'NONE',  ( 5.000000000000000000, 26.79245525562714292, 32.34446384429980981 ) ) ;
#13667=ORIENTED_EDGE ( 'NONE', *, *, #51726, .F. ) ;
#13670=EDGE_CURVE ( 'NONE', #35666, #68796, #45551, .T. ) ;
#13671=VERTEX_POINT ( 'NONE', #48632 ) ;
#13680=DIRECTION ( 'NONE',  ( -1.000000000000000000, 0.000000000000000000, -0.000000000000000000 ) ) ;
#13693=AXIS2_PLACEMENT_3D ( 'NONE', #34487, #5945, #51785 ) ;
#13703=AXIS2_PLACEMENT_3D ( 'NONE', #35468, #69312, #34353 ) ;
#13714=DIRECTION ( 'NONE',  ( 0.000000000000000000, 0.6691306063588675634, -0.7431448254773856954 ) ) ;
#13718=AXIS2_PLACEMENT_3D ( 'NONE', #24516, #47452, #70356 ) ;
#13721=DIRECTION ( 'NONE',  ( 0.000000000000000000, 0.000000000000000000, -1.000000000000000000 ) ) ;
#13724=CARTESIAN_POINT ( 'NONE',  ( 0.000000000000000000, -26.08949754953044220, 27.05870788708222818 ) ) ;
#13750=ORIENTED_EDGE ( 'NONE', *, *, #45768, .F. ) ;
#13754=EDGE_CURVE ( 'NONE', #73125, #32561, #20340, .T. ) ;
#13771=LINE ( 'NONE', #30688, #64254 ) ;
#13792=CYLINDRICAL_SURFACE ( 'NONE', #31202, 16.00000000000000000 ) ;
#13801=DIRECTION ( 'NONE',  ( 0.000000000000000000, 0.000000000000000000, 1.000000000000000000 ) ) ;
#13811=EDGE_CURVE ( 'NONE', #48459, #64733, #38087, .T. ) ;
#13825=CARTESIAN_POINT ( 'NONE',  ( 0.000000000000000000, -18.13022148937263012, 15.02647892043544608 ) ) ;
#13828=AXIS2_PLACEMENT_3D ( 'NONE', #72315, #73420, #55772 ) ;
#13842=VERTEX_POINT ( 'NONE', #5383 ) ;
#13850=ORIENTED_EDGE ( 'NONE', *, *, #7997, .F. ) ;
#13855=DIRECTION ( 'NONE',  ( -1.000000000000000000, -0.000000000000000000, -0.000000000000000000 ) ) ;
#13857=VERTEX_POINT ( 'NONE', #28279 ) ;
#13867=VERTEX_POINT ( 'NONE', #51217 ) ;
#13881=DIRECTION ( 'NONE',  ( -1.000000000000000000, -0.000000000000000000, 0.000000000000000000 ) ) ;
#13895=CARTESIAN_POINT ( 'NONE',  ( 0.000000000000000000, -4.261787119644969479, -26.19803753235780519 ) ) ;
#13915=EDGE_LOOP ( 'NONE', ( #53850, #49635, #54370, #36643 ) ) ;
#13929=ORIENTED_EDGE ( 'NONE', *, *, #17918, .F. ) ;
#13937=ORIENTED_EDGE ( 'NONE', *, *, #37935, .F. ) ;
#13945=ORIENTED_EDGE ( 'NONE', *, *, #35419, .F. ) ;
#13949=VERTEX_POINT ( 'NONE', #22658 ) ;
#13958=AXIS2_PLACEMENT_3D ( 'NONE', #67044, #33569, #11022 ) ;
#13983=AXIS2_PLACEMENT_3D ( 'NONE', #66477, #71717, #36775 ) ;
#13987=EDGE_CURVE ( 'NONE', #15802, #21912, #68895, .T. ) ;
#14000=CARTESIAN_POINT ( 'NONE',  ( 0.000000000000000000, -36.13751322684404244, -21.40280677340410165 ) ) ;
#14009=DIRECTION ( 'NONE',  ( 0.000000000000000000, 0.7431448254773946882, -0.6691306063588577935 ) ) ;
#14010=CIRCLE ( 'NONE', #56040, 16.00000000000000000 ) ;
#14018=VECTOR ( 'NONE', #47575, 1000.000000000000000 ) ;
#14021=VERTEX_POINT ( 'NONE', #65109 ) ;
#14029=CARTESIAN_POINT ( 'NONE',  ( 5.000000000000000000, -35.47612816024539484, 22.48208911017487921 ) ) ;
#14037=ORIENTED_EDGE ( 'NONE', *, *, #33979, .F. ) ;
#14059=CIRCLE ( 'NONE', #2144, 37.49900000000000233 ) ;
#14067=ORIENTED_EDGE ( 'NONE', *, *, #46776, .T. ) ;
#14070=ORIENTED_EDGE ( 'NONE', *, *, #38007, .F. ) ;
#14074=VECTOR ( 'NONE', #41121, 1000.000000000000000 ) ;
#14090=FACE_OUTER_BOUND ( 'NONE', #63625, .T. ) ;
#14092=LINE ( 'NONE', #32499, #52619 ) ;
#14105=EDGE_CURVE ( 'NONE', #51481, #7862, #2046, .T. ) ;
#14108=VERTEX_POINT ( 'NONE', #37641 ) ;
#14136=EDGE_CURVE ( 'NONE', #67800, #14697, #69245, .T. ) ;
#14142=EDGE_CURVE ( 'NONE', #59223, #42410, #36883, .T. ) ;
#14157=CARTESIAN_POINT ( 'NONE',  ( -3.000000000000000000, -18.13022148937263012, 15.02647892043544608 ) ) ;
#14170=EDGE_CURVE ( 'NONE', #58159, #18231, #14010, .T. ) ;
#14184=DIRECTION ( 'NONE',  ( -1.000000000000000000, 0.000000000000000000, -0.000000000000000000 ) ) ;
#14191=DIRECTION ( 'NONE',  ( -1.000000000000000000, 0.000000000000000000, 0.000000000000000000 ) ) ;
#14193=EDGE_LOOP ( 'NONE', ( #66569, #53415, #30582, #58879 ) ) ;
#14212=DIRECTION ( 'NONE',  ( 1.000000000000000000, 0.000000000000000000, 0.000000000000000000 ) ) ;
#14242=VECTOR ( 'NONE', #40010, 1000.000000000000000 ) ;
#14244=DIRECTION ( 'NONE',  ( 0.000000000000000000, 0.7071067811865487940, -0.7071067811865462405 ) ) ;
#14251=PLANE ( 'NONE',  #25261 ) ;
#14253=VECTOR ( 'NONE', #35755, 1000.000000000000000 ) ;
#14257=CARTESIAN_POINT ( 'NONE',  ( 10.00000000000000000, 22.74946021919175720, -29.81001611430984255 ) ) ;
#14270=FACE_OUTER_BOUND ( 'NONE', #4321, .T. ) ;
#14287=CARTESIAN_POINT ( 'NONE',  ( -3.000000000000000000, 5.835314593368772229, -22.81335362449846826 ) ) ;
#14291=PLANE ( 'NONE',  #38822 ) ;
#14301=AXIS2_PLACEMENT_3D ( 'NONE', #46265, #51899, #57919 ) ;
#14316=DIRECTION ( 'NONE',  ( 0.000000000000000000, -0.7071067811865536790, 0.7071067811865413555 ) ) ;
#14317=ORIENTED_EDGE ( 'NONE', *, *, #13811, .F. ) ;
#14321=VERTEX_POINT ( 'NONE', #10177 ) ;
#14338=ORIENTED_EDGE ( 'NONE', *, *, #66195, .T. ) ;
#14364=EDGE_CURVE ( 'NONE', #56884, #16859, #27258, .T. ) ;
#14373=EDGE_CURVE ( 'NONE', #11102, #11035, #1541, .T. ) ;
#14389=VECTOR ( 'NONE', #44085, 1000.000000000000000 ) ;
#14395=VECTOR ( 'NONE', #62957, 999.9999999999998863 ) ;
#14405=ORIENTED_EDGE ( 'NONE', *, *, #3770, .F. ) ;
#14408=LINE ( 'NONE', #31691, #7006 ) ;
#14415=AXIS2_PLACEMENT_3D ( 'NONE', #57959, #22639, #63242 ) ;
#14428=ORIENTED_EDGE ( 'NONE', *, *, #55658, .T. ) ;
#14433=DIRECTION ( 'NONE',  ( 0.000000000000000000, 0.7071067811865437980, 0.7071067811865512365 ) ) ;
#14453=EDGE_CURVE ( 'NONE', #59274, #32004, #69186, .T. ) ;
#14477=DIRECTION ( 'NONE',  ( 0.000000000000000000, 0.5000000000000039968, -0.8660254037844363761 ) ) ;
#14480=CYLINDRICAL_SURFACE ( 'NONE', #20642, 16.00000000000000000 ) ;
#14499=DIRECTION ( 'NONE',  ( 0.000000000000000000, 0.8090169943749487835, -0.5877852522924713607 ) ) ;
#14514=DIRECTION ( 'NONE',  ( -1.000000000000000000, -0.000000000000000000, -0.000000000000000000 ) ) ;
#14519=CARTESIAN_POINT ( 'NONE',  ( 0.000000000000000000, -22.67460108101783334, 6.353146135317912169 ) ) ;
#14524=DIRECTION ( 'NONE',  ( -0.000000000000000000, 0.9945218953682731788, 0.1045284632676559550 ) ) ;
#14525=ORIENTED_EDGE ( 'NONE', *, *, #25215, .T. ) ;
#14532=DIRECTION ( 'NONE',  ( -1.000000000000000000, 0.000000000000000000, 0.000000000000000000 ) ) ;
#14547=ORIENTED_EDGE ( 'NONE', *, *, #73847, .T. ) ;
#14563=DIRECTION ( 'NONE',  ( -1.000000000000000000, -0.000000000000000000, 0.000000000000000000 ) ) ;
#14597=EDGE_LOOP ( 'NONE', ( #20445, #16365, #37571, #54692 ) ) ;
#14602=EDGE_LOOP ( 'NONE', ( #15250, #46334, #44092, #51040 ) ) ;
#14603=DIRECTION ( 'NONE',  ( 1.000000000000000000, 0.000000000000000000, 0.000000000000000000 ) ) ;
#14624=EDGE_LOOP ( 'NONE', ( #36265, #56426, #55287, #4108 ) ) ;
#14645=DIRECTION ( 'NONE',  ( -1.000000000000000000, -0.000000000000000000, 0.000000000000000000 ) ) ;
#14647=DIRECTION ( 'NONE',  ( 0.000000000000000000, -0.8090169943749531134, 0.5877852522924653655 ) ) ;
#14657=AXIS2_PLACEMENT_3D ( 'NONE', #18352, #51836, #1119 ) ;
#14672=AXIS2_PLACEMENT_3D ( 'NONE', #16761, #11115, #613 ) ;
#14697=VERTEX_POINT ( 'NONE', #22124 ) ;
#14719=DIRECTION ( 'NONE',  ( 0.000000000000000000, 0.000000000000000000, 1.000000000000000000 ) ) ;
#14731=ORIENTED_EDGE ( 'NONE', *, *, #17146, .T. ) ;
#14744=DIRECTION ( 'NONE',  ( 0.000000000000000000, -0.5877852522924624790, -0.8090169943749550008 ) ) ;
#14745=DIRECTION ( 'NONE',  ( 0.000000000000000000, 0.9135454576426003115, 0.4067366430758017071 ) ) ;
#14757=EDGE_CURVE ( 'NONE', #13857, #21073, #58184, .T. ) ;
#14760=DIRECTION ( 'NONE',  ( 1.000000000000000000, -0.000000000000000000, -0.000000000000000000 ) ) ;
#14762=AXIS2_PLACEMENT_3D ( 'NONE', #31872, #20220, #43563 ) ;
#14766=CARTESIAN_POINT ( 'NONE',  ( 10.00000000000000000, -38.55633173627023069, 16.65560815589396526 ) ) ;
#14767=EDGE_CURVE ( 'NONE', #67442, #27250, #46536, .T. ) ;
#14781=EDGE_LOOP ( 'NONE', ( #13929, #38070, #64097, #67670 ) ) ;
#14790=ORIENTED_EDGE ( 'NONE', *, *, #9917, .T. ) ;
#14791=EDGE_LOOP ( 'NONE', ( #35142, #1179, #53118, #45968 ) ) ;
#14806=ORIENTED_EDGE ( 'NONE', *, *, #66333, .T. ) ;
#14814=LINE ( 'NONE', #60695, #3109 ) ;
#14817=LINE ( 'NONE', #26094, #52306 ) ;
#14835=AXIS2_PLACEMENT_3D ( 'NONE', #47213, #34823, #29527 ) ;
#14838=LINE ( 'NONE', #37787, #60646 ) ;
#14845=CARTESIAN_POINT ( 'NONE',  ( -10.00000000000000000, 0.000000000000000000, 0.000000000000000000 ) ) ;
#14850=VECTOR ( 'NONE', #49935, 1000.000000000000000 ) ;
#14886=AXIS2_PLACEMENT_3D ( 'NONE', #46759, #47132, #29814 ) ;
#14891=DIRECTION ( 'NONE',  ( -1.000000000000000000, 0.000000000000000000, 0.000000000000000000 ) ) ;
#14892=DIRECTION ( 'NONE',  ( -1.000000000000000000, -0.000000000000000000, 0.000000000000000000 ) ) ;
#14894=DIRECTION ( 'NONE',  ( 0.000000000000000000, 0.000000000000000000, -1.000000000000000000 ) ) ;
#14925=FACE_BOUND ( 'NONE', #55864, .T. ) ;
#14926=EDGE_CURVE ( 'NONE', #64628, #46924, #66063, .T. ) ;
#14930=CYLINDRICAL_SURFACE ( 'NONE', #37268, 16.00000000000000000 ) ;
#14936=DIRECTION ( 'NONE',  ( 0.000000000000000000, 0.9510565162951521989, 0.3090169943749515591 ) ) ;
#14940=DIRECTION ( 'NONE',  ( -1.000000000000000000, 0.000000000000000000, -0.000000000000000000 ) ) ;
#14953=DIRECTION ( 'NONE',  ( -0.000000000000000000, 0.1045284632676570929, -0.9945218953682730678 ) ) ;
#14956=CARTESIAN_POINT ( 'NONE',  ( 10.00000000000000000, 12.26510123303259725, 35.53030884539089840 ) ) ;
#14966=PLANE ( 'NONE',  #5744 ) ;
#14975=LINE ( 'NONE', #37183, #28175 ) ;
#14982=LINE ( 'NONE', #33372, #45266 ) ;
#14984=VECTOR ( 'NONE', #43995, 1000.000000000000000 ) ;
#14996=DIRECTION ( 'NONE',  ( -1.000000000000000000, 0.000000000000000000, 0.000000000000000000 ) ) ;
#15012=CARTESIAN_POINT ( 'NONE',  ( -10.00000000000000000, 0.000000000000000000, 0.000000000000000000 ) ) ;
#15019=CARTESIAN_POINT ( 'NONE',  ( 10.00000000000000000, 27.13269053701096922, 25.88420570971410228 ) ) ;
#15020=ADVANCED_FACE ( 'NONE', ( #72045 ), #26181, .T. ) ;
#15021=CARTESIAN_POINT ( 'NONE',  ( 10.00000000000000000, -35.92658777277502935, -10.74501242461320594 ) ) ;
#15043=LINE ( 'NONE', #21411, #15485 ) ;
#15049=CIRCLE ( 'NONE', #9043, 42.00000000000000000 ) ;
#15058=CARTESIAN_POINT ( 'NONE',  ( 10.00000000000000000, 0.000000000000000000, 0.000000000000000000 ) ) ;
#15074=ORIENTED_EDGE ( 'NONE', *, *, #46776, .F. ) ;
#15096=VERTEX_POINT ( 'NONE', #10380 ) ;
#15108=ADVANCED_FACE ( 'NONE', ( #9268 ), #26923, .T. ) ;
#15114=LINE ( 'NONE', #2412, #9353 ) ;
#15119=DIRECTION ( 'NONE',  ( 0.000000000000000000, -0.9876883405951393247, 0.1564344650402205161 ) ) ;
#15120=ADVANCED_FACE ( 'NONE', ( #33297 ), #32927, .F. ) ;
#15122=LINE ( 'NONE', #72620, #44268 ) ;
#15129=DIRECTION ( 'NONE',  ( -0.000000000000000000, -0.5877852522924789103, 0.8090169943749432324 ) ) ;
#15139=ORIENTED_EDGE ( 'NONE', *, *, #11631, .F. ) ;
#15142=AXIS2_PLACEMENT_3D ( 'NONE', #33196, #21930, #27935 ) ;
#15145=ORIENTED_EDGE ( 'NONE', *, *, #10303, .F. ) ;
#15148=EDGE_CURVE ( 'NONE', #8551, #57100, #65136, .T. ) ;
#15167=DIRECTION ( 'NONE',  ( 1.000000000000000000, -0.000000000000000000, -0.000000000000000000 ) ) ;
#15168=LINE ( 'NONE', #56526, #691 ) ;
#15183=DIRECTION ( 'NONE',  ( 1.000000000000000000, 0.000000000000000000, -0.000000000000000000 ) ) ;
#15204=AXIS2_PLACEMENT_3D ( 'NONE', #2353, #71084, #60214 ) ;
#15206=DIRECTION ( 'NONE',  ( -1.000000000000000000, 0.000000000000000000, -0.000000000000000000 ) ) ;
#15207=DIRECTION ( 'NONE',  ( -1.000000000000000000, 0.000000000000000000, 0.000000000000000000 ) ) ;
#15210=DIRECTION ( 'NONE',  ( 0.000000000000000000, 0.8660254037844432595, -0.4999999999999919509 ) ) ;
#15213=DIRECTION ( 'NONE',  ( 0.000000000000000000, -0.5877852522924789103, 0.8090169943749432324 ) ) ;
#15223=CYLINDRICAL_SURFACE ( 'NONE', #17299, 16.00000000000000000 ) ;
#15232=ORIENTED_EDGE ( 'NONE', *, *, #22071, .T. ) ;
#15233=CARTESIAN_POINT ( 'NONE',  ( -3.000000000000000000, 16.61724383029390140, -20.69703378468903665 ) ) ;
#15237=ORIENTED_EDGE ( 'NONE', *, *, #36241, .F. ) ;
#15250=ORIENTED_EDGE ( 'NONE', *, *, #9187, .F. ) ;
#15251=VERTEX_POINT ( 'NONE', #22409 ) ;
#15277=VERTEX_POINT ( 'NONE', #32789 ) ;
#15292=EDGE_CURVE ( 'NONE', #12564, #17471, #3520, .T. ) ;
#15303=AXIS2_PLACEMENT_3D ( 'NONE', #55523, #67170, #4039 ) ;
#15323=CARTESIAN_POINT ( 'NONE',  ( 10.00000000000000000, 0.000000000000000000, 0.000000000000000000 ) ) ;
#15330=DIRECTION ( 'NONE',  ( 0.000000000000000000, -0.8910065241883722287, 0.4539904997395382558 ) ) ;
#15350=VERTEX_POINT ( 'NONE', #62128 ) ;
#15356=ORIENTED_EDGE ( 'NONE', *, *, #62833, .T. ) ;
#15360=CARTESIAN_POINT ( 'NONE',  ( 0.000000000000000000, -30.80686688397025108, 21.53537804866070715 ) ) ;
#15373=CARTESIAN_POINT ( 'NONE',  ( 10.00000000000000000, -40.68715046381937128, 10.41901085202062660 ) ) ;
#15375=EDGE_CURVE ( 'NONE', #44000, #68072, #57054, .T. ) ;
#15383=AXIS2_PLACEMENT_3D ( 'NONE', #55374, #49718, #15891 ) ;
#15394=CARTESIAN_POINT ( 'NONE',  ( 0.000000000000000000, 14.60985201121704513, 18.46759930825707841 ) ) ;
#15400=DIRECTION ( 'NONE',  ( -1.000000000000000000, -0.000000000000000000, 0.000000000000000000 ) ) ;
#15402=VECTOR ( 'NONE', #25753, 1000.000000000000000 ) ;
#15403=CIRCLE ( 'NONE', #57447, 15.99999999999999822 ) ;
#15411=ORIENTED_EDGE ( 'NONE', *, *, #44740, .T. ) ;
#15414=ORIENTED_EDGE ( 'NONE', *, *, #56224, .T. ) ;
#15417=VERTEX_POINT ( 'NONE', #10813 ) ;
#15426=DIRECTION ( 'NONE',  ( 1.000000000000000000, -0.000000000000000000, 0.000000000000000000 ) ) ;
#15452=EDGE_CURVE ( 'NONE', #26707, #34118, #391, .T. ) ;
#15469=ADVANCED_FACE ( 'NONE', ( #11177 ), #15709, .F. ) ;
#15484=LINE ( 'NONE', #3489, #73648 ) ;
#15485=VECTOR ( 'NONE', #20688, 999.9999999999998863 ) ;
#15493=FACE_OUTER_BOUND ( 'NONE', #40693, .T. ) ;
#15503=LINE ( 'NONE', #32782, #47992 ) ;
#15507=CARTESIAN_POINT ( 'NONE',  ( 10.00000000000000000, -6.736453364083292428, -36.88895765772640800 ) ) ;
#15516=LINE ( 'NONE', #7753, #48636 ) ;
#15534=ORIENTED_EDGE ( 'NONE', *, *, #41524, .F. ) ;
#15544=DIRECTION ( 'NONE',  ( -1.000000000000000000, -0.000000000000000000, -0.000000000000000000 ) ) ;
#15549=VECTOR ( 'NONE', #39772, 1000.000000000000000 ) ;
#15551=AXIS2_PLACEMENT_3D ( 'NONE', #60188, #43270, #9027 ) ;
#15553=EDGE_CURVE ( 'NONE', #9784, #34086, #30673, .T. ) ;
#15560=DIRECTION ( 'NONE',  ( 1.000000000000000000, 0.000000000000000000, -0.000000000000000000 ) ) ;
#15566=CARTESIAN_POINT ( 'NONE',  ( 0.000000000000000000, -37.01155633439063308, 6.555932627142289526 ) ) ;
#15571=DIRECTION ( 'NONE',  ( 0.000000000000000000, 0.000000000000000000, 1.000000000000000000 ) ) ;
#15585=CARTESIAN_POINT ( 'NONE',  ( 0.000000000000000000, 14.60985201121729737, -18.46759930825687945 ) ) ;
#15595=LINE ( 'NONE', #55819, #12164 ) ;
#15615=EDGE_CURVE ( 'NONE', #70065, #16929, #7761, .T. ) ;
#15619=ORIENTED_EDGE ( 'NONE', *, *, #33025, .F. ) ;
#15631=ORIENTED_EDGE ( 'NONE', *, *, #70276, .F. ) ;
#15632=EDGE_LOOP ( 'NONE', ( #11449, #26314, #48379, #3421 ) ) ;
#15639=PLANE ( 'NONE',  #43820 ) ;
#15655=CARTESIAN_POINT ( 'NONE',  ( -3.000000000000000000, -26.23277895567251505, 4.042438405569750870 ) ) ;
#15656=AXIS2_PLACEMENT_3D ( 'NONE', #42952, #42576, #65887 ) ;
#15660=DIRECTION ( 'NONE',  ( -1.000000000000000000, 0.000000000000000000, 0.000000000000000000 ) ) ;
#15709=PLANE ( 'NONE',  #42372 ) ;
#15720=EDGE_LOOP ( 'NONE', ( #63534, #68746, #64368, #17008 ) ) ;
#15722=DIRECTION ( 'NONE',  ( 0.000000000000000000, -0.9781476007338070211, 0.2079116908177525425 ) ) ;
#15733=DIRECTION ( 'NONE',  ( -1.000000000000000000, 0.000000000000000000, -0.000000000000000000 ) ) ;
#15739=CARTESIAN_POINT ( 'NONE',  ( 10.00000000000000000, -4.992566952384716927, -37.16516213103282951 ) ) ;
#15740=ORIENTED_EDGE ( 'NONE', *, *, #2446, .F. ) ;
#15748=CARTESIAN_POINT ( 'NONE',  ( 10.00000000000000000, 0.000000000000000000, 0.000000000000000000 ) ) ;
#15781=PRODUCT_DEFINITION_SHAPE ( 'NONE', 'NONE',  #11351 ) ;
#15783=ORIENTED_EDGE ( 'NONE', *, *, #44646, .F. ) ;
#15792=VECTOR ( 'NONE', #57662, 1000.000000000000000 ) ;
#15794=ORIENTED_EDGE ( 'NONE', *, *, #6291, .F. ) ;
#15802=VERTEX_POINT ( 'NONE', #54364 ) ;
#15804=ORIENTED_EDGE ( 'NONE', *, *, #9917, .F. ) ;
#15805=DIRECTION ( 'NONE',  ( 0.000000000000000000, 0.000000000000000000, 1.000000000000000000 ) ) ;
#15806=ORIENTED_EDGE ( 'NONE', *, *, #70363, .F. ) ;
#15812=EDGE_LOOP ( 'NONE', ( #47813, #3748, #16167, #34285 ) ) ;
#15816=CARTESIAN_POINT ( 'NONE',  ( -3.000000000000000000, -22.32062822937469804, -14.36278369418829826 ) ) ;
#15820=ADVANCED_FACE ( 'NONE', ( #49455 ), #42714, .T. ) ;
#15832=EDGE_LOOP ( 'NONE', ( #16776, #33086, #3674, #69516 ) ) ;
#15839=DIRECTION ( 'NONE',  ( 0.000000000000000000, 0.9135454576426063067, -0.4067366430757881068 ) ) ;
#15843=DIRECTION ( 'NONE',  ( -1.000000000000000000, -0.000000000000000000, 0.000000000000000000 ) ) ;
#15862=ORIENTED_EDGE ( 'NONE', *, *, #62118, .T. ) ;
#15863=CARTESIAN_POINT ( 'NONE',  ( -3.000000000000000000, 16.83928648764945279, -16.46020748918028076 ) ) ;
#15869=CARTESIAN_POINT ( 'NONE',  ( 10.00000000000000000, -27.75498641678764855, 31.52238457039589647 ) ) ;
#15876=DIRECTION ( 'NONE',  ( 1.000000000000000000, 0.000000000000000000, -0.000000000000000000 ) ) ;
#15879=DIRECTION ( 'NONE',  ( -1.000000000000000000, 0.000000000000000000, -0.000000000000000000 ) ) ;
#15881=DIRECTION ( 'NONE',  ( 0.000000000000000000, 0.000000000000000000, -1.000000000000000000 ) ) ;
#15889=DIRECTION ( 'NONE',  ( 0.000000000000000000, -0.3090169943749548342, 0.9510565162951511997 ) ) ;
#15891=DIRECTION ( 'NONE',  ( 0.000000000000000000, 0.000000000000000000, 1.000000000000000000 ) ) ;
#15898=CARTESIAN_POINT ( 'NONE',  ( 0.000000000000000000, 0.000000000000000000, 0.000000000000000000 ) ) ;
#15899=AXIS2_PLACEMENT_3D ( 'NONE', #62003, #3385, #72513 ) ;
#15931=CARTESIAN_POINT ( 'NONE',  ( -3.000000000000000000, -18.13022148937263012, 15.02647892043544608 ) ) ;
#15947=EDGE_CURVE ( 'NONE', #70917, #16273, #51304, .T. ) ;
#15969=EDGE_CURVE ( 'NONE', #11647, #52639, #56966, .T. ) ;
#15971=EDGE_CURVE ( 'NONE', #7975, #61324, #44193, .T. ) ;
#16004=DIRECTION ( 'NONE',  ( 0.000000000000000000, 0.000000000000000000, -1.000000000000000000 ) ) ;
#16008=AXIS2_PLACEMENT_3D ( 'NONE', #72379, #43837, #65647 ) ;
#16027=EDGE_CURVE ( 'NONE', #24755, #12738, #47244, .T. ) ;
#16029=CARTESIAN_POINT ( 'NONE',  ( 0.000000000000000000, -37.01155633439053361, -6.555932627142825986 ) ) ;
#16030=LINE ( 'NONE', #10392, #5414 ) ;
#16031=DIRECTION ( 'NONE',  ( 0.000000000000000000, 0.8910065241883656784, 0.4539904997395510788 ) ) ;
#16039=FACE_BOUND ( 'NONE', #32018, .T. ) ;
#16045=DIRECTION ( 'NONE',  ( 1.000000000000000000, 0.000000000000000000, 0.000000000000000000 ) ) ;
#16052=VECTOR ( 'NONE', #43356, 1000.000000000000000 ) ;
#16054=CARTESIAN_POINT ( 'NONE',  ( 10.00000000000000000, 0.000000000000000000, 0.000000000000000000 ) ) ;
#16066=EDGE_CURVE ( 'NONE', #7862, #1439, #41421, .T. ) ;
#16071=DIRECTION ( 'NONE',  ( -0.000000000000000000, 0.5000000000000039968, -0.8660254037844363761 ) ) ;
#16077=DIRECTION ( 'NONE',  ( 0.000000000000000000, -0.9510565162951503115, -0.3090169943749573878 ) ) ;
#16078=LINE ( 'NONE', #4078, #56851 ) ;
#16095=EDGE_LOOP ( 'NONE', ( #10099, #67814, #62626, #10909 ) ) ;
#16124=CIRCLE ( 'NONE', #10150, 16.00000000000000000 ) ;
#16136=CARTESIAN_POINT ( 'NONE',  ( 0.000000000000000000, -17.80606268964563554, 33.00180498840040855 ) ) ;
#16167=ORIENTED_EDGE ( 'NONE', *, *, #55949, .T. ) ;
#16183=ORIENTED_EDGE ( 'NONE', *, *, #41582, .F. ) ;
#16188=VERTEX_POINT ( 'NONE', #26701 ) ;
#16191=CARTESIAN_POINT ( 'NONE',  ( -3.000000000000000000, -13.04903810567647682, -19.60159698893442481 ) ) ;
#16193=EDGE_CURVE ( 'NONE', #55937, #22473, #32853, .T. ) ;
#16210=EDGE_CURVE ( 'NONE', #35258, #27250, #66216, .T. ) ;
#16214=CIRCLE ( 'NONE', #19801, 16.00000000000000000 ) ;
#16215=EDGE_LOOP ( 'NONE', ( #25504, #56579, #40577, #21188 ) ) ;
#16232=FACE_OUTER_BOUND ( 'NONE', #70468, .T. ) ;
#16241=AXIS2_PLACEMENT_3D ( 'NONE', #69018, #40069, #61896 ) ;
#16242=FACE_OUTER_BOUND ( 'NONE', #73538, .T. ) ;
#16246=CARTESIAN_POINT ( 'NONE',  ( 10.00000000000000000, -33.17418723428319538, 17.67226234102814431 ) ) ;
#16255=VERTEX_POINT ( 'NONE', #25970 ) ;
#16266=ORIENTED_EDGE ( 'NONE', *, *, #32153, .T. ) ;
#16272=EDGE_LOOP ( 'NONE', ( #29564, #43194, #68294, #59009 ) ) ;
#16273=VERTEX_POINT ( 'NONE', #20332 ) ;
#16275=ORIENTED_EDGE ( 'NONE', *, *, #68504, .T. ) ;
#16285=DIRECTION ( 'NONE',  ( 0.000000000000000000, 0.000000000000000000, 1.000000000000000000 ) ) ;
#16286=AXIS2_PLACEMENT_3D ( 'NONE', #23173, #46102, #6259 ) ;
#16300=CARTESIAN_POINT ( 'NONE',  ( -3.000000000000000000, -1.278221433540502217, 26.51162292216071847 ) ) ;
#16302=DIRECTION ( 'NONE',  ( 1.000000000000000000, 0.000000000000000000, -0.000000000000000000 ) ) ;
#16305=DIRECTION ( 'NONE',  ( 0.000000000000000000, 0.8090169943749504489, -0.5877852522924689183 ) ) ;
#16308=LINE ( 'NONE', #39990, #27621 ) ;
#16315=CYLINDRICAL_SURFACE ( 'NONE', #770, 16.00000000000000000 ) ;
#16332=AXIS2_PLACEMENT_3D ( 'NONE', #3933, #26831, #72678 ) ;
#16338=CARTESIAN_POINT ( 'NONE',  ( 10.00000000000000000, -33.17418723428294669, -17.67226234102862747 ) ) ;
#16341=AXIS2_PLACEMENT_3D ( 'NONE', #46675, #17361, #18459 ) ;
#16342=VECTOR ( 'NONE', #37231, 1000.000000000000000 ) ;
#16349=CIRCLE ( 'NONE', #67979, 16.00000000000000000 ) ;
#16351=EDGE_LOOP ( 'NONE', ( #51515, #20069, #15232, #49610 ) ) ;
#16362=CARTESIAN_POINT ( 'NONE',  ( 0.000000000000000000, -16.23288003029521320, 33.80338159004277543 ) ) ;
#16365=ORIENTED_EDGE ( 'NONE', *, *, #64982, .F. ) ;
#16374=DIRECTION ( 'NONE',  ( 0.000000000000000000, 0.9510565162951543083, -0.3090169943749448977 ) ) ;
#16382=EDGE_LOOP ( 'NONE', ( #23393, #5954, #51252, #48165 ) ) ;
#16392=CARTESIAN_POINT ( 'NONE',  ( 10.00000000000000000, 0.000000000000000000, 0.000000000000000000 ) ) ;
#16433=ORIENTED_EDGE ( 'NONE', *, *, #2607, .F. ) ;
#16440=VECTOR ( 'NONE', #40574, 1000.000000000000000 ) ;
#16455=EDGE_CURVE ( 'NONE', #69721, #31367, #49637, .T. ) ;
#16468=CIRCLE ( 'NONE', #11618, 16.00000000000000000 ) ;
#16470=DIRECTION ( 'NONE',  ( -1.000000000000000000, 0.000000000000000000, 0.000000000000000000 ) ) ;
#16480=DIRECTION ( 'NONE',  ( 0.000000000000000000, 0.000000000000000000, 1.000000000000000000 ) ) ;
#16481=CARTESIAN_POINT ( 'NONE',  ( 0.000000000000000000, -17.67226234102801286, -33.17418723428327354 ) ) ;
#16500=DIRECTION ( 'NONE',  ( 0.000000000000000000, -0.2079116908177532086, -0.9781476007338069101 ) ) ;
#16501=CARTESIAN_POINT ( 'NONE',  ( 0.000000000000000000, 16.23288003029543347, -33.80338159004267595 ) ) ;
#16508=CARTESIAN_POINT ( 'NONE',  ( 0.000000000000000000, 14.60985201121704513, 18.46759930825707841 ) ) ;
#16529=ORIENTED_EDGE ( 'NONE', *, *, #15947, .F. ) ;
#16540=VERTEX_POINT ( 'NONE', #36418 ) ;
#16542=ORIENTED_EDGE ( 'NONE', *, *, #5902, .T. ) ;
#16563=ORIENTED_EDGE ( 'NONE', *, *, #38260, .T. ) ;
#16564=AXIS2_PLACEMENT_3D ( 'NONE', #47637, #70544, #19055 ) ;
#16568=VECTOR ( 'NONE', #25778, 1000.000000000000000 ) ;
#16571=EDGE_CURVE ( 'NONE', #67855, #41196, #52987, .T. ) ;
#16582=CYLINDRICAL_SURFACE ( 'NONE', #58510, 16.00000000000000000 ) ;
#16588=CARTESIAN_POINT ( 'NONE',  ( 10.00000000000000000, -37.22597642581153821, -5.202137450156795850 ) ) ;
#16591=CYLINDRICAL_SURFACE ( 'NONE', #59876, 37.49900000000000233 ) ;
#16595=DIRECTION ( 'NONE',  ( -1.000000000000000000, 0.000000000000000000, 0.000000000000000000 ) ) ;
#16596=AXIS2_PLACEMENT_3D ( 'NONE', #32862, #15207, #55060 ) ;
#16600=PLANE ( 'NONE',  #20226 ) ;
#16610=DIRECTION ( 'NONE',  ( 0.000000000000000000, 0.000000000000000000, 1.000000000000000000 ) ) ;
#16611=DIRECTION ( 'NONE',  ( 0.000000000000000000, 0.000000000000000000, 1.000000000000000000 ) ) ;
#16612=DIRECTION ( 'NONE',  ( 0.000000000000000000, 0.9510565162951544194, -0.3090169943749447867 ) ) ;
#16616=AXIS2_PLACEMENT_3D ( 'NONE', #65313, #54758, #38205 ) ;
#16618=AXIS2_PLACEMENT_3D ( 'NONE', #58059, #57320, #35125 ) ;
#16624=EDGE_LOOP ( 'NONE', ( #53532, #69174, #26505, #58707 ) ) ;
#16630=ADVANCED_FACE ( 'NONE', ( #3353 ), #54828, .F. ) ;
#16638=DIRECTION ( 'NONE',  ( -1.000000000000000000, 0.000000000000000000, 0.000000000000000000 ) ) ;
#16644=VECTOR ( 'NONE', #6580, 1000.000000000000000 ) ;
#16646=FACE_OUTER_BOUND ( 'NONE', #2240, .T. ) ;
#16650=AXIS2_PLACEMENT_3D ( 'NONE', #30095, #11686, #34260 ) ;
#16651=VERTEX_POINT ( 'NONE', #26245 ) ;
#16673=DIRECTION ( 'NONE',  ( -1.000000000000000000, 0.000000000000000000, -0.000000000000000000 ) ) ;
#16680=VECTOR ( 'NONE', #70279, 1000.000000000000114 ) ;
#16683=DIRECTION ( 'NONE',  ( 0.000000000000000000, 0.7071067811865487940, -0.7071067811865462405 ) ) ;
#16690=DIRECTION ( 'NONE',  ( 0.000000000000000000, 0.000000000000000000, 1.000000000000000000 ) ) ;
#16700=LINE ( 'NONE', #45661, #26165 ) ;
#16718=DIRECTION ( 'NONE',  ( 0.000000000000000000, -0.7071067811865389130, -0.7071067811865563435 ) ) ;
#16719=AXIS2_PLACEMENT_3D ( 'NONE', #41296, #36015, #18351 ) ;
#16733=AXIS2_PLACEMENT_3D ( 'NONE', #54782, #47300, #42396 ) ;
#16761=CARTESIAN_POINT ( 'NONE',  ( 0.000000000000000000, -37.58145647212453611, -0.6853352020794456489 ) ) ;
#16774=AXIS2_PLACEMENT_3D ( 'NONE', #41814, #31273, #53838 ) ;
#16776=ORIENTED_EDGE ( 'NONE', *, *, #66053, .T. ) ;
#16780=ORIENTED_EDGE ( 'NONE', *, *, #52387, .T. ) ;
#16784=DIRECTION ( 'NONE',  ( -1.000000000000000000, -0.000000000000000000, 0.000000000000000000 ) ) ;
#16787=ORIENTED_EDGE ( 'NONE', *, *, #63613, .F. ) ;
#16799=FACE_OUTER_BOUND ( 'NONE', #17858, .T. ) ;
#16817=FACE_OUTER_BOUND ( 'NONE', #27658, .T. ) ;
#16835=CARTESIAN_POINT ( 'NONE',  ( -3.000000000000000000, 18.84667830672605859, -18.68964196561243796 ) ) ;
#16838=ORIENTED_EDGE ( 'NONE', *, *, #26802, .T. ) ;
#16847=DIRECTION ( 'NONE',  ( 0.000000000000000000, 0.000000000000000000, 1.000000000000000000 ) ) ;
#16852=CARTESIAN_POINT ( 'NONE',  ( 10.00000000000000000, 36.88895765772633695, 6.736453364083687667 ) ) ;
#16859=VERTEX_POINT ( 'NONE', #11923 ) ;
#16862=CARTESIAN_POINT ( 'NONE',  ( 0.000000000000000000, -40.98264845739743123, -9.188173127307734944 ) ) ;
#16877=LINE ( 'NONE', #39810, #6823 ) ;
#16904=CIRCLE ( 'NONE', #144, 16.00000000000000000 ) ;
#16905=ADVANCED_FACE ( 'NONE', ( #68722 ), #17207, .T. ) ;
#16913=EDGE_LOOP ( 'NONE', ( #42908, #47864, #49159, #8552 ) ) ;
#16914=ORIENTED_EDGE ( 'NONE', *, *, #25456, .T. ) ;
#16917=DIRECTION ( 'NONE',  ( 0.000000000000000000, -0.8090169943749402348, -0.5877852522924830181 ) ) ;
#16929=VERTEX_POINT ( 'NONE', #70530 ) ;
#16932=ORIENTED_EDGE ( 'NONE', *, *, #53043, .F. ) ;
#16943=DIRECTION ( 'NONE',  ( 0.000000000000000000, 0.4539904997395412534, 0.8910065241883706744 ) ) ;
#16967=CYLINDRICAL_SURFACE ( 'NONE', #7342, 37.49900000000000233 ) ;
#16975=EDGE_LOOP ( 'NONE', ( #8907, #34198, #1690, #48747 ) ) ;
#16990=EDGE_CURVE ( 'NONE', #32331, #67112, #32954, .T. ) ;
#16991=CARTESIAN_POINT ( 'NONE',  ( 0.000000000000000000, -16.65560815589439159, 38.55633173627004595 ) ) ;
#16992=CARTESIAN_POINT ( 'NONE',  ( 0.000000000000000000, -27.13269053701078448, -25.88420570971428702 ) ) ;
#16998=CARTESIAN_POINT ( 'NONE',  ( 0.000000000000000000, -36.13751322684434797, 21.40280677340357940 ) ) ;
#17003=DIRECTION ( 'NONE',  ( -1.000000000000000000, -0.000000000000000000, 0.000000000000000000 ) ) ;
#17008=ORIENTED_EDGE ( 'NONE', *, *, #41400, .T. ) ;
#17010=ORIENTED_EDGE ( 'NONE', *, *, #53208, .F. ) ;
#17024=AXIS2_PLACEMENT_3D ( 'NONE', #49215, #49950, #72143 ) ;
#17056=ORIENTED_EDGE ( 'NONE', *, *, #25152, .F. ) ;
#17092=ORIENTED_EDGE ( 'NONE', *, *, #54722, .T. ) ;
#17099=CARTESIAN_POINT ( 'NONE',  ( 10.00000000000000000, 0.000000000000000000, 0.000000000000000000 ) ) ;
#17111=ORIENTED_EDGE ( 'NONE', *, *, #51398, .F. ) ;
#17114=ORIENTED_EDGE ( 'NONE', *, *, #69857, .T. ) ;
#17115=CARTESIAN_POINT ( 'NONE',  ( 0.000000000000000000, -0.8828120875898013420, -37.48860685352291711 ) ) ;
#17141=CARTESIAN_POINT ( 'NONE',  ( 0.000000000000000000, 0.000000000000000000, 0.000000000000000000 ) ) ;
#17146=EDGE_CURVE ( 'NONE', #7677, #14321, #19779, .T. ) ;
#17153=ORIENTED_EDGE ( 'NONE', *, *, #69031, .F. ) ;
#17162=CARTESIAN_POINT ( 'NONE',  ( 5.000000000000000000, 35.47612816024556537, -22.48208911017461631 ) ) ;
#17178=ADVANCED_FACE ( 'NONE', ( #60037 ), #71275, .T. ) ;
#17182=DIRECTION ( 'NONE',  ( 0.000000000000000000, -0.4067366430757897722, -0.9135454576426056406 ) ) ;
#17184=EDGE_CURVE ( 'NONE', #47180, #10365, #63898, .T. ) ;
#17189=EDGE_LOOP ( 'NONE', ( #70713, #61160, #28392, #11904 ) ) ;
#17190=ORIENTED_EDGE ( 'NONE', *, *, #31496, .T. ) ;
#17195=CARTESIAN_POINT ( 'NONE',  ( 0.000000000000000000, -11.95096189432312350, -23.69967320028773372 ) ) ;
#17197=AXIS2_PLACEMENT_3D ( 'NONE', #70395, #30555, #18903 ) ;
#17202=ORIENTED_EDGE ( 'NONE', *, *, #59343, .F. ) ;
#17204=VECTOR ( 'NONE', #39918, 1000.000000000000000 ) ;
#17207=CYLINDRICAL_SURFACE ( 'NONE', #13693, 16.00000000000000000 ) ;
#17213=ORIENTED_EDGE ( 'NONE', *, *, #15947, .T. ) ;
#17231=FACE_OUTER_BOUND ( 'NONE', #33462, .T. ) ;
#17244=CARTESIAN_POINT ( 'NONE',  ( 0.000000000000000000, -10.74501242461258244, -35.92658777277521409 ) ) ;
#17251=DIRECTION ( 'NONE',  ( 0.000000000000000000, 0.000000000000000000, 1.000000000000000000 ) ) ;
#17262=VECTOR ( 'NONE', #26201, 1000.000000000000000 ) ;
#17268=FACE_OUTER_BOUND ( 'NONE', #11715, .T. ) ;
#17272=CARTESIAN_POINT ( 'NONE',  ( 0.000000000000000000, -12.26510123303234501, -35.53030884539098366 ) ) ;
#17299=AXIS2_PLACEMENT_3D ( 'NONE', #36673, #66374, #25765 ) ;
#17311=EDGE_CURVE ( 'NONE', #23404, #57225, #11469, .T. ) ;
#17318=CARTESIAN_POINT ( 'NONE',  ( 0.000000000000000000, 30.00120703465236716, -22.64427369931138756 ) ) ;
#17329=CIRCLE ( 'NONE', #50912, 16.00000000000000355 ) ;
#17355=CARTESIAN_POINT ( 'NONE',  ( 0.000000000000000000, -0.9646360437375309793, 23.52805723605590416 ) ) ;
#17361=DIRECTION ( 'NONE',  ( -1.000000000000000000, 0.000000000000000000, 0.000000000000000000 ) ) ;
#17401=DIRECTION ( 'NONE',  ( 0.000000000000000000, 0.000000000000000000, 1.000000000000000000 ) ) ;
#17410=ADVANCED_FACE ( 'NONE', ( #53181 ), #64102, .T. ) ;
#17416=DIRECTION ( 'NONE',  ( 0.000000000000000000, -0.5877852522924689183, -0.8090169943749504489 ) ) ;
#17438=CYLINDRICAL_SURFACE ( 'NONE', #37833, 37.49900000000000233 ) ;
#17441=AXIS2_PLACEMENT_3D ( 'NONE', #73456, #21961, #37422 ) ;
#17449=CARTESIAN_POINT ( 'NONE',  ( 0.000000000000000000, 21.53537804866081373, 30.80686688397018358 ) ) ;
#17463=VECTOR ( 'NONE', #69059, 1000.000000000000000 ) ;
#17466=ADVANCED_FACE ( 'NONE', ( #7324 ), #70446, .F. ) ;
#17471=VERTEX_POINT ( 'NONE', #24973 ) ;
#17480=ORIENTED_EDGE ( 'NONE', *, *, #53128, .F. ) ;
#17493=CARTESIAN_POINT ( 'NONE',  ( 0.000000000000000000, 10.96151621346540317, -35.95386929396244113 ) ) ;
#17501=DIRECTION ( 'NONE',  ( -1.000000000000000000, 0.000000000000000000, 0.000000000000000000 ) ) ;
#17509=VERTEX_POINT ( 'NONE', #29126 ) ;
#17513=DIRECTION ( 'NONE',  ( 0.000000000000000000, -0.4067366430757887730, -0.9135454576426059736 ) ) ;
#17536=VERTEX_POINT ( 'NONE', #18588 ) ;
#17545=PLANE ( 'NONE',  #13164 ) ;
#17553=VERTEX_POINT ( 'NONE', #43018 ) ;
#17582=VECTOR ( 'NONE', #35367, 1000.000000000000000 ) ;
#17588=CARTESIAN_POINT ( 'NONE',  ( 0.000000000000000000, 21.32104025579114648, 30.84782396557224970 ) ) ;
#17590=DIRECTION ( 'NONE',  ( 0.000000000000000000, 0.000000000000000000, -1.000000000000000000 ) ) ;
#17596=EDGE_LOOP ( 'NONE', ( #11116, #70140, #71739, #1168 ) ) ;
#17607=CARTESIAN_POINT ( 'NONE',  ( 0.000000000000000000, 0.000000000000000000, 0.000000000000000000 ) ) ;
#17608=EDGE_CURVE ( 'NONE', #20975, #17752, #72314, .T. ) ;
#17611=ORIENTED_EDGE ( 'NONE', *, *, #73163, .T. ) ;
#17614=LINE ( 'NONE', #64582, #73860 ) ;
#17621=CARTESIAN_POINT ( 'NONE',  ( 0.000000000000000000, 0.000000000000000000, 0.000000000000000000 ) ) ;
#17629=DIRECTION ( 'NONE',  ( 1.000000000000000000, -0.000000000000000000, -0.000000000000000000 ) ) ;
#17637=CIRCLE ( 'NONE', #4449, 42.00000000000000000 ) ;
#17646=ORIENTED_EDGE ( 'NONE', *, *, #66895, .F. ) ;
#17647=EDGE_CURVE ( 'NONE', #28395, #56198, #17329, .T. ) ;
#17656=ORIENTED_EDGE ( 'NONE', *, *, #44412, .T. ) ;
#17667=ORIENTED_EDGE ( 'NONE', *, *, #32824, .F. ) ;
#17690=EDGE_LOOP ( 'NONE', ( #16838, #58558, #26936, #13654 ) ) ;
#17706=CARTESIAN_POINT ( 'NONE',  ( 0.000000000000000000, 5.835314593368772229, -22.81335362449846826 ) ) ;
#17707=VERTEX_POINT ( 'NONE', #4287 ) ;
#17712=LINE ( 'NONE', #35013, #33330 ) ;
#17713=DIRECTION ( 'NONE',  ( 0.000000000000000000, -1.000000000000000000, 1.156482317317870936E-15 ) ) ;
#17725=ORIENTED_EDGE ( 'NONE', *, *, #58584, .F. ) ;
#17752=VERTEX_POINT ( 'NONE', #27934 ) ;
#17753=VERTEX_POINT ( 'NONE', #28296 ) ;
#17770=ORIENTED_EDGE ( 'NONE', *, *, #25215, .F. ) ;
#17778=CARTESIAN_POINT ( 'NONE',  ( 0.000000000000000000, 0.000000000000000000, 0.000000000000000000 ) ) ;
#17781=FACE_OUTER_BOUND ( 'NONE', #53470, .T. ) ;
#17784=ORIENTED_EDGE ( 'NONE', *, *, #39423, .T. ) ;
#17786=CARTESIAN_POINT ( 'NONE',  ( 0.000000000000000000, -0.9646360437375307573, 23.52805723605590060 ) ) ;
#17788=CARTESIAN_POINT ( 'NONE',  ( 0.000000000000000000, -14.54903810567645195, -22.19967320028775504 ) ) ;
#17791=EDGE_LOOP ( 'NONE', ( #6606, #52069, #42845, #67023 ) ) ;
#17796=CYLINDRICAL_SURFACE ( 'NONE', #7039, 37.49900000000000233 ) ;
#17841=ORIENTED_EDGE ( 'NONE', *, *, #3860, .F. ) ;
#17857=AXIS2_PLACEMENT_3D ( 'NONE', #71518, #24209, #47136 ) ;
#17858=EDGE_LOOP ( 'NONE', ( #9647, #35507, #17114, #44952 ) ) ;
#17869=DIRECTION ( 'NONE',  ( -1.000000000000000000, 0.000000000000000000, 0.000000000000000000 ) ) ;
#17878=AXIS2_PLACEMENT_3D ( 'NONE', #5032, #27936, #17401 ) ;
#17881=DIRECTION ( 'NONE',  ( 0.000000000000000000, 0.000000000000000000, 1.000000000000000000 ) ) ;
#17882=CARTESIAN_POINT ( 'NONE',  ( -3.000000000000000000, 16.61724383029390140, -20.69703378468903665 ) ) ;
#17897=CARTESIAN_POINT ( 'NONE',  ( 10.00000000000000000, 0.000000000000000000, 0.000000000000000000 ) ) ;
#17901=AXIS2_PLACEMENT_3D ( 'NONE', #33122, #67724, #73345 ) ;
#17918=EDGE_CURVE ( 'NONE', #58363, #60133, #68959, .T. ) ;
#17925=EDGE_CURVE ( 'NONE', #16651, #72554, #1752, .T. ) ;
#17932=CARTESIAN_POINT ( 'NONE',  ( 0.000000000000000000, 36.13751322684419165, 21.40280677340384585 ) ) ;
#17969=AXIS2_PLACEMENT_3D ( 'NONE', #68537, #55758, #10259 ) ;
#17970=AXIS2_PLACEMENT_3D ( 'NONE', #25128, #64993, #58227 ) ;
#17982=CARTESIAN_POINT ( 'NONE',  ( 0.000000000000000000, 36.88895765772642221, -6.736453364083161865 ) ) ;
#18010=DIRECTION ( 'NONE',  ( -1.000000000000000000, 0.000000000000000000, 0.000000000000000000 ) ) ;
#18034=ORIENTED_EDGE ( 'NONE', *, *, #56694, .T. ) ;
#18046=ORIENTED_EDGE ( 'NONE', *, *, #46181, .F. ) ;
#18085=ADVANCED_FACE ( 'NONE', ( #2374 ), #30881, .F. ) ;
#18102=DIRECTION ( 'NONE',  ( -1.000000000000000000, 0.000000000000000000, -0.000000000000000000 ) ) ;
#18103=VECTOR ( 'NONE', #23446, 1000.000000000000000 ) ;
#18108=CARTESIAN_POINT ( 'NONE',  ( -10.00000000000000000, 0.000000000000000000, 0.000000000000000000 ) ) ;
#18110=VERTEX_POINT ( 'NONE', #10845 ) ;
#18113=ORIENTED_EDGE ( 'NONE', *, *, #43748, .T. ) ;
#18115=AXIS2_PLACEMENT_3D ( 'NONE', #19539, #64677, #31190 ) ;
#18121=AXIS2_PLACEMENT_3D ( 'NONE', #34232, #39887, #32731 ) ;
#18123=EDGE_LOOP ( 'NONE', ( #22762, #26755, #37911, #32636 ) ) ;
#18125=ORIENTED_EDGE ( 'NONE', *, *, #57591, .T. ) ;
#18138=CYLINDRICAL_SURFACE ( 'NONE', #64079, 42.00000000000000000 ) ;
#18147=DIRECTION ( 'NONE',  ( 0.000000000000000000, 0.6691306063588675634, -0.7431448254773856954 ) ) ;
#18149=DIRECTION ( 'NONE',  ( 0.000000000000000000, -0.3090169943749349057, -0.9510565162951576390 ) ) ;
#18159=EDGE_LOOP ( 'NONE', ( #33688, #45733, #61619, #27516 ) ) ;
#18160=EDGE_CURVE ( 'NONE', #3179, #9784, #64182, .T. ) ;
#18173=CARTESIAN_POINT ( 'NONE',  ( 0.000000000000000000, 6.762365576493645669, -25.66652317338392209 ) ) ;
#18183=DIRECTION ( 'NONE',  ( 0.000000000000000000, 0.4067366430757887730, 0.9135454576426059736 ) ) ;
#18187=VERTEX_POINT ( 'NONE', #68369 ) ;
#18200=CIRCLE ( 'NONE', #44626, 16.00000000000000355 ) ;
#18216=EDGE_LOOP ( 'NONE', ( #9846, #52235, #51969, #62930 ) ) ;
#18226=AXIS2_PLACEMENT_3D ( 'NONE', #64427, #13646, #70046 ) ;
#18231=VERTEX_POINT ( 'NONE', #16862 ) ;
#18236=VERTEX_POINT ( 'NONE', #11940 ) ;
#18240=LINE ( 'NONE', #35528, #65506 ) ;
#18245=DIRECTION ( 'NONE',  ( 0.000000000000000000, 0.1564344650402244852, 0.9876883405951387696 ) ) ;
#18250=ADVANCED_FACE ( 'NONE', ( #52165 ), #27758, .T. ) ;
#18251=CARTESIAN_POINT ( 'NONE',  ( 10.00000000000000000, 38.55633173627010990, 16.65560815589424593 ) ) ;
#18255=ORIENTED_EDGE ( 'NONE', *, *, #11683, .F. ) ;
#18257=FACE_OUTER_BOUND ( 'NONE', #44857, .T. ) ;
#18259=AXIS2_PLACEMENT_3D ( 'NONE', #51317, #46810, #46064 ) ;
#18260=CARTESIAN_POINT ( 'NONE',  ( 0.000000000000000000, 0.000000000000000000, 0.000000000000000000 ) ) ;
#18281=CIRCLE ( 'NONE', #30294, 37.49900000000000233 ) ;
#18288=DIRECTION ( 'NONE',  ( 1.000000000000000000, -0.000000000000000000, 0.000000000000000000 ) ) ;
#18301=VERTEX_POINT ( 'NONE', #29585 ) ;
#18320=ORIENTED_EDGE ( 'NONE', *, *, #1254, .F. ) ;
#18329=CIRCLE ( 'NONE', #35126, 37.49900000000000944 ) ;
#18335=DIRECTION ( 'NONE',  ( 0.000000000000000000, 0.8090169943749486725, -0.5877852522924714718 ) ) ;
#18342=DIRECTION ( 'NONE',  ( 0.000000000000000000, 0.000000000000000000, 1.000000000000000000 ) ) ;
#18351=DIRECTION ( 'NONE',  ( 0.000000000000000000, 0.000000000000000000, 1.000000000000000000 ) ) ;
#18352=CARTESIAN_POINT ( 'NONE',  ( 0.000000000000000000, 0.000000000000000000, 0.000000000000000000 ) ) ;
#18354=EDGE_CURVE ( 'NONE', #9960, #73246, #58181, .T. ) ;
#18360=AXIS2_PLACEMENT_3D ( 'NONE', #17099, #40030, #27991 ) ;
#18371=ORIENTED_EDGE ( 'NONE', *, *, #30848, .F. ) ;
#18376=CARTESIAN_POINT ( 'NONE',  ( 4.999999999999999112, 40.68715046381927891, 10.41901085202092858 ) ) ;
#18380=ORIENTED_EDGE ( 'NONE', *, *, #69914, .F. ) ;
#18397=ORIENTED_EDGE ( 'NONE', *, *, #28357, .T. ) ;
#18405=ORIENTED_EDGE ( 'NONE', *, *, #69497, .T. ) ;
#18408=CARTESIAN_POINT ( 'NONE',  ( 10.00000000000000000, 12.42422080174639021, 35.38097989696516521 ) ) ;
#18410=VECTOR ( 'NONE', #41323, 1000.000000000000000 ) ;
#18423=ORIENTED_EDGE ( 'NONE', *, *, #62568, .T. ) ;
#18425=DIRECTION ( 'NONE',  ( -1.000000000000000000, 0.000000000000000000, 0.000000000000000000 ) ) ;
#18459=DIRECTION ( 'NONE',  ( 0.000000000000000000, 0.000000000000000000, 1.000000000000000000 ) ) ;
#18470=ORIENTED_EDGE ( 'NONE', *, *, #60385, .F. ) ;
#18474=VECTOR ( 'NONE', #15210, 1000.000000000000000 ) ;
#18490=EDGE_LOOP ( 'NONE', ( #59643, #59511, #20023, #46369 ) ) ;
#18509=CARTESIAN_POINT ( 'NONE',  ( -3.000000000000000000, -3.948201729842038432, -23.21447184625298021 ) ) ;
#18532=AXIS2_PLACEMENT_3D ( 'NONE', #12448, #24478, #52309 ) ;
#18541=FACE_OUTER_BOUND ( 'NONE', #7113, .T. ) ;
#18564=AXIS2_PLACEMENT_3D ( 'NONE', #56704, #67971, #16847 ) ;
#18565=EDGE_CURVE ( 'NONE', #30584, #55375, #26920, .T. ) ;
#18571=ORIENTED_EDGE ( 'NONE', *, *, #16990, .F. ) ;
#18578=VERTEX_POINT ( 'NONE', #57001 ) ;
#18585=DIRECTION ( 'NONE',  ( -1.000000000000000000, 0.000000000000000000, 0.000000000000000000 ) ) ;
#18588=CARTESIAN_POINT ( 'NONE',  ( 0.000000000000000000, -35.38097989696503021, -12.42422080174676147 ) ) ;
#18607=EDGE_CURVE ( 'NONE', #61409, #27461, #11488, .T. ) ;
#18616=CARTESIAN_POINT ( 'NONE',  ( 10.00000000000000000, 35.47612816024523141, 22.48208911017513145 ) ) ;
#18621=CARTESIAN_POINT ( 'NONE',  ( 0.000000000000000000, -12.42422080174614862, -35.38097989696524337 ) ) ;
#18646=CARTESIAN_POINT ( 'NONE',  ( 0.000000000000000000, -35.47612816024539484, 22.48208911017487921 ) ) ;
#18648=ADVANCED_FACE ( 'NONE', ( #34416 ), #45352, .T. ) ;
#18652=DIRECTION ( 'NONE',  ( 0.000000000000000000, 0.000000000000000000, 1.000000000000000000 ) ) ;
#18669=DIRECTION ( 'NONE',  ( 1.000000000000000000, -0.000000000000000000, -0.000000000000000000 ) ) ;
#18683=DIRECTION ( 'NONE',  ( -1.000000000000000000, 0.000000000000000000, 0.000000000000000000 ) ) ;
#18691=ADVANCED_FACE ( 'NONE', ( #21656 ), #67902, .T. ) ;
#18695=AXIS2_PLACEMENT_3D ( 'NONE', #22810, #12974, #52848 ) ;
#18707=ORIENTED_EDGE ( 'NONE', *, *, #31719, .T. ) ;
#18726=CARTESIAN_POINT ( 'NONE',  ( 10.00000000000000000, -6.736453364083817341, 36.88895765772630142 ) ) ;
#18730=LINE ( 'NONE', #47683, #69596 ) ;
#18733=ADVANCED_FACE ( 'NONE', ( #29507 ), #6955, .T. ) ;
#18734=LINE ( 'NONE', #7096, #51163 ) ;
#18738=VERTEX_POINT ( 'NONE', #63755 ) ;
#18774=EDGE_LOOP ( 'NONE', ( #57072, #7849, #2141, #26927 ) ) ;
#18788=CIRCLE ( 'NONE', #22401, 16.00000000000000000 ) ;
#18791=CARTESIAN_POINT ( 'NONE',  ( 0.000000000000000000, -3.948201729842348850, 23.21447184625293048 ) ) ;
#18792=LINE ( 'NONE', #453, #17582 ) ;
#18794=CARTESIAN_POINT ( 'NONE',  ( 10.00000000000000000, 0.000000000000000000, 0.000000000000000000 ) ) ;
#18823=ADVANCED_FACE ( 'NONE', ( #53564 ), #30617, .T. ) ;
#18828=CARTESIAN_POINT ( 'NONE',  ( 10.00000000000000000, 37.01155633439059756, 6.555932627142549762 ) ) ;
#18838=LINE ( 'NONE', #53798, #19024 ) ;
#18842=VECTOR ( 'NONE', #12420, 1000.000000000000000 ) ;
#18846=VERTEX_POINT ( 'NONE', #40817 ) ;
#18858=ORIENTED_EDGE ( 'NONE', *, *, #40686, .F. ) ;
#18861=DIRECTION ( 'NONE',  ( 0.000000000000000000, 0.000000000000000000, 1.000000000000000000 ) ) ;
#18867=CARTESIAN_POINT ( 'NONE',  ( 0.000000000000000000, 22.07842321921481243, 8.187992925817422218 ) ) ;
#18900=DIRECTION ( 'NONE',  ( 1.000000000000000000, 0.000000000000000000, 0.000000000000000000 ) ) ;
#18903=DIRECTION ( 'NONE',  ( 0.000000000000000000, 0.000000000000000000, 1.000000000000000000 ) ) ;
#18907=DIRECTION ( 'NONE',  ( -1.000000000000000000, -0.000000000000000000, -0.000000000000000000 ) ) ;
#18912=ORIENTED_EDGE ( 'NONE', *, *, #23458, .F. ) ;
#18932=EDGE_LOOP ( 'NONE', ( #43384, #46215, #1980, #62842 ) ) ;
#18942=AXIS2_PLACEMENT_3D ( 'NONE', #50996, #57381, #5158 ) ;
#18953=CARTESIAN_POINT ( 'NONE',  ( -3.000000000000000000, -0.9646360437375307573, 23.52805723605590060 ) ) ;
#18956=LINE ( 'NONE', #42646, #10826 ) ;
#18965=CARTESIAN_POINT ( 'NONE',  ( 10.00000000000000000, -35.38097989696520074, 12.42422080174625520 ) ) ;
#18970=CARTESIAN_POINT ( 'NONE',  ( -3.000000000000000000, 22.07842321921481243, 8.187992925817422218 ) ) ;
#18978=CARTESIAN_POINT ( 'NONE',  ( 10.00000000000000000, -2.663952781846440576, 41.91543099594817789 ) ) ;
#18994=EDGE_CURVE ( 'NONE', #55743, #67887, #14817, .T. ) ;
#19006=LINE ( 'NONE', #41958, #71221 ) ;
#19016=AXIS2_PLACEMENT_3D ( 'NONE', #52778, #58408, #59530 ) ;
#19018=EDGE_CURVE ( 'NONE', #3129, #67030, #43422, .T. ) ;
#19024=VECTOR ( 'NONE', #53434, 1000.000000000000000 ) ;
#19025=CARTESIAN_POINT ( 'NONE',  ( 10.00000000000000000, 16.45098606841126454, 33.79645857604518966 ) ) ;
#19030=AXIS2_PLACEMENT_3D ( 'NONE', #10508, #10896, #51107 ) ;
#19038=VERTEX_POINT ( 'NONE', #67059 ) ;
#19047=VECTOR ( 'NONE', #10277, 999.9999999999998863 ) ;
#19055=DIRECTION ( 'NONE',  ( 0.000000000000000000, 0.7071067811865439090, 0.7071067811865512365 ) ) ;
#19065=CIRCLE ( 'NONE', #40652, 42.00000000000000000 ) ;
#19066=ORIENTED_EDGE ( 'NONE', *, *, #13235, .F. ) ;
#19068=CARTESIAN_POINT ( 'NONE',  ( 0.000000000000000000, 26.50000000000000000, -1.500000000000001332 ) ) ;
#19087=DIRECTION ( 'NONE',  ( -1.000000000000000000, 0.000000000000000000, -0.000000000000000000 ) ) ;
#19102=ADVANCED_FACE ( 'NONE', ( #39985 ), #23071, .F. ) ;
#19103=CARTESIAN_POINT ( 'NONE',  ( 10.00000000000000000, 0.000000000000000000, 0.000000000000000000 ) ) ;
#19106=AXIS2_PLACEMENT_3D ( 'NONE', #3834, #22598, #5323 ) ;
#19109=AXIS2_PLACEMENT_3D ( 'NONE', #55472, #51302, #74236 ) ;
#19110=AXIS2_PLACEMENT_3D ( 'NONE', #70460, #24986, #53195 ) ;
#19122=CARTESIAN_POINT ( 'NONE',  ( 10.00000000000000000, 35.53030884539102630, -12.26510123303222599 ) ) ;
#19124=ORIENTED_EDGE ( 'NONE', *, *, #11186, .F. ) ;
#19135=ORIENTED_EDGE ( 'NONE', *, *, #41227, .F. ) ;
#19142=ORIENTED_EDGE ( 'NONE', *, *, #30753, .F. ) ;
#19165=CARTESIAN_POINT ( 'NONE',  ( 0.000000000000000000, 33.17418723428333749, -17.67226234102790272 ) ) ;
#19189=DIRECTION ( 'NONE',  ( 0.000000000000000000, 0.000000000000000000, 1.000000000000000000 ) ) ;
#19194=VECTOR ( 'NONE', #32715, 1000.000000000000000 ) ;
#19202=DIRECTION ( 'NONE',  ( 0.000000000000000000, -0.1564344650402170189, -0.9876883405951399908 ) ) ;
#19219=ORIENTED_EDGE ( 'NONE', *, *, #993, .T. ) ;
#19225=CARTESIAN_POINT ( 'NONE',  ( 10.00000000000000000, 37.01155633439059756, 6.555932627142549762 ) ) ;
#19238=VERTEX_POINT ( 'NONE', #1648 ) ;
#19241=CARTESIAN_POINT ( 'NONE',  ( 0.000000000000000000, -22.48208911017525580, 35.47612816024516036 ) ) ;
#19261=FACE_OUTER_BOUND ( 'NONE', #66970, .T. ) ;
#19277=DIRECTION ( 'NONE',  ( 1.000000000000000000, 0.000000000000000000, -0.000000000000000000 ) ) ;
#19279=LINE ( 'NONE', #24559, #14074 ) ;
#19285=DIRECTION ( 'NONE',  ( 1.000000000000000000, -0.000000000000000000, 0.000000000000000000 ) ) ;
#19286=EDGE_CURVE ( 'NONE', #11835, #53383, #69659, .T. ) ;
#19287=EDGE_CURVE ( 'NONE', #44028, #33537, #15049, .T. ) ;
#19295=CIRCLE ( 'NONE', #27719, 37.49900000000000944 ) ;
#19311=ORIENTED_EDGE ( 'NONE', *, *, #2727, .F. ) ;
#19318=EDGE_CURVE ( 'NONE', #60587, #20975, #57107, .T. ) ;
#19334=DIRECTION ( 'NONE',  ( -1.000000000000000000, -0.000000000000000000, -0.000000000000000000 ) ) ;
#19362=EDGE_CURVE ( 'NONE', #41055, #9960, #70376, .T. ) ;
#19368=DIRECTION ( 'NONE',  ( 0.000000000000000000, 0.5877852522924685852, 0.8090169943749508930 ) ) ;
#19396=ORIENTED_EDGE ( 'NONE', *, *, #5951, .F. ) ;
#19420=DIRECTION ( 'NONE',  ( 1.000000000000000000, 0.000000000000000000, 0.000000000000000000 ) ) ;
#19428=COLOUR_RGB ( '', 0.31764706, 0.68627451, 0.89019608) ;
#19430=DIRECTION ( 'NONE',  ( -1.000000000000000000, -0.000000000000000000, -0.000000000000000000 ) ) ;
#19435=VERTEX_POINT ( 'NONE', #6024 ) ;
#19436=DIRECTION ( 'NONE',  ( -1.000000000000000000, -0.000000000000000000, 0.000000000000000000 ) ) ;
#19441=VECTOR ( 'NONE', #34032, 1000.000000000000000 ) ;
#19450=ADVANCED_FACE ( 'NONE', ( #63165 ), #10905, .T. ) ;
#19464=DIRECTION ( 'NONE',  ( 0.000000000000000000, 0.000000000000000000, 1.000000000000000000 ) ) ;
#19477=VECTOR ( 'NONE', #11595, 1000.000000000000114 ) ;
#19481=DIRECTION ( 'NONE',  ( -1.000000000000000000, 0.000000000000000000, 0.000000000000000000 ) ) ;
#19488=ORIENTED_EDGE ( 'NONE', *, *, #46860, .F. ) ;
#19491=ORIENTED_EDGE ( 'NONE', *, *, #6774, .F. ) ;
#19492=VECTOR ( 'NONE', #41982, 1000.000000000000000 ) ;
#19495=AXIS2_PLACEMENT_3D ( 'NONE', #3480, #33496, #66258 ) ;
#19507=ORIENTED_EDGE ( 'NONE', *, *, #42354, .F. ) ;
#19513=( NAMED_UNIT ( * ) PLANE_ANGLE_UNIT ( ) SI_UNIT ( $, .RADIAN. ) );
#19514=ORIENTED_EDGE ( 'NONE', *, *, #51883, .T. ) ;
#19535=CARTESIAN_POINT ( 'NONE',  ( 10.00000000000000000, -22.64427369931191336, 30.00120703465197280 ) ) ;
#19537=ADVANCED_FACE ( 'NONE', ( #29286 ), #13106, .T. ) ;
#19539=CARTESIAN_POINT ( 'NONE',  ( -3.000000000000000000, 16.83928648764923253, 16.46020748918050458 ) ) ;
#19541=CARTESIAN_POINT ( 'NONE',  ( 10.00000000000000000, 37.16516213103277977, 4.992566952385115719 ) ) ;
#19543=DIRECTION ( 'NONE',  ( -0.000000000000000000, 0.5877852522924696954, 0.8090169943749498938 ) ) ;
#19548=CARTESIAN_POINT ( 'NONE',  ( -3.000000000000000000, -10.45096189432344147, 21.10159698893426494 ) ) ;
#19552=PLANE ( 'NONE',  #8880 ) ;
#19554=VECTOR ( 'NONE', #69490, 999.9999999999998863 ) ;
#19585=DIRECTION ( 'NONE',  ( -1.000000000000000000, -0.000000000000000000, 0.000000000000000000 ) ) ;
#19594=EDGE_CURVE ( 'NONE', #54186, #47415, #64621, .T. ) ;
#19617=VERTEX_POINT ( 'NONE', #70235 ) ;
#19618=DIRECTION ( 'NONE',  ( 1.000000000000000000, 0.000000000000000000, 0.000000000000000000 ) ) ;
#19625=DIRECTION ( 'NONE',  ( 0.000000000000000000, -0.8090169943749508930, 0.5877852522924683631 ) ) ;
#19629=EDGE_CURVE ( 'NONE', #72554, #35320, #72568, .T. ) ;
#19635=CARTESIAN_POINT ( 'NONE',  ( 0.000000000000000000, 5.202137450156389953, 37.22597642581160216 ) ) ;
#19654=ORIENTED_EDGE ( 'NONE', *, *, #14105, .T. ) ;
#19670=VERTEX_POINT ( 'NONE', #54090 ) ;
#19677=DIRECTION ( 'NONE',  ( -1.000000000000000000, 0.000000000000000000, 0.000000000000000000 ) ) ;
#19683=EDGE_CURVE ( 'NONE', #2618, #32855, #23387, .T. ) ;
#19693=PLANE ( 'NONE',  #7532 ) ;
#19719=ORIENTED_EDGE ( 'NONE', *, *, #67114, .F. ) ;
#19723=AXIS2_PLACEMENT_3D ( 'NONE', #19122, #52225, #47694 ) ;
#19735=DIRECTION ( 'NONE',  ( 1.000000000000000000, 0.000000000000000000, 0.000000000000000000 ) ) ;
#19737=CARTESIAN_POINT ( 'NONE',  ( -3.000000000000000000, -10.45096189432344147, 21.10159698893426494 ) ) ;
#19742=CARTESIAN_POINT ( 'NONE',  ( 0.000000000000000000, 0.000000000000000000, 37.49900000000000233 ) ) ;
#19747=VECTOR ( 'NONE', #40976, 1000.000000000000000 ) ;
#19752=DIRECTION ( 'NONE',  ( 1.000000000000000000, 0.000000000000000000, -0.000000000000000000 ) ) ;
#19753=ORIENTED_EDGE ( 'NONE', *, *, #49069, .T. ) ;
#19754=CIRCLE ( 'NONE', #55781, 16.00000000000000355 ) ;
#19762=CARTESIAN_POINT ( 'NONE',  ( -3.000000000000000000, 9.615535125378775305, 24.73947219025917121 ) ) ;
#19772=VERTEX_POINT ( 'NONE', #38264 ) ;
#19779=LINE ( 'NONE', #32163, #48264 ) ;
#19780=DIRECTION ( 'NONE',  ( 1.000000000000000000, 0.000000000000000000, 0.000000000000000000 ) ) ;
#19786=EDGE_CURVE ( 'NONE', #56288, #2618, #48544, .T. ) ;
#19791=ORIENTED_EDGE ( 'NONE', *, *, #23211, .T. ) ;
#19801=AXIS2_PLACEMENT_3D ( 'NONE', #31060, #19780, #25799 ) ;
#19804=DIRECTION ( 'NONE',  ( 0.000000000000000000, 0.000000000000000000, 1.000000000000000000 ) ) ;
#19810=CARTESIAN_POINT ( 'NONE',  ( 10.00000000000000000, 0.000000000000000000, 0.000000000000000000 ) ) ;
#19819=DIRECTION ( 'NONE',  ( 1.000000000000000000, -0.000000000000000000, 0.000000000000000000 ) ) ;
#19831=DIRECTION ( 'NONE',  ( 0.000000000000000000, -1.000000000000000000, -1.040834085586084257E-14 ) ) ;
#19836=VECTOR ( 'NONE', #32221, 1000.000000000000000 ) ;
#19852=ADVANCED_FACE ( 'NONE', ( #21928 ), #44870, .T. ) ;
#19871=CARTESIAN_POINT ( 'NONE',  ( 10.00000000000000178, 0.000000000000000000, 21.00000000000000000 ) ) ;
#19886=AXIS2_PLACEMENT_3D ( 'NONE', #10607, #4995, #51573 ) ;
#19887=ORIENTED_EDGE ( 'NONE', *, *, #54736, .F. ) ;
#19888=CARTESIAN_POINT ( 'NONE',  ( -3.000000000000000000, 14.60985201121729737, -18.46759930825687945 ) ) ;
#19894=ORIENTED_EDGE ( 'NONE', *, *, #17311, .F. ) ;
#19899=CARTESIAN_POINT ( 'NONE',  ( -3.000000000000000000, -0.9646360437372163421, -23.52805723605591126 ) ) ;
#19902=DIRECTION ( 'NONE',  ( 0.000000000000000000, -0.9781476007338041345, -0.2079116908177664480 ) ) ;
#19907=CARTESIAN_POINT ( 'NONE',  ( 0.000000000000000000, -20.55727247249748046, 16.78983467731285018 ) ) ;
#19911=DIRECTION ( 'NONE',  ( 0.000000000000000000, -0.6691306063588662312, 0.7431448254773870277 ) ) ;
#19920=AXIS2_PLACEMENT_3D ( 'NONE', #32417, #55362, #15881 ) ;
#19928=CIRCLE ( 'NONE', #39166, 16.00000000000000000 ) ;
#19932=LINE ( 'NONE', #59806, #69469 ) ;
#19957=ORIENTED_EDGE ( 'NONE', *, *, #63694, .T. ) ;
#19959=ADVANCED_FACE ( 'NONE', ( #51609 ), #18138, .T. ) ;
#19977=CARTESIAN_POINT ( 'NONE',  ( 0.000000000000000000, 0.000000000000000000, 0.000000000000000000 ) ) ;
#19986=DIRECTION ( 'NONE',  ( -1.000000000000000000, 0.000000000000000000, -0.000000000000000000 ) ) ;
#19992=LINE ( 'NONE', #72237, #13231 ) ;
#19993=ORIENTED_EDGE ( 'NONE', *, *, #54809, .T. ) ;
#20001=CARTESIAN_POINT ( 'NONE',  ( 0.000000000000000000, 22.64427369931212297, -30.00120703465181293 ) ) ;
#20003=VERTEX_POINT ( 'NONE', #57258 ) ;
#20007=AXIS2_PLACEMENT_3D ( 'NONE', #5586, #34881, #41260 ) ;
#20023=ORIENTED_EDGE ( 'NONE', *, *, #59501, .T. ) ;
#20057=ORIENTED_EDGE ( 'NONE', *, *, #69758, .T. ) ;
#20059=VERTEX_POINT ( 'NONE', #5402 ) ;
#20062=FACE_OUTER_BOUND ( 'NONE', #47871, .T. ) ;
#20069=ORIENTED_EDGE ( 'NONE', *, *, #57236, .T. ) ;
#20101=LINE ( 'NONE', #20491, #15402 ) ;
#20109=LINE ( 'NONE', #44814, #71857 ) ;
#20113=FACE_OUTER_BOUND ( 'NONE', #66292, .T. ) ;
#20119=ADVANCED_FACE ( 'NONE', ( #42926 ), #53093, .T. ) ;
#20140=ORIENTED_EDGE ( 'NONE', *, *, #16571, .F. ) ;
#20159=ORIENTED_EDGE ( 'NONE', *, *, #14453, .F. ) ;
#20167=CARTESIAN_POINT ( 'NONE',  ( 10.00000000000000000, 21.53537804866081373, 30.80686688397018358 ) ) ;
#20174=CARTESIAN_POINT ( 'NONE',  ( 10.00000000000000000, -25.88420570971381807, -27.13269053701123212 ) ) ;
#20183=AXIS2_PLACEMENT_3D ( 'NONE', #6269, #63408, #51366 ) ;
#20201=VERTEX_POINT ( 'NONE', #36527 ) ;
#20207=EDGE_CURVE ( 'NONE', #56328, #51709, #7959, .T. ) ;
#20220=DIRECTION ( 'NONE',  ( -1.000000000000000000, 0.000000000000000000, 0.000000000000000000 ) ) ;
#20225=CIRCLE ( 'NONE', #1084, 15.99999999999999645 ) ;
#20226=AXIS2_PLACEMENT_3D ( 'NONE', #19737, #43067, #14477 ) ;
#20260=AXIS2_PLACEMENT_3D ( 'NONE', #4919, #10910, #15805 ) ;
#20277=DIRECTION ( 'NONE',  ( -1.000000000000000000, 0.000000000000000000, 0.000000000000000000 ) ) ;
#20285=DIRECTION ( 'NONE',  ( -1.000000000000000000, 0.000000000000000000, 0.000000000000000000 ) ) ;
#20287=EDGE_CURVE ( 'NONE', #18187, #15802, #22120, .T. ) ;
#20288=DIRECTION ( 'NONE',  ( 0.000000000000000000, -0.7431448254773870277, -0.6691306063588662312 ) ) ;
#20292=ADVANCED_FACE ( 'NONE', ( #5963 ), #55958, .T. ) ;
#20317=CIRCLE ( 'NONE', #8299, 42.00000000000000000 ) ;
#20331=ORIENTED_EDGE ( 'NONE', *, *, #53638, .F. ) ;
#20332=CARTESIAN_POINT ( 'NONE',  ( 0.000000000000000000, -25.88420570971419821, 27.13269053701087330 ) ) ;
#20340=CIRCLE ( 'NONE', #50346, 37.49900000000000944 ) ;
#20345=ORIENTED_EDGE ( 'NONE', *, *, #43825, .F. ) ;
#20351=ORIENTED_EDGE ( 'NONE', *, *, #32810, .F. ) ;
#20358=ORIENTED_EDGE ( 'NONE', *, *, #66728, .T. ) ;
#20363=ORIENTED_EDGE ( 'NONE', *, *, #47308, .T. ) ;
#20374=DIRECTION ( 'NONE',  ( 0.000000000000000000, -0.9510565162951543083, 0.3090169943749448977 ) ) ;
#20375=CARTESIAN_POINT ( 'NONE',  ( -3.000000000000000000, -14.54903810567676636, 22.19967320028755964 ) ) ;
#20381=DIRECTION ( 'NONE',  ( -0.000000000000000000, 0.4067366430758000417, -0.9135454576426009776 ) ) ;
#20384=DIRECTION ( 'NONE',  ( -1.000000000000000000, -0.000000000000000000, -0.000000000000000000 ) ) ;
#20388=LINE ( 'NONE', #42581, #12186 ) ;
#20395=CARTESIAN_POINT ( 'NONE',  ( 0.000000000000000000, -22.67460108101782978, 6.353146135317912169 ) ) ;
#20400=CARTESIAN_POINT ( 'NONE',  ( 50.00005079999999680, 2.571758278209441661E-15, -21.00000000000000000 ) ) ;
#20405=LINE ( 'NONE', #44077, #68317 ) ;
#20409=ORIENTED_EDGE ( 'NONE', *, *, #14926, .F. ) ;
#20412=LINE ( 'NONE', #71152, #13066 ) ;
#20420=ORIENTED_EDGE ( 'NONE', *, *, #69088, .F. ) ;
#20426=AXIS2_PLACEMENT_3D ( 'NONE', #71322, #14191, #43166 ) ;
#20427=CIRCLE ( 'NONE', #62475, 37.49900000000000233 ) ;
#20431=ORIENTED_EDGE ( 'NONE', *, *, #65130, .F. ) ;
#20442=EDGE_CURVE ( 'NONE', #31367, #31252, #63838, .T. ) ;
#20445=ORIENTED_EDGE ( 'NONE', *, *, #56090, .F. ) ;
#20470=DIRECTION ( 'NONE',  ( -1.000000000000000000, -0.000000000000000000, 0.000000000000000000 ) ) ;
#20478=PLANE ( 'NONE',  #65132 ) ;
#20488=EDGE_CURVE ( 'NONE', #18578, #52314, #1819, .T. ) ;
#20491=CARTESIAN_POINT ( 'NONE',  ( 5.000000000000000000, 16.65560815589464028, -38.55633173626993226 ) ) ;
#20513=AXIS2_PLACEMENT_3D ( 'NONE', #1370, #30253, #23155 ) ;
#20528=ORIENTED_EDGE ( 'NONE', *, *, #46698, .T. ) ;
#20539=LINE ( 'NONE', #9627, #28412 ) ;
#20543=ORIENTED_EDGE ( 'NONE', *, *, #50845, .T. ) ;
#20548=ORIENTED_EDGE ( 'NONE', *, *, #65995, .T. ) ;
#20559=EDGE_LOOP ( 'NONE', ( #36156, #6187, #12609, #61203 ) ) ;
#20587=LINE ( 'NONE', #66818, #67333 ) ;
#20593=CARTESIAN_POINT ( 'NONE',  ( 4.999999999999999112, 3.925862922256769583, -41.81611651403857621 ) ) ;
#20609=FILL_AREA_STYLE ('',( #55561 ) ) ;
#20613=ORIENTED_EDGE ( 'NONE', *, *, #8430, .F. ) ;
#20617=PLANE ( 'NONE',  #44181 ) ;
#20618=VECTOR ( 'NONE', #59791, 1000.000000000000114 ) ;
#20625=DIRECTION ( 'NONE',  ( 0.000000000000000000, 0.000000000000000000, 1.000000000000000000 ) ) ;
#20626=CIRCLE ( 'NONE', #1465, 42.00000000000000000 ) ;
#20640=EDGE_LOOP ( 'NONE', ( #61510, #69476, #67920, #56511 ) ) ;
#20641=ORIENTED_EDGE ( 'NONE', *, *, #40402, .T. ) ;
#20642=AXIS2_PLACEMENT_3D ( 'NONE', #5450, #51282, #33238 ) ;
#20644=EDGE_CURVE ( 'NONE', #13867, #10228, #31406, .T. ) ;
#20645=VERTEX_POINT ( 'NONE', #38207 ) ;
#20672=AXIS2_PLACEMENT_3D ( 'NONE', #23274, #40936, #34537 ) ;
#20688=DIRECTION ( 'NONE',  ( -0.000000000000000000, 0.9781476007338042455, 0.2079116908177664758 ) ) ;
#20700=ORIENTED_EDGE ( 'NONE', *, *, #51004, .F. ) ;
#20703=ORIENTED_EDGE ( 'NONE', *, *, #66728, .F. ) ;
#20710=ORIENTED_EDGE ( 'NONE', *, *, #57574, .T. ) ;
#20719=VECTOR ( 'NONE', #50928, 1000.000000000000000 ) ;
#20728=VERTEX_POINT ( 'NONE', #15655 ) ;
#20729=ADVANCED_FACE ( 'NONE', ( #40068 ), #38587, .F. ) ;
#20735=DIRECTION ( 'NONE',  ( 0.000000000000000000, 0.000000000000000000, 1.000000000000000000 ) ) ;
#20739=CARTESIAN_POINT ( 'NONE',  ( 10.00000000000000000, 33.79645857604513992, 16.45098606841138178 ) ) ;
#20756=DIRECTION ( 'NONE',  ( 0.000000000000000000, 0.000000000000000000, 1.000000000000000000 ) ) ;
#20773=ADVANCED_FACE ( 'NONE', ( #72766 ), #5503, .T. ) ;
#20774=LINE ( 'NONE', #45205, #765 ) ;
#20777=CARTESIAN_POINT ( 'NONE',  ( 4.999999999999999112, -41.81611651403864727, 3.925862922256025289 ) ) ;
#20788=CARTESIAN_POINT ( 'NONE',  ( 0.000000000000000000, -10.41901085202107247, 40.68715046381925049 ) ) ;
#20810=DIRECTION ( 'NONE',  ( 0.000000000000000000, 0.000000000000000000, 1.000000000000000000 ) ) ;
#20818=EDGE_CURVE ( 'NONE', #68659, #57100, #71002, .T. ) ;
#20822=ORIENTED_EDGE ( 'NONE', *, *, #12449, .T. ) ;
#20830=AXIS2_PLACEMENT_3D ( 'NONE', #54661, #43021, #53183 ) ;
#20844=ORIENTED_EDGE ( 'NONE', *, *, #21305, .T. ) ;
#20850=LINE ( 'NONE', #49425, #23691 ) ;
#20858=CARTESIAN_POINT ( 'NONE',  ( -3.000000000000000000, -0.9646360437372163421, -23.52805723605591126 ) ) ;
#20872=DIRECTION ( 'NONE',  ( 1.000000000000000000, -0.000000000000000000, -0.000000000000000000 ) ) ;
#20875=AXIS2_PLACEMENT_3D ( 'NONE', #8318, #26704, #60577 ) ;
#20876=EDGE_CURVE ( 'NONE', #51690, #26546, #52081, .T. ) ;
#20891=AXIS2_PLACEMENT_3D ( 'NONE', #5808, #64420, #7276 ) ;
#20905=ORIENTED_EDGE ( 'NONE', *, *, #50739, .T. ) ;
#20906=LINE ( 'NONE', #61142, #44650 ) ;
#20918=VERTEX_POINT ( 'NONE', #53196 ) ;
#20966=ADVANCED_FACE ( 'NONE', ( #30616 ), #36636, .T. ) ;
#20969=CARTESIAN_POINT ( 'NONE',  ( -3.000000000000000000, 18.84667830672579925, 18.68964196561269020 ) ) ;
#20975=VERTEX_POINT ( 'NONE', #13336 ) ;
#20986=ORIENTED_EDGE ( 'NONE', *, *, #51546, .T. ) ;
#20987=FACE_OUTER_BOUND ( 'NONE', #61742, .T. ) ;
#20995=ORIENTED_EDGE ( 'NONE', *, *, #27237, .F. ) ;
#21012=CARTESIAN_POINT ( 'NONE',  ( 0.000000000000000000, 8.688484142253939169, 21.88630264137371029 ) ) ;
#21014=DIRECTION ( 'NONE',  ( -1.000000000000000000, 0.000000000000000000, 0.000000000000000000 ) ) ;
#21037=CIRCLE ( 'NONE', #46286, 16.00000000000000000 ) ;
#21062=EDGE_LOOP ( 'NONE', ( #59086, #7464, #64654, #33012 ) ) ;
#21066=CYLINDRICAL_SURFACE ( 'NONE', #20875, 37.49900000000000233 ) ;
#21068=VERTEX_POINT ( 'NONE', #44134 ) ;
#21073=VERTEX_POINT ( 'NONE', #27191 ) ;
#21083=EDGE_CURVE ( 'NONE', #10069, #10617, #32633, .T. ) ;
#21089=FACE_OUTER_BOUND ( 'NONE', #3886, .T. ) ;
#21104=DIRECTION ( 'NONE',  ( 0.000000000000000000, 0.000000000000000000, 1.000000000000000000 ) ) ;
#21139=EDGE_LOOP ( 'NONE', ( #10921, #10624, #46326, #65349 ) ) ;
#21140=CARTESIAN_POINT ( 'NONE',  ( 0.000000000000000000, -20.55727247249726020, -16.78983467731313084 ) ) ;
#21151=VERTEX_POINT ( 'NONE', #2670 ) ;
#21159=CARTESIAN_POINT ( 'NONE',  ( 10.00000000000000000, -32.34446384429951138, -26.79245525562750530 ) ) ;
#21167=DIRECTION ( 'NONE',  ( -1.000000000000000000, 0.000000000000000000, -0.000000000000000000 ) ) ;
#21185=CARTESIAN_POINT ( 'NONE',  ( -3.000000000000000000, -19.89357724625003598, 12.59942793731059574 ) ) ;
#21188=ORIENTED_EDGE ( 'NONE', *, *, #55423, .F. ) ;
#21189=ADVANCED_FACE ( 'NONE', ( #53390 ), #1559, .F. ) ;
#21204=DIRECTION ( 'NONE',  ( 0.000000000000000000, 0.000000000000000000, 1.000000000000000000 ) ) ;
#21209=CIRCLE ( 'NONE', #22461, 37.49900000000000233 ) ;
#21211=VECTOR ( 'NONE', #49961, 999.9999999999998863 ) ;
#21222=EDGE_CURVE ( 'NONE', #14321, #68714, #20626, .T. ) ;
#21231=FACE_OUTER_BOUND ( 'NONE', #41668, .T. ) ;
#21232=VERTEX_POINT ( 'NONE', #18791 ) ;
#21234=ORIENTED_EDGE ( 'NONE', *, *, #41073, .T. ) ;
#21258=DIRECTION ( 'NONE',  ( 0.000000000000000000, 0.000000000000000000, -1.000000000000000000 ) ) ;
#21264=CARTESIAN_POINT ( 'NONE',  ( 0.000000000000000000, 37.01155633439059756, 6.555932627142549762 ) ) ;
#21270=ORIENTED_EDGE ( 'NONE', *, *, #14105, .F. ) ;
#21272=DIRECTION ( 'NONE',  ( -1.000000000000000000, 0.000000000000000000, 0.000000000000000000 ) ) ;
#21305=EDGE_CURVE ( 'NONE', #5518, #37933, #47098, .T. ) ;
#21325=DIRECTION ( 'NONE',  ( -1.000000000000000000, 0.000000000000000000, 0.000000000000000000 ) ) ;
#21329=DIRECTION ( 'NONE',  ( 1.000000000000000000, -0.000000000000000000, -0.000000000000000000 ) ) ;
#21345=EDGE_LOOP ( 'NONE', ( #68643, #4860, #3806, #238 ) ) ;
#21353=DIRECTION ( 'NONE',  ( 0.000000000000000000, 0.000000000000000000, 1.000000000000000000 ) ) ;
#21384=EDGE_CURVE ( 'NONE', #30754, #33832, #32681, .T. ) ;
#21411=CARTESIAN_POINT ( 'NONE',  ( 0.000000000000000000, -23.29833615347104825, -3.418703333116803744 ) ) ;
#21425=ORIENTED_EDGE ( 'NONE', *, *, #44669, .T. ) ;
#21438=ORIENTED_EDGE ( 'NONE', *, *, #36388, .T. ) ;
#21462=CARTESIAN_POINT ( 'NONE',  ( 0.000000000000000000, 9.615535125378775305, 24.73947219025917121 ) ) ;
#21477=ADVANCED_FACE ( 'NONE', ( #30265 ), #11229, .F. ) ;
#21480=DIRECTION ( 'NONE',  ( -1.000000000000000000, -0.000000000000000000, 0.000000000000000000 ) ) ;
#21488=CARTESIAN_POINT ( 'NONE',  ( 10.00000000000000000, 17.80606268964540462, 33.00180498840053644 ) ) ;
#21500=DIRECTION ( 'NONE',  ( -1.000000000000000000, -0.000000000000000000, -0.000000000000000000 ) ) ;
#21515=CARTESIAN_POINT ( 'NONE',  ( -3.000000000000000000, -0.9646360437375307573, 23.52805723605590060 ) ) ;
#21520=ORIENTED_EDGE ( 'NONE', *, *, #68681, .T. ) ;
#21532=EDGE_LOOP ( 'NONE', ( #29760, #11813, #18571, #24869 ) ) ;
#21537=ORIENTED_EDGE ( 'NONE', *, *, #60997, .F. ) ;
#21552=ORIENTED_EDGE ( 'NONE', *, *, #46181, .T. ) ;
#21573=CARTESIAN_POINT ( 'NONE',  ( 10.00000000000000000, 0.000000000000000000, 0.000000000000000000 ) ) ;
#21574=DIRECTION ( 'NONE',  ( -1.000000000000000000, -0.000000000000000000, 0.000000000000000000 ) ) ;
#21580=VERTEX_POINT ( 'NONE', #18978 ) ;
#21585=DIRECTION ( 'NONE',  ( -1.000000000000000000, 0.000000000000000000, 0.000000000000000000 ) ) ;
#21586=DIRECTION ( 'NONE',  ( 0.000000000000000000, 0.000000000000000000, 1.000000000000000000 ) ) ;
#21628=ORIENTED_EDGE ( 'NONE', *, *, #38643, .F. ) ;
#21636=DIRECTION ( 'NONE',  ( -1.000000000000000000, 0.000000000000000000, -0.000000000000000000 ) ) ;
#21644=ORIENTED_EDGE ( 'NONE', *, *, #39108, .F. ) ;
#21654=DIRECTION ( 'NONE',  ( 1.000000000000000000, 0.000000000000000000, -0.000000000000000000 ) ) ;
#21656=FACE_OUTER_BOUND ( 'NONE', #69415, .T. ) ;
#21660=DIRECTION ( 'NONE',  ( 0.000000000000000000, 0.000000000000000000, 1.000000000000000000 ) ) ;
#21674=ORIENTED_EDGE ( 'NONE', *, *, #64527, .F. ) ;
#21676=FACE_BOUND ( 'NONE', #61839, .T. ) ;
#21687=DIRECTION ( 'NONE',  ( -1.000000000000000000, 0.000000000000000000, -0.000000000000000000 ) ) ;
#21689=EDGE_LOOP ( 'NONE', ( #65947, #8074, #11473, #48353 ) ) ;
#21698=CARTESIAN_POINT ( 'NONE',  ( 10.00000000000000178, 2.571758278209441661E-15, -21.00000000000000000 ) ) ;
#21700=ADVANCED_FACE ( 'NONE', ( #25383 ), #20478, .F. ) ;
#21707=ORIENTED_EDGE ( 'NONE', *, *, #2239, .F. ) ;
#21728=ORIENTED_EDGE ( 'NONE', *, *, #7880, .T. ) ;
#21729=CARTESIAN_POINT ( 'NONE',  ( 10.00000000000000000, -10.96151621346461447, -35.95386929396268272 ) ) ;
#21731=CARTESIAN_POINT ( 'NONE',  ( 0.000000000000000000, 6.762365576493643893, -25.66652317338391853 ) ) ;
#21766=DIRECTION ( 'NONE',  ( 1.000000000000000000, -0.000000000000000000, 0.000000000000000000 ) ) ;
#21774=CARTESIAN_POINT ( 'NONE',  ( 10.00000000000000000, -41.81611651403859042, -3.925862922256606602 ) ) ;
#21792=VECTOR ( 'NONE', #18425, 1000.000000000000000 ) ;
#21793=EDGE_CURVE ( 'NONE', #49620, #27381, #68196, .T. ) ;
#21798=EDGE_LOOP ( 'NONE', ( #73584, #20710, #50204, #70895 ) ) ;
#21847=DIRECTION ( 'NONE',  ( 0.000000000000000000, -0.9510565162951500895, -0.3090169943749583314 ) ) ;
#21850=MECHANICAL_DESIGN_GEOMETRIC_PRESENTATION_REPRESENTATION('',(#35052),#31397);
#21851=VECTOR ( 'NONE', #34518, 1000.000000000000000 ) ;
#21863=DIRECTION ( 'NONE',  ( -1.000000000000000000, 0.000000000000000000, 0.000000000000000000 ) ) ;
#21867=CARTESIAN_POINT ( 'NONE',  ( -3.000000000000000000, -10.45096189432344147, 21.10159698893426494 ) ) ;
#21892=EDGE_CURVE ( 'NONE', #24265, #19617, #53123, .T. ) ;
#21912=VERTEX_POINT ( 'NONE', #58770 ) ;
#21918=ORIENTED_EDGE ( 'NONE', *, *, #36572, .T. ) ;
#21928=FACE_OUTER_BOUND ( 'NONE', #29749, .T. ) ;
#21930=DIRECTION ( 'NONE',  ( -1.000000000000000000, 0.000000000000000000, 0.000000000000000000 ) ) ;
#21931=DIRECTION ( 'NONE',  ( 0.000000000000000000, 0.000000000000000000, 1.000000000000000000 ) ) ;
#21938=ORIENTED_EDGE ( 'NONE', *, *, #57746, .T. ) ;
#21956=LINE ( 'NONE', #33977, #48155 ) ;
#21957=CARTESIAN_POINT ( 'NONE',  ( 10.00000000000000000, 5.202137450156907761, -37.22597642581151689 ) ) ;
#21960=DIRECTION ( 'NONE',  ( 0.000000000000000000, 0.000000000000000000, 1.000000000000000000 ) ) ;
#21961=DIRECTION ( 'NONE',  ( -1.000000000000000000, 0.000000000000000000, -0.000000000000000000 ) ) ;
#21995=ADVANCED_FACE ( 'NONE', ( #23445 ), #41111, .T. ) ;
#22007=EDGE_LOOP ( 'NONE', ( #53301, #18046, #56551, #72572 ) ) ;
#22027=VECTOR ( 'NONE', #57033, 1000.000000000000000 ) ;
#22045=DIRECTION ( 'NONE',  ( 0.000000000000000000, 0.000000000000000000, 1.000000000000000000 ) ) ;
#22055=CARTESIAN_POINT ( 'NONE',  ( 10.00000000000000000, 0.000000000000000000, 0.000000000000000000 ) ) ;
#22057=ADVANCED_FACE ( 'NONE', ( #37688 ), #37322, .T. ) ;
#22071=EDGE_CURVE ( 'NONE', #59943, #24232, #20388, .T. ) ;
#22104=ORIENTED_EDGE ( 'NONE', *, *, #47855, .F. ) ;
#22119=VECTOR ( 'NONE', #18183, 1000.000000000000000 ) ;
#22120=LINE ( 'NONE', #28122, #8847 ) ;
#22121=DIRECTION ( 'NONE',  ( 0.000000000000000000, 0.000000000000000000, 1.000000000000000000 ) ) ;
#22124=CARTESIAN_POINT ( 'NONE',  ( 10.00000000000000000, 12.42422080174688404, -35.38097989696498047 ) ) ;
#22126=VECTOR ( 'NONE', #48174, 1000.000000000000000 ) ;
#22127=ORIENTED_EDGE ( 'NONE', *, *, #51883, .F. ) ;
#22139=CARTESIAN_POINT ( 'NONE',  ( 10.00000000000000000, -10.74501242461258244, -35.92658777277521409 ) ) ;
#22143=CARTESIAN_POINT ( 'NONE',  ( -3.000000000000000000, -18.13022148937243472, -15.02647892043568767 ) ) ;
#22167=EDGE_CURVE ( 'NONE', #74246, #8203, #36189, .T. ) ;
#22180=ORIENTED_EDGE ( 'NONE', *, *, #52963, .T. ) ;
#22184=ORIENTED_EDGE ( 'NONE', *, *, #56794, .T. ) ;
#22195=LINE ( 'NONE', #15816, #64155 ) ;
#22196=CARTESIAN_POINT ( 'NONE',  ( 0.000000000000000000, -30.80686688396994910, -21.53537804866113703 ) ) ;
#22210=VERTEX_POINT ( 'NONE', #28236 ) ;
#22213=CARTESIAN_POINT ( 'NONE',  ( -3.000000000000000000, -23.29833615347109443, 3.418703333116492438 ) ) ;
#22215=ORIENTED_EDGE ( 'NONE', *, *, #32917, .F. ) ;
#22221=VERTEX_POINT ( 'NONE', #56833 ) ;
#22231=ADVANCED_FACE ( 'NONE', ( #67356 ), #61358, .T. ) ;
#22265=LINE ( 'NONE', #55731, #54006 ) ;
#22283=VERTEX_POINT ( 'NONE', #50049 ) ;
#22285=ORIENTED_EDGE ( 'NONE', *, *, #35783, .F. ) ;
#22286=ORIENTED_EDGE ( 'NONE', *, *, #73058, .F. ) ;
#22290=ORIENTED_EDGE ( 'NONE', *, *, #7016, .T. ) ;
#22301=CARTESIAN_POINT ( 'NONE',  ( -10.00000000000000000, 0.000000000000000000, 0.000000000000000000 ) ) ;
#22311=VECTOR ( 'NONE', #62563, 1000.000000000000000 ) ;
#22313=CYLINDRICAL_SURFACE ( 'NONE', #11861, 16.00000000000000000 ) ;
#22333=CARTESIAN_POINT ( 'NONE',  ( 10.00000000000000000, -10.41901085202107247, 40.68715046381925049 ) ) ;
#22334=CARTESIAN_POINT ( 'NONE',  ( 0.000000000000000000, -35.92658777277517856, 10.74501242461269257 ) ) ;
#22338=CARTESIAN_POINT ( 'NONE',  ( 0.000000000000000000, 35.38097989696528600, -12.42422080174602605 ) ) ;
#22362=DIRECTION ( 'NONE',  ( -1.000000000000000000, -0.000000000000000000, -0.000000000000000000 ) ) ;
#22379=ORIENTED_EDGE ( 'NONE', *, *, #73675, .F. ) ;
#22383=LINE ( 'NONE', #38567, #58604 ) ;
#22401=AXIS2_PLACEMENT_3D ( 'NONE', #67343, #15843, #21847 ) ;
#22409=CARTESIAN_POINT ( 'NONE',  ( 10.00000000000000000, 26.79245525562714647, 32.34446384429980981 ) ) ;
#22414=VERTEX_POINT ( 'NONE', #17706 ) ;
#22434=LINE ( 'NONE', #17162, #73260 ) ;
#22441=CARTESIAN_POINT ( 'NONE',  ( -3.000000000000000000, -18.13022148937263012, 15.02647892043544608 ) ) ;
#22460=EDGE_LOOP ( 'NONE', ( #42544, #44278, #11476, #62710 ) ) ;
#22461=AXIS2_PLACEMENT_3D ( 'NONE', #52066, #44960, #68640 ) ;
#22465=VECTOR ( 'NONE', #42145, 1000.000000000000000 ) ;
#22471=ADVANCED_FACE ( 'NONE', ( #64320 ), #39914, .T. ) ;
#22472=VERTEX_POINT ( 'NONE', #62863 ) ;
#22473=VERTEX_POINT ( 'NONE', #58301 ) ;
#22480=ADVANCED_FACE ( 'NONE', ( #6796 ), #23358, .F. ) ;
#22510=FACE_OUTER_BOUND ( 'NONE', #18490, .T. ) ;
#22511=ORIENTED_EDGE ( 'NONE', *, *, #36681, .T. ) ;
#22525=CARTESIAN_POINT ( 'NONE',  ( 10.00000000000000000, -40.68715046381921496, -10.41901085202121457 ) ) ;
#22536=CARTESIAN_POINT ( 'NONE',  ( 4.999999999999999112, 9.188173127307898369, -40.98264845739739570 ) ) ;
#22544=DIRECTION ( 'NONE',  ( 0.000000000000000000, 0.000000000000000000, 1.000000000000000000 ) ) ;
#22546=DIRECTION ( 'NONE',  ( 0.000000000000000000, -0.3090169943749573878, 0.9510565162951503115 ) ) ;
#22563=EDGE_LOOP ( 'NONE', ( #72323, #17770, #6197, #82 ) ) ;
#22564=ORIENTED_EDGE ( 'NONE', *, *, #26743, .F. ) ;
#22583=ORIENTED_EDGE ( 'NONE', *, *, #30753, .T. ) ;
#22596=AXIS2_PLACEMENT_3D ( 'NONE', #71148, #65539, #14009 ) ;
#22598=DIRECTION ( 'NONE',  ( -1.000000000000000000, -0.000000000000000000, -0.000000000000000000 ) ) ;
#22608=FACE_OUTER_BOUND ( 'NONE', #17189, .T. ) ;
#22618=DIRECTION ( 'NONE',  ( 0.000000000000000000, 0.000000000000000000, 1.000000000000000000 ) ) ;
#22632=PLANE ( 'NONE',  #1780 ) ;
#22636=DIRECTION ( 'NONE',  ( 0.000000000000000000, -0.9510565162951500895, -0.3090169943749581649 ) ) ;
#22639=DIRECTION ( 'NONE',  ( -1.000000000000000000, 0.000000000000000000, 0.000000000000000000 ) ) ;
#22654=DIRECTION ( 'NONE',  ( -1.000000000000000000, -0.000000000000000000, 0.000000000000000000 ) ) ;
#22658=CARTESIAN_POINT ( 'NONE',  ( 10.00000000000000000, -31.52238457039580055, -27.75498641678775869 ) ) ;
#22670=EDGE_CURVE ( 'NONE', #11862, #69710, #53766, .T. ) ;
#22681=LINE ( 'NONE', #69275, #822 ) ;
#22692=DIRECTION ( 'NONE',  ( 0.000000000000000000, 0.000000000000000000, 1.000000000000000000 ) ) ;
#22708=AXIS2_PLACEMENT_3D ( 'NONE', #51566, #39930, #56481 ) ;
#22720=ADVANCED_FACE ( 'NONE', ( #27408 ), #27031, .T. ) ;
#22725=LINE ( 'NONE', #40009, #30490 ) ;
#22736=DIRECTION ( 'NONE',  ( -1.000000000000000000, 0.000000000000000000, -0.000000000000000000 ) ) ;
#22745=CARTESIAN_POINT ( 'NONE',  ( 10.00000000000000000, 21.32104025579158701, -30.84782396557194772 ) ) ;
#22761=DIRECTION ( 'NONE',  ( -1.000000000000000000, 0.000000000000000000, 0.000000000000000000 ) ) ;
#22762=ORIENTED_EDGE ( 'NONE', *, *, #51789, .F. ) ;
#22789=CIRCLE ( 'NONE', #73149, 37.49900000000000233 ) ;
#22800=ORIENTED_EDGE ( 'NONE', *, *, #32496, .F. ) ;
#22804=FACE_OUTER_BOUND ( 'NONE', #50111, .T. ) ;
#22810=CARTESIAN_POINT ( 'NONE',  ( 10.00000000000000000, 35.95386929396256903, -10.96151621346501237 ) ) ;
#22849=CARTESIAN_POINT ( 'NONE',  ( 0.000000000000000000, 16.83928648764945279, -16.46020748918028076 ) ) ;
#22855=CIRCLE ( 'NONE', #20426, 16.00000000000000000 ) ;
#22858=VECTOR ( 'NONE', #31264, 1000.000000000000114 ) ;
#22867=ORIENTED_EDGE ( 'NONE', *, *, #67586, .F. ) ;
#22872=ORIENTED_EDGE ( 'NONE', *, *, #48473, .T. ) ;
#22890=CARTESIAN_POINT ( 'NONE',  ( 10.00000000000000000, 30.00120703465205452, 22.64427369931179967 ) ) ;
#22913=DIRECTION ( 'NONE',  ( 1.000000000000000000, -0.000000000000000000, 0.000000000000000000 ) ) ;
#22914=EDGE_CURVE ( 'NONE', #63709, #58611, #71099, .T. ) ;
#22920=AXIS2_PLACEMENT_3D ( 'NONE', #48472, #32275, #54851 ) ;
#22921=EDGE_CURVE ( 'NONE', #47629, #26649, #34175, .T. ) ;
#22923=LINE ( 'NONE', #6008, #35653 ) ;
#22924=EDGE_CURVE ( 'NONE', #8777, #51805, #62725, .T. ) ;
#22929=EDGE_CURVE ( 'NONE', #25052, #3791, #41080, .T. ) ;
#22953=EDGE_CURVE ( 'NONE', #34118, #5113, #30274, .T. ) ;
#22960=ORIENTED_EDGE ( 'NONE', *, *, #69177, .T. ) ;
#22962=ORIENTED_EDGE ( 'NONE', *, *, #45634, .T. ) ;
#22964=DIRECTION ( 'NONE',  ( -1.000000000000000000, 0.000000000000000000, 0.000000000000000000 ) ) ;
#22980=VERTEX_POINT ( 'NONE', #69855 ) ;
#22987=CARTESIAN_POINT ( 'NONE',  ( 10.00000000000000000, -30.84782396557233142, 21.32104025579104345 ) ) ;
#23001=DIRECTION ( 'NONE',  ( 0.000000000000000000, 0.000000000000000000, 1.000000000000000000 ) ) ;
#23034=ORIENTED_EDGE ( 'NONE', *, *, #54518, .T. ) ;
#23048=VERTEX_POINT ( 'NONE', #24739 ) ;
#23051=CARTESIAN_POINT ( 'NONE',  ( 0.000000000000000000, 0.000000000000000000, 0.000000000000000000 ) ) ;
#23071=PLANE ( 'NONE',  #4305 ) ;
#23076=ORIENTED_EDGE ( 'NONE', *, *, #7962, .F. ) ;
#23085=DIRECTION ( 'NONE',  ( -1.000000000000000000, 0.000000000000000000, 0.000000000000000000 ) ) ;
#23111=VECTOR ( 'NONE', #21574, 1000.000000000000000 ) ;
#23117=DIRECTION ( 'NONE',  ( 1.000000000000000000, 0.000000000000000000, -0.000000000000000000 ) ) ;
#23121=DIRECTION ( 'NONE',  ( -0.000000000000000000, 0.8090169943749426773, 0.5877852522924797984 ) ) ;
#23128=ADVANCED_FACE ( 'NONE', ( #46429 ), #41527, .T. ) ;
#23136=VERTEX_POINT ( 'NONE', #47172 ) ;
#23144=DIRECTION ( 'NONE',  ( 0.000000000000000000, 0.9510565162951503115, 0.3090169943749573878 ) ) ;
#23155=DIRECTION ( 'NONE',  ( 0.000000000000000000, 0.1564344650402312298, -0.9876883405951375483 ) ) ;
#23162=DIRECTION ( 'NONE',  ( 0.000000000000000000, 0.000000000000000000, 1.000000000000000000 ) ) ;
#23164=ORIENTED_EDGE ( 'NONE', *, *, #46282, .F. ) ;
#23173=CARTESIAN_POINT ( 'NONE',  ( -10.00000000000000000, 0.000000000000000000, 0.000000000000000000 ) ) ;
#23196=VERTEX_POINT ( 'NONE', #68996 ) ;
#23210=DIRECTION ( 'NONE',  ( -1.000000000000000000, -0.000000000000000000, -0.000000000000000000 ) ) ;
#23211=EDGE_CURVE ( 'NONE', #40041, #19435, #63361, .T. ) ;
#23213=VECTOR ( 'NONE', #26887, 1000.000000000000000 ) ;
#23216=AXIS2_PLACEMENT_3D ( 'NONE', #59895, #48601, #31666 ) ;
#23234=DIRECTION ( 'NONE',  ( -0.000000000000000000, -0.9510565162951506446, -0.3090169943749562220 ) ) ;
#23242=DIRECTION ( 'NONE',  ( 1.000000000000000000, 0.000000000000000000, 0.000000000000000000 ) ) ;
#23250=ORIENTED_EDGE ( 'NONE', *, *, #14136, .F. ) ;
#23253=VERTEX_POINT ( 'NONE', #58082 ) ;
#23255=EDGE_LOOP ( 'NONE', ( #51693, #29095, #73116, #13034 ) ) ;
#23259=ORIENTED_EDGE ( 'NONE', *, *, #15615, .F. ) ;
#23262=CARTESIAN_POINT ( 'NONE',  ( 10.00000000000000000, 0.000000000000000000, 0.000000000000000000 ) ) ;
#23274=CARTESIAN_POINT ( 'NONE',  ( 10.00000000000000000, 0.000000000000000000, 0.000000000000000000 ) ) ;
#23277=CIRCLE ( 'NONE', #58035, 37.49900000000000233 ) ;
#23278=LINE ( 'NONE', #22536, #69694 ) ;
#23293=ADVANCED_FACE ( 'NONE', ( #48279 ), #19693, .F. ) ;
#23306=ORIENTED_EDGE ( 'NONE', *, *, #63152, .F. ) ;
#23308=CARTESIAN_POINT ( 'NONE',  ( 10.00000000000000000, -2.663952781845854378, -41.91543099594820632 ) ) ;
#23312=ORIENTED_EDGE ( 'NONE', *, *, #26210, .T. ) ;
#23319=CARTESIAN_POINT ( 'NONE',  ( 10.00000000000000000, -29.81001611431024756, 22.74946021919122785 ) ) ;
#23320=AXIS2_PLACEMENT_3D ( 'NONE', #38534, #73839, #27228 ) ;
#23327=EDGE_LOOP ( 'NONE', ( #33852, #43681, #66865, #19753 ) ) ;
#23328=ORIENTED_EDGE ( 'NONE', *, *, #50391, .F. ) ;
#23339=ORIENTED_EDGE ( 'NONE', *, *, #21793, .T. ) ;
#23349=ADVANCED_FACE ( 'NONE', ( #20062 ), #24972, .F. ) ;
#23351=DIRECTION ( 'NONE',  ( -1.000000000000000000, 0.000000000000000000, 0.000000000000000000 ) ) ;
#23358=PLANE ( 'NONE',  #5027 ) ;
#23359=CIRCLE ( 'NONE', #65369, 37.49900000000000233 ) ;
#23362=CARTESIAN_POINT ( 'NONE',  ( 10.00000000000000000, 0.000000000000000000, 0.000000000000000000 ) ) ;
#23365=CIRCLE ( 'NONE', #2986, 16.00000000000000711 ) ;
#23368=CARTESIAN_POINT ( 'NONE',  ( -3.000000000000000000, 26.50000000000000000, -1.500000000000001332 ) ) ;
#23374=VERTEX_POINT ( 'NONE', #22745 ) ;
#23382=DIRECTION ( 'NONE',  ( 0.000000000000000000, 0.3090169943749412340, 0.9510565162951556406 ) ) ;
#23387=CIRCLE ( 'NONE', #65357, 42.00000000000000000 ) ;
#23391=AXIS2_PLACEMENT_3D ( 'NONE', #40157, #73610, #22121 ) ;
#23393=ORIENTED_EDGE ( 'NONE', *, *, #15553, .T. ) ;
#23404=VERTEX_POINT ( 'NONE', #62605 ) ;
#23433=ADVANCED_FACE ( 'NONE', ( #68228 ), #11800, .F. ) ;
#23445=FACE_OUTER_BOUND ( 'NONE', #6546, .T. ) ;
#23446=DIRECTION ( 'NONE',  ( -1.000000000000000000, -0.000000000000000000, 0.000000000000000000 ) ) ;
#23451=DIRECTION ( 'NONE',  ( -1.000000000000000000, 0.000000000000000000, 0.000000000000000000 ) ) ;
#23458=EDGE_CURVE ( 'NONE', #63855, #60337, #24325, .T. ) ;
#23459=EDGE_CURVE ( 'NONE', #32352, #69078, #34377, .T. ) ;
#23478=VECTOR ( 'NONE', #72086, 1000.000000000000000 ) ;
#23483=ORIENTED_EDGE ( 'NONE', *, *, #34559, .T. ) ;
#23485=ORIENTED_EDGE ( 'NONE', *, *, #68003, .T. ) ;
#23495=CARTESIAN_POINT ( 'NONE',  ( 10.00000000000000000, -30.00120703465222149, 22.64427369931158296 ) ) ;
#23502=ORIENTED_EDGE ( 'NONE', *, *, #15971, .F. ) ;
#23518=CARTESIAN_POINT ( 'NONE',  ( 0.000000000000000000, 0.000000000000000000, 0.000000000000000000 ) ) ;
#23535=AXIS2_PLACEMENT_3D ( 'NONE', #51938, #483, #23382 ) ;
#23538=DIRECTION ( 'NONE',  ( 1.000000000000000000, -0.000000000000000000, 0.000000000000000000 ) ) ;
#23540=LINE ( 'NONE', #36663, #39745 ) ;
#23546=CIRCLE ( 'NONE', #59614, 42.00000000000000000 ) ;
#23561=PLANE ( 'NONE',  #33055 ) ;
#23568=LINE ( 'NONE', #63082, #8864 ) ;
#23578=CARTESIAN_POINT ( 'NONE',  ( 0.000000000000000000, 5.202137450156907761, -37.22597642581151689 ) ) ;
#23614=FACE_OUTER_BOUND ( 'NONE', #9813, .T. ) ;
#23633=DIRECTION ( 'NONE',  ( 0.000000000000000000, 0.000000000000000000, 1.000000000000000000 ) ) ;
#23643=VECTOR ( 'NONE', #24252, 1000.000000000000000 ) ;
#23644=LINE ( 'NONE', #6365, #69265 ) ;
#23650=DIRECTION ( 'NONE',  ( -1.000000000000000000, 0.000000000000000000, 0.000000000000000000 ) ) ;
#23653=ORIENTED_EDGE ( 'NONE', *, *, #20818, .F. ) ;
#23655=CIRCLE ( 'NONE', #70428, 37.49900000000000233 ) ;
#23656=ORIENTED_EDGE ( 'NONE', *, *, #2614, .F. ) ;
#23673=EDGE_CURVE ( 'NONE', #68825, #16929, #60455, .T. ) ;
#23684=VERTEX_POINT ( 'NONE', #72635 ) ;
#23685=DIRECTION ( 'NONE',  ( 1.000000000000000000, -0.000000000000000000, -0.000000000000000000 ) ) ;
#23691=VECTOR ( 'NONE', #66362, 1000.000000000000000 ) ;
#23696=ORIENTED_EDGE ( 'NONE', *, *, #48973, .T. ) ;
#23715=CARTESIAN_POINT ( 'NONE',  ( 10.00000000000000000, 35.92658777277511462, 10.74501242461295014 ) ) ;
#23719=VERTEX_POINT ( 'NONE', #21140 ) ;
#23721=DIRECTION ( 'NONE',  ( 0.000000000000000000, 0.9135454576426002005, 0.4067366430758017071 ) ) ;
#23748=EDGE_LOOP ( 'NONE', ( #48354, #51887, #35349, #14547 ) ) ;
#23756=VECTOR ( 'NONE', #46168, 1000.000000000000000 ) ;
#23766=AXIS2_PLACEMENT_3D ( 'NONE', #68120, #50449, #16611 ) ;
#23778=CARTESIAN_POINT ( 'NONE',  ( 10.00000000000000000, -5.202137450156129717, -37.22597642581163768 ) ) ;
#23796=DIRECTION ( 'NONE',  ( 0.000000000000000000, 0.9510565162951544194, -0.3090169943749447867 ) ) ;
#23800=EDGE_CURVE ( 'NONE', #69032, #14021, #31322, .T. ) ;
#23803=AXIS2_PLACEMENT_3D ( 'NONE', #31304, #37338, #55723 ) ;
#23816=FACE_OUTER_BOUND ( 'NONE', #14781, .T. ) ;
#23824=LINE ( 'NONE', #69685, #22119 ) ;
#23827=ADVANCED_FACE ( 'NONE', ( #56859 ), #11709, .F. ) ;
#23853=ORIENTED_EDGE ( 'NONE', *, *, #36572, .F. ) ;
#23861=ORIENTED_EDGE ( 'NONE', *, *, #68432, .T. ) ;
#23878=EDGE_CURVE ( 'NONE', #37933, #62989, #34563, .T. ) ;
#23881=EDGE_CURVE ( 'NONE', #69032, #68072, #7481, .T. ) ;
#23891=DIRECTION ( 'NONE',  ( -1.000000000000000000, 0.000000000000000000, 0.000000000000000000 ) ) ;
#23894=CARTESIAN_POINT ( 'NONE',  ( 10.00000000000000000, 30.84782396557248418, -21.32104025579081252 ) ) ;
#23915=PLANE ( 'NONE',  #6401 ) ;
#23916=FACE_OUTER_BOUND ( 'NONE', #47648, .T. ) ;
#23921=VECTOR ( 'NONE', #54487, 1000.000000000000000 ) ;
#23941=ORIENTED_EDGE ( 'NONE', *, *, #23878, .F. ) ;
#23945=LINE ( 'NONE', #29935, #28073 ) ;
#23962=AXIS2_PLACEMENT_3D ( 'NONE', #70416, #53518, #6283 ) ;
#23971=ADVANCED_FACE ( 'NONE', ( #2622 ), #25503, .T. ) ;
#23991=EDGE_LOOP ( 'NONE', ( #72285, #72734, #57510, #39519 ) ) ;
#23998=DIRECTION ( 'NONE',  ( -1.000000000000000000, -0.000000000000000000, -0.000000000000000000 ) ) ;
#24002=DIRECTION ( 'NONE',  ( -1.000000000000000000, -0.000000000000000000, 0.000000000000000000 ) ) ;
#24009=CARTESIAN_POINT ( 'NONE',  ( 5.000000000000000000, -38.55633173626998911, -16.65560815589452304 ) ) ;
#24012=EDGE_CURVE ( 'NONE', #11350, #51481, #47195, .T. ) ;
#24044=EDGE_CURVE ( 'NONE', #40343, #26594, #8819, .T. ) ;
#24073=VERTEX_POINT ( 'NONE', #20969 ) ;
#24089=EDGE_LOOP ( 'NONE', ( #14428, #23312, #32716, #20543 ) ) ;
#24104=ORIENTED_EDGE ( 'NONE', *, *, #42778, .F. ) ;
#24105=DIRECTION ( 'NONE',  ( 0.000000000000000000, -0.7071067811865536790, 0.7071067811865414665 ) ) ;
#24109=CYLINDRICAL_SURFACE ( 'NONE', #26219, 37.49900000000000233 ) ;
#24127=VERTEX_POINT ( 'NONE', #51031 ) ;
#24141=EDGE_CURVE ( 'NONE', #31995, #40041, #16078, .T. ) ;
#24143=VECTOR ( 'NONE', #6417, 1000.000000000000000 ) ;
#24144=EDGE_LOOP ( 'NONE', ( #1555, #41415, #22511, #17213 ) ) ;
#24148=CARTESIAN_POINT ( 'NONE',  ( 0.000000000000000000, 16.83928648764923253, 16.46020748918050458 ) ) ;
#24195=VECTOR ( 'NONE', #10294, 1000.000000000000114 ) ;
#24201=DIRECTION ( 'NONE',  ( 0.000000000000000000, 0.4539904997395479702, -0.8910065241883673437 ) ) ;
#24209=DIRECTION ( 'NONE',  ( -1.000000000000000000, -0.000000000000000000, -0.000000000000000000 ) ) ;
#24221=CYLINDRICAL_SURFACE ( 'NONE', #71512, 16.00000000000000000 ) ;
#24222=ORIENTED_EDGE ( 'NONE', *, *, #25117, .T. ) ;
#24224=VERTEX_POINT ( 'NONE', #58153 ) ;
#24232=VERTEX_POINT ( 'NONE', #6652 ) ;
#24235=ORIENTED_EDGE ( 'NONE', *, *, #68418, .F. ) ;
#24241=VERTEX_POINT ( 'NONE', #68710 ) ;
#24252=DIRECTION ( 'NONE',  ( -1.000000000000000000, 0.000000000000000000, -0.000000000000000000 ) ) ;
#24265=VERTEX_POINT ( 'NONE', #17195 ) ;
#24273=EDGE_CURVE ( 'NONE', #15802, #45606, #23568, .T. ) ;
#24279=VECTOR ( 'NONE', #49581, 1000.000000000000000 ) ;
#24304=EDGE_CURVE ( 'NONE', #52685, #9960, #23945, .T. ) ;
#24305=ORIENTED_EDGE ( 'NONE', *, *, #62118, .F. ) ;
#24325=CIRCLE ( 'NONE', #18360, 37.49900000000000233 ) ;
#24331=EDGE_LOOP ( 'NONE', ( #37690, #26350, #39992, #2367 ) ) ;
#24351=ORIENTED_EDGE ( 'NONE', *, *, #31196, .T. ) ;
#24353=CARTESIAN_POINT ( 'NONE',  ( -10.00000000000000000, 0.000000000000000000, 0.000000000000000000 ) ) ;
#24354=EDGE_CURVE ( 'NONE', #51153, #15251, #54475, .T. ) ;
#24359=ORIENTED_EDGE ( 'NONE', *, *, #25330, .F. ) ;
#24361=ORIENTED_EDGE ( 'NONE', *, *, #34472, .F. ) ;
#24365=CARTESIAN_POINT ( 'NONE',  ( 10.00000000000000000, -33.80338159004273280, -16.23288003029533044 ) ) ;
#24381=DIRECTION ( 'NONE',  ( -1.000000000000000000, 0.000000000000000000, 0.000000000000000000 ) ) ;
#24387=AXIS2_PLACEMENT_3D ( 'NONE', #24924, #53504, #2038 ) ;
#24403=ORIENTED_EDGE ( 'NONE', *, *, #37301, .F. ) ;
#24424=DIRECTION ( 'NONE',  ( -0.000000000000000000, -0.9945218953682741780, 0.1045284632676447834 ) ) ;
#24425=ORIENTED_EDGE ( 'NONE', *, *, #55067, .T. ) ;
#24448=CYLINDRICAL_SURFACE ( 'NONE', #69218, 37.49900000000000233 ) ;
#24454=LINE ( 'NONE', #13537, #44746 ) ;
#24462=EDGE_CURVE ( 'NONE', #16859, #67669, #27640, .T. ) ;
#24478=DIRECTION ( 'NONE',  ( -1.000000000000000000, -0.000000000000000000, -0.000000000000000000 ) ) ;
#24491=AXIS2_PLACEMENT_3D ( 'NONE', #69682, #70037, #24201 ) ;
#24496=ORIENTED_EDGE ( 'NONE', *, *, #69686, .F. ) ;
#24502=ORIENTED_EDGE ( 'NONE', *, *, #5951, .T. ) ;
#24516=CARTESIAN_POINT ( 'NONE',  ( 0.000000000000000000, 0.000000000000000000, 0.000000000000000000 ) ) ;
#24518=CARTESIAN_POINT ( 'NONE',  ( -3.000000000000000000, 22.07842321921492612, -8.187992925817130896 ) ) ;
#24523=EDGE_LOOP ( 'NONE', ( #32977, #30492, #25615, #35817 ) ) ;
#24524=CIRCLE ( 'NONE', #31698, 15.99999999999999822 ) ;
#24528=CARTESIAN_POINT ( 'NONE',  ( 0.000000000000000000, 22.64427369931169309, 30.00120703465213623 ) ) ;
#24529=DIRECTION ( 'NONE',  ( 1.000000000000000000, -0.000000000000000000, 0.000000000000000000 ) ) ;
#24538=ORIENTED_EDGE ( 'NONE', *, *, #6450, .F. ) ;
#24539=CIRCLE ( 'NONE', #31768, 16.00000000000000000 ) ;
#24550=ORIENTED_EDGE ( 'NONE', *, *, #56694, .F. ) ;
#24554=EDGE_CURVE ( 'NONE', #66848, #27381, #10044, .T. ) ;
#24559=CARTESIAN_POINT ( 'NONE',  ( 4.999999999999999112, 10.41901085202078292, 40.68715046381932865 ) ) ;
#24574=DIRECTION ( 'NONE',  ( -1.000000000000000000, -0.000000000000000000, 0.000000000000000000 ) ) ;
#24582=CARTESIAN_POINT ( 'NONE',  ( -3.000000000000000000, -19.89357724624987256, -12.59942793731086041 ) ) ;
#24586=EDGE_LOOP ( 'NONE', ( #23696, #61957, #65387, #18397 ) ) ;
#24593=VECTOR ( 'NONE', #65121, 999.9999999999998863 ) ;
#24602=EDGE_CURVE ( 'NONE', #18738, #11035, #30498, .T. ) ;
#24619=LINE ( 'NONE', #42298, #73200 ) ;
#24626=ORIENTED_EDGE ( 'NONE', *, *, #12719, .T. ) ;
#24644=CYLINDRICAL_SURFACE ( 'NONE', #70471, 16.00000000000000000 ) ;
#24650=CARTESIAN_POINT ( 'NONE',  ( 10.00000000000000000, -26.08949754953005495, -27.05870788708258701 ) ) ;
#24651=AXIS2_PLACEMENT_3D ( 'NONE', #21515, #4257, #72281 ) ;
#24668=CARTESIAN_POINT ( 'NONE',  ( -3.000000000000000000, -22.32062822937469804, -14.36278369418829826 ) ) ;
#24679=DIRECTION ( 'NONE',  ( 1.000000000000000000, 0.000000000000000000, 0.000000000000000000 ) ) ;
#24684=ORIENTED_EDGE ( 'NONE', *, *, #55586, .T. ) ;
#24685=VERTEX_POINT ( 'NONE', #1979 ) ;
#24695=ORIENTED_EDGE ( 'NONE', *, *, #19018, .T. ) ;
#24706=DIRECTION ( 'NONE',  ( 1.000000000000000000, 0.000000000000000000, -0.000000000000000000 ) ) ;
#24719=ADVANCED_FACE ( 'NONE', ( #3811 ), #21066, .T. ) ;
#24720=CARTESIAN_POINT ( 'NONE',  ( 10.00000000000000000, 0.000000000000000000, 0.000000000000000000 ) ) ;
#24724=ORIENTED_EDGE ( 'NONE', *, *, #41231, .F. ) ;
#24725=LINE ( 'NONE', #25467, #57330 ) ;
#24739=CARTESIAN_POINT ( 'NONE',  ( 10.00000000000000000, 33.00180498840046539, 17.80606268964551120 ) ) ;
#24745=DIRECTION ( 'NONE',  ( 1.000000000000000000, -0.000000000000000000, -0.000000000000000000 ) ) ;
#24746=ORIENTED_EDGE ( 'NONE', *, *, #19786, .F. ) ;
#24755=VERTEX_POINT ( 'NONE', #66933 ) ;
#24760=DIRECTION ( 'NONE',  ( -1.000000000000000000, 0.000000000000000000, -0.000000000000000000 ) ) ;
#24764=AXIS2_PLACEMENT_3D ( 'NONE', #71769, #72148, #48487 ) ;
#24766=VERTEX_POINT ( 'NONE', #66581 ) ;
#24774=AXIS2_PLACEMENT_3D ( 'NONE', #32232, #19481, #2974 ) ;
#24777=DIRECTION ( 'NONE',  ( -1.000000000000000000, -0.000000000000000000, -0.000000000000000000 ) ) ;
#24790=PRESENTATION_STYLE_ASSIGNMENT (( #12762 ) ) ;
#24816=DIRECTION ( 'NONE',  ( -1.000000000000000000, -0.000000000000000000, 0.000000000000000000 ) ) ;
#24823=LINE ( 'NONE', #19907, #65624 ) ;
#24869=ORIENTED_EDGE ( 'NONE', *, *, #33916, .F. ) ;
#24880=CYLINDRICAL_SURFACE ( 'NONE', #32828, 16.00000000000000000 ) ;
#24883=CIRCLE ( 'NONE', #6854, 42.00000000000000000 ) ;
#24884=DIRECTION ( 'NONE',  ( 0.000000000000000000, 0.000000000000000000, 1.000000000000000000 ) ) ;
#24887=DIRECTION ( 'NONE',  ( 1.000000000000000000, -0.000000000000000000, -0.000000000000000000 ) ) ;
#24899=CARTESIAN_POINT ( 'NONE',  ( -3.000000000000000000, 9.615535125378775305, 24.73947219025917121 ) ) ;
#24902=FACE_OUTER_BOUND ( 'NONE', #51950, .T. ) ;
#24903=CARTESIAN_POINT ( 'NONE',  ( 10.00000000000000000, 35.92658777277525672, -10.74501242461245809 ) ) ;
#24924=CARTESIAN_POINT ( 'NONE',  ( 10.00000000000000000, -22.64427369931148348, -30.00120703465229965 ) ) ;
#24935=DIRECTION ( 'NONE',  ( 0.000000000000000000, 0.8910065241883688980, -0.4539904997395445840 ) ) ;
#24936=EDGE_CURVE ( 'NONE', #66201, #61596, #22195, .T. ) ;
#24938=ADVANCED_FACE ( 'NONE', ( #27828 ), #40228, .T. ) ;
#24949=DIRECTION ( 'NONE',  ( -1.000000000000000000, 0.000000000000000000, 0.000000000000000000 ) ) ;
#24972=PLANE ( 'NONE',  #67576 ) ;
#24973=CARTESIAN_POINT ( 'NONE',  ( 0.000000000000000000, -15.48615015657556171, -39.04073710021360455 ) ) ;
#24978=CARTESIAN_POINT ( 'NONE',  ( 10.00000000000000000, 0.000000000000000000, 0.000000000000000000 ) ) ;
#24986=DIRECTION ( 'NONE',  ( -1.000000000000000000, 0.000000000000000000, 0.000000000000000000 ) ) ;
#24994=AXIS2_PLACEMENT_3D ( 'NONE', #55100, #25789, #72012 ) ;
#25008=CARTESIAN_POINT ( 'NONE',  ( 4.999999999999999112, -36.13751322684434797, 21.40280677340357940 ) ) ;
#25027=CIRCLE ( 'NONE', #45448, 42.00000000000000000 ) ;
#25052=VERTEX_POINT ( 'NONE', #7495 ) ;
#25055=ORIENTED_EDGE ( 'NONE', *, *, #20876, .T. ) ;
#25057=EDGE_CURVE ( 'NONE', #766, #35203, #6752, .T. ) ;
#25074=CIRCLE ( 'NONE', #35911, 16.00000000000000000 ) ;
#25085=VECTOR ( 'NONE', #36120, 1000.000000000000000 ) ;
#25087=DIRECTION ( 'NONE',  ( -1.000000000000000000, -0.000000000000000000, 0.000000000000000000 ) ) ;
#25092=EDGE_LOOP ( 'NONE', ( #69164, #61586, #799, #33665 ) ) ;
#25098=AXIS2_PLACEMENT_3D ( 'NONE', #62056, #10920, #69180 ) ;
#25102=CARTESIAN_POINT ( 'NONE',  ( 0.000000000000000000, 15.48615015657637883, -39.04073710021327770 ) ) ;
#25117=EDGE_CURVE ( 'NONE', #20003, #3283, #585, .T. ) ;
#25128=CARTESIAN_POINT ( 'NONE',  ( 10.00000000000000000, 0.000000000000000000, 0.000000000000000000 ) ) ;
#25130=CIRCLE ( 'NONE', #19109, 16.00000000000000000 ) ;
#25140=ORIENTED_EDGE ( 'NONE', *, *, #52782, .F. ) ;
#25152=EDGE_CURVE ( 'NONE', #39781, #70065, #23365, .T. ) ;
#25157=ORIENTED_EDGE ( 'NONE', *, *, #48042, .F. ) ;
#25208=AXIS2_PLACEMENT_3D ( 'NONE', #1855, #46568, #19464 ) ;
#25214=DIRECTION ( 'NONE',  ( -1.000000000000000000, -0.000000000000000000, -0.000000000000000000 ) ) ;
#25215=EDGE_CURVE ( 'NONE', #67909, #22221, #59363, .T. ) ;
#25216=FACE_OUTER_BOUND ( 'NONE', #34801, .T. ) ;
#25235=EDGE_CURVE ( 'NONE', #63232, #53287, #14975, .T. ) ;
#25257=ORIENTED_EDGE ( 'NONE', *, *, #45355, .T. ) ;
#25261=AXIS2_PLACEMENT_3D ( 'NONE', #19888, #1546, #36811 ) ;
#25263=DIRECTION ( 'NONE',  ( 1.000000000000000000, 0.000000000000000000, 0.000000000000000000 ) ) ;
#25287=EDGE_LOOP ( 'NONE', ( #61846, #22872, #35671, #42833 ) ) ;
#25289=EDGE_CURVE ( 'NONE', #43284, #70987, #24539, .T. ) ;
#25295=CARTESIAN_POINT ( 'NONE',  ( 10.00000000000000000, 21.53537804866126137, -30.80686688396986028 ) ) ;
#25330=EDGE_CURVE ( 'NONE', #67207, #33925, #39401, .T. ) ;
#25347=ORIENTED_EDGE ( 'NONE', *, *, #45618, .F. ) ;
#25372=DIRECTION ( 'NONE',  ( 0.000000000000000000, -0.5877852522924624790, -0.8090169943749552228 ) ) ;
#25377=AXIS2_PLACEMENT_3D ( 'NONE', #41633, #64571, #52173 ) ;
#25378=ORIENTED_EDGE ( 'NONE', *, *, #72649, .F. ) ;
#25382=CARTESIAN_POINT ( 'NONE',  ( -3.000000000000000000, -1.278221433540502217, 26.51162292216071847 ) ) ;
#25383=FACE_OUTER_BOUND ( 'NONE', #34417, .T. ) ;
#25388=ADVANCED_FACE ( 'NONE', ( #45045 ), #32998, .F. ) ;
#25402=VERTEX_POINT ( 'NONE', #63095 ) ;
#25417=CIRCLE ( 'NONE', #38628, 16.00000000000000000 ) ;
#25451=DIRECTION ( 'NONE',  ( 0.000000000000000000, 0.000000000000000000, 1.000000000000000000 ) ) ;
#25456=EDGE_CURVE ( 'NONE', #51709, #39121, #11925, .T. ) ;
#25466=ORIENTED_EDGE ( 'NONE', *, *, #39404, .F. ) ;
#25467=CARTESIAN_POINT ( 'NONE',  ( 10.00000000000000000, 4.992566952384984269, 37.16516213103279398 ) ) ;
#25473=CARTESIAN_POINT ( 'NONE',  ( -3.000000000000000000, 6.762365576493643893, -25.66652317338391853 ) ) ;
#25490=CARTESIAN_POINT ( 'NONE',  ( -3.000000000000000000, -10.45096189432344147, 21.10159698893426494 ) ) ;
#25499=ORIENTED_EDGE ( 'NONE', *, *, #46860, .T. ) ;
#25503=CYLINDRICAL_SURFACE ( 'NONE', #49587, 42.00000000000000000 ) ;
#25504=ORIENTED_EDGE ( 'NONE', *, *, #58392, .F. ) ;
#25506=ORIENTED_EDGE ( 'NONE', *, *, #1737, .F. ) ;
#25515=DIRECTION ( 'NONE',  ( 0.000000000000000000, -0.3090169943749349057, -0.9510565162951577500 ) ) ;
#25520=DIRECTION ( 'NONE',  ( 0.000000000000000000, 0.000000000000000000, 1.000000000000000000 ) ) ;
#25578=ORIENTED_EDGE ( 'NONE', *, *, #34830, .T. ) ;
#25586=ORIENTED_EDGE ( 'NONE', *, *, #6333, .F. ) ;
#25590=VERTEX_POINT ( 'NONE', #43111 ) ;
#25615=ORIENTED_EDGE ( 'NONE', *, *, #6771, .T. ) ;
#25622=ORIENTED_EDGE ( 'NONE', *, *, #26207, .T. ) ;
#25626=ADVANCED_FACE ( 'NONE', ( #37088 ), #2556, .F. ) ;
#25659=CIRCLE ( 'NONE', #35271, 42.00000000000000000 ) ;
#25661=DIRECTION ( 'NONE',  ( -1.000000000000000000, -0.000000000000000000, 0.000000000000000000 ) ) ;
#25686=ORIENTED_EDGE ( 'NONE', *, *, #57295, .T. ) ;
#25687=DIRECTION ( 'NONE',  ( -1.000000000000000000, 0.000000000000000000, 0.000000000000000000 ) ) ;
#25690=CARTESIAN_POINT ( 'NONE',  ( 0.000000000000000000, -35.38097989696520074, 12.42422080174625520 ) ) ;
#25692=ORIENTED_EDGE ( 'NONE', *, *, #24141, .F. ) ;
#25693=EDGE_CURVE ( 'NONE', #24127, #55748, #13771, .T. ) ;
#25740=EDGE_CURVE ( 'NONE', #11281, #58611, #16214, .T. ) ;
#25749=ORIENTED_EDGE ( 'NONE', *, *, #19287, .T. ) ;
#25751=DIRECTION ( 'NONE',  ( -1.000000000000000000, -0.000000000000000000, 0.000000000000000000 ) ) ;
#25753=DIRECTION ( 'NONE',  ( -1.000000000000000000, 0.000000000000000000, -0.000000000000000000 ) ) ;
#25756=CARTESIAN_POINT ( 'NONE',  ( 0.000000000000000000, -38.55633173627022359, 16.65560815589396526 ) ) ;
#25765=DIRECTION ( 'NONE',  ( 0.000000000000000000, 0.000000000000000000, 1.000000000000000000 ) ) ;
#25774=AXIS2_PLACEMENT_3D ( 'NONE', #3785, #27424, #33434 ) ;
#25775=AXIS2_PLACEMENT_3D ( 'NONE', #26450, #15544, #20810 ) ;
#25778=DIRECTION ( 'NONE',  ( 1.000000000000000000, 0.000000000000000000, -0.000000000000000000 ) ) ;
#25779=EDGE_CURVE ( 'NONE', #67855, #11835, #36599, .T. ) ;
#25789=DIRECTION ( 'NONE',  ( -1.000000000000000000, 0.000000000000000000, 0.000000000000000000 ) ) ;
#25792=ADVANCED_FACE ( 'NONE', ( #49834 ), #5117, .T. ) ;
#25795=ORIENTED_EDGE ( 'NONE', *, *, #42799, .F. ) ;
#25799=DIRECTION ( 'NONE',  ( 0.000000000000000000, 0.000000000000000000, -1.000000000000000000 ) ) ;
#25831=VECTOR ( 'NONE', #24424, 1000.000000000000114 ) ;
#25842=CARTESIAN_POINT ( 'NONE',  ( -10.00000000000000000, 0.000000000000000000, 0.000000000000000000 ) ) ;
#25843=DIRECTION ( 'NONE',  ( 0.000000000000000000, 0.000000000000000000, 1.000000000000000000 ) ) ;
#25860=ADVANCED_FACE ( 'NONE', ( #67883 ), #15639, .F. ) ;
#25879=CARTESIAN_POINT ( 'NONE',  ( -3.000000000000000000, -0.9646360437375307573, 23.52805723605590060 ) ) ;
#25907=DIRECTION ( 'NONE',  ( -1.000000000000000000, -0.000000000000000000, 0.000000000000000000 ) ) ;
#25927=DIRECTION ( 'NONE',  ( -1.000000000000000000, 0.000000000000000000, -0.000000000000000000 ) ) ;
#25933=CARTESIAN_POINT ( 'NONE',  ( -3.000000000000000000, -19.89357724625003598, 12.59942793731059574 ) ) ;
#25935=FACE_OUTER_BOUND ( 'NONE', #1786, .T. ) ;
#25938=AXIS2_PLACEMENT_3D ( 'NONE', #6462, #63975, #52680 ) ;
#25941=CARTESIAN_POINT ( 'NONE',  ( -3.000000000000000000, -13.04903810567675038, 19.60159698893425428 ) ) ;
#25944=VECTOR ( 'NONE', #31553, 1000.000000000000000 ) ;
#25953=AXIS2_PLACEMENT_3D ( 'NONE', #18828, #64714, #13196 ) ;
#25958=DIRECTION ( 'NONE',  ( 0.000000000000000000, 0.000000000000000000, -1.000000000000000000 ) ) ;
#25970=CARTESIAN_POINT ( 'NONE',  ( 0.000000000000000000, 17.80606268964540106, 33.00180498840052934 ) ) ;
#25976=DIRECTION ( 'NONE',  ( 1.000000000000000000, 0.000000000000000000, 0.000000000000000000 ) ) ;
#25984=LINE ( 'NONE', #7596, #65270 ) ;
#25989=EDGE_LOOP ( 'NONE', ( #71181, #44969, #53087, #59662 ) ) ;
#26005=DIRECTION ( 'NONE',  ( -0.000000000000000000, 0.9510565162951539753, -0.3090169943749460635 ) ) ;
#26024=CARTESIAN_POINT ( 'NONE',  ( 10.00000000000000000, -6.555932627142676772, 37.01155633439056203 ) ) ;
#26037=CARTESIAN_POINT ( 'NONE',  ( 0.000000000000000000, -13.04903810567675038, 19.60159698893425428 ) ) ;
#26040=EDGE_CURVE ( 'NONE', #7975, #23684, #45103, .T. ) ;
#26072=EDGE_LOOP ( 'NONE', ( #67258, #45221, #34382, #21918 ) ) ;
#26090=CARTESIAN_POINT ( 'NONE',  ( 0.000000000000000000, -21.32104025579135964, 30.84782396557210760 ) ) ;
#26094=CARTESIAN_POINT ( 'NONE',  ( 0.000000000000000000, -3.948201729842038432, -23.21447184625298021 ) ) ;
#26096=DIRECTION ( 'NONE',  ( -1.000000000000000000, 0.000000000000000000, -0.000000000000000000 ) ) ;
#26102=LINE ( 'NONE', #9188, #30921 ) ;
#26105=CARTESIAN_POINT ( 'NONE',  ( 0.000000000000000000, 16.83928648764945279, -16.46020748918028076 ) ) ;
#26109=EDGE_CURVE ( 'NONE', #52121, #16273, #52279, .T. ) ;
#26112=AXIS2_PLACEMENT_3D ( 'NONE', #50654, #61952, #11542 ) ;
#26119=DIRECTION ( 'NONE',  ( 0.000000000000000000, 0.4999999999999929501, 0.8660254037844427044 ) ) ;
#26122=DIRECTION ( 'NONE',  ( 0.000000000000000000, -0.9781476007338070211, 0.2079116908177525425 ) ) ;
#26131=EDGE_LOOP ( 'NONE', ( #69269, #14037, #9135, #58446 ) ) ;
#26149=ADVANCED_FACE ( 'NONE', ( #65583 ), #36998, .F. ) ;
#26153=ORIENTED_EDGE ( 'NONE', *, *, #7795, .T. ) ;
#26156=DIRECTION ( 'NONE',  ( -1.000000000000000000, 0.000000000000000000, -0.000000000000000000 ) ) ;
#26165=VECTOR ( 'NONE', #19277, 1000.000000000000000 ) ;
#26172=AXIS2_PLACEMENT_3D ( 'NONE', #59433, #12083, #19202 ) ;
#26181=CYLINDRICAL_SURFACE ( 'NONE', #32685, 16.00000000000000000 ) ;
#26201=DIRECTION ( 'NONE',  ( -1.000000000000000000, 0.000000000000000000, 0.000000000000000000 ) ) ;
#26205=DIRECTION ( 'NONE',  ( 0.000000000000000000, 0.8910065241883688980, -0.4539904997395447506 ) ) ;
#26207=EDGE_CURVE ( 'NONE', #17536, #66848, #46277, .T. ) ;
#26209=CARTESIAN_POINT ( 'NONE',  ( 0.000000000000000000, -29.81001611431024045, 22.74946021919122430 ) ) ;
#26210=EDGE_CURVE ( 'NONE', #60556, #30694, #15168, .T. ) ;
#26219=AXIS2_PLACEMENT_3D ( 'NONE', #36473, #64326, #13177 ) ;
#26225=ADVANCED_FACE ( 'NONE', ( #61792 ), #45245, .T. ) ;
#26227=DIRECTION ( 'NONE',  ( 0.000000000000000000, 0.000000000000000000, 1.000000000000000000 ) ) ;
#26243=DIRECTION ( 'NONE',  ( 0.000000000000000000, -0.9781476007338040235, -0.2079116908177671419 ) ) ;
#26245=CARTESIAN_POINT ( 'NONE',  ( 10.00000000000000000, 10.74501242461333028, -35.92658777277499382 ) ) ;
#26252=CARTESIAN_POINT ( 'NONE',  ( 10.00000000000000000, 0.000000000000000000, 0.000000000000000000 ) ) ;
#26267=ORIENTED_EDGE ( 'NONE', *, *, #12038, .F. ) ;
#26272=DIRECTION ( 'NONE',  ( -1.000000000000000000, -0.000000000000000000, -0.000000000000000000 ) ) ;
#26279=ORIENTED_EDGE ( 'NONE', *, *, #69758, .F. ) ;
#26292=ADVANCED_FACE ( 'NONE', ( #38850 ), #39600, .T. ) ;
#26298=CARTESIAN_POINT ( 'NONE',  ( 0.000000000000000000, 18.84667830672579925, 18.68964196561269020 ) ) ;
#26314=ORIENTED_EDGE ( 'NONE', *, *, #23881, .F. ) ;
#26316=ADVANCED_FACE ( 'NONE', ( #27563 ), #67795, .T. ) ;
#26328=DIRECTION ( 'NONE',  ( -1.000000000000000000, 0.000000000000000000, -0.000000000000000000 ) ) ;
#26331=VERTEX_POINT ( 'NONE', #51976 ) ;
#26335=ORIENTED_EDGE ( 'NONE', *, *, #58978, .F. ) ;
#26343=VERTEX_POINT ( 'NONE', #12854 ) ;
#26350=ORIENTED_EDGE ( 'NONE', *, *, #66313, .T. ) ;
#26376=AXIS2_PLACEMENT_3D ( 'NONE', #16029, #68287, #10764 ) ;
#26380=CARTESIAN_POINT ( 'NONE',  ( 10.00000000000000000, 27.75498641678786527, -31.52238457039571173 ) ) ;
#26398=DIRECTION ( 'NONE',  ( -1.000000000000000000, 0.000000000000000000, 0.000000000000000000 ) ) ;
#26413=AXIS2_PLACEMENT_3D ( 'NONE', #53125, #64047, #40739 ) ;
#26415=EDGE_CURVE ( 'NONE', #8512, #8585, #22681, .T. ) ;
#26422=ORIENTED_EDGE ( 'NONE', *, *, #19362, .T. ) ;
#26430=CIRCLE ( 'NONE', #48017, 16.00000000000000000 ) ;
#26434=ORIENTED_EDGE ( 'NONE', *, *, #1687, .T. ) ;
#26446=ORIENTED_EDGE ( 'NONE', *, *, #59343, .T. ) ;
#26450=CARTESIAN_POINT ( 'NONE',  ( 10.00000000000000000, 0.000000000000000000, 0.000000000000000000 ) ) ;
#26461=ORIENTED_EDGE ( 'NONE', *, *, #23459, .F. ) ;
#26465=LINE ( 'NONE', #62172, #51578 ) ;
#26491=CARTESIAN_POINT ( 'NONE',  ( -3.000000000000000000, 14.60985201121729737, -18.46759930825687945 ) ) ;
#26497=CARTESIAN_POINT ( 'NONE',  ( 0.000000000000000000, -4.261787119645322974, 26.19803753235775190 ) ) ;
#26499=DIRECTION ( 'NONE',  ( -1.000000000000000000, 0.000000000000000000, 0.000000000000000000 ) ) ;
#26505=ORIENTED_EDGE ( 'NONE', *, *, #44547, .F. ) ;
#26515=CARTESIAN_POINT ( 'NONE',  ( 0.000000000000000000, 0.8828120875905820508, -37.48860685352290290 ) ) ;
#26537=DIRECTION ( 'NONE',  ( 0.000000000000000000, 0.7431448254773954654, -0.6691306063588569053 ) ) ;
#26541=ORIENTED_EDGE ( 'NONE', *, *, #53876, .F. ) ;
#26546=VERTEX_POINT ( 'NONE', #19241 ) ;
#26590=AXIS2_PLACEMENT_3D ( 'NONE', #21185, #5047, #44138 ) ;
#26594=VERTEX_POINT ( 'NONE', #63521 ) ;
#26597=LINE ( 'NONE', #48423, #2453 ) ;
#26599=CYLINDRICAL_SURFACE ( 'NONE', #54766, 16.00000000000000000 ) ;
#26606=DIRECTION ( 'NONE',  ( 0.000000000000000000, 0.000000000000000000, -1.000000000000000000 ) ) ;
#26619=EDGE_CURVE ( 'NONE', #63855, #35666, #11996, .T. ) ;
#26621=DIRECTION ( 'NONE',  ( 0.000000000000000000, 0.000000000000000000, -1.000000000000000000 ) ) ;
#26642=ORIENTED_EDGE ( 'NONE', *, *, #70656, .F. ) ;
#26646=ORIENTED_EDGE ( 'NONE', *, *, #70276, .T. ) ;
#26649=VERTEX_POINT ( 'NONE', #58596 ) ;
#26665=EDGE_CURVE ( 'NONE', #42918, #70364, #18734, .T. ) ;
#26666=CARTESIAN_POINT ( 'NONE',  ( 10.00000000000000000, 0.000000000000000000, 0.000000000000000000 ) ) ;
#26669=ADVANCED_FACE ( 'NONE', ( #12360 ), #762, .T. ) ;
#26670=CARTESIAN_POINT ( 'NONE',  ( 10.00000000000000000, 15.48615015657582283, 39.04073710021349797 ) ) ;
#26678=AXIS2_PLACEMENT_3D ( 'NONE', #55877, #4772, #27675 ) ;
#26687=ORIENTED_EDGE ( 'NONE', *, *, #42689, .F. ) ;
#26701=CARTESIAN_POINT ( 'NONE',  ( 0.000000000000000000, -1.278221433540501550, 26.51162292216071847 ) ) ;
#26704=DIRECTION ( 'NONE',  ( -1.000000000000000000, 0.000000000000000000, 0.000000000000000000 ) ) ;
#26706=EDGE_CURVE ( 'NONE', #25402, #19772, #30014, .T. ) ;
#26707=VERTEX_POINT ( 'NONE', #68789 ) ;
#26733=DIRECTION ( 'NONE',  ( -1.000000000000000000, 0.000000000000000000, 0.000000000000000000 ) ) ;
#26743=EDGE_CURVE ( 'NONE', #68977, #62228, #53331, .T. ) ;
#26744=CYLINDRICAL_SURFACE ( 'NONE', #63533, 42.00000000000000000 ) ;
#26748=CARTESIAN_POINT ( 'NONE',  ( 0.000000000000000000, 10.74501242461282757, 35.92658777277515014 ) ) ;
#26749=DIRECTION ( 'NONE',  ( 0.000000000000000000, 0.000000000000000000, 1.000000000000000000 ) ) ;
#26755=ORIENTED_EDGE ( 'NONE', *, *, #30855, .F. ) ;
#26786=AXIS2_PLACEMENT_3D ( 'NONE', #18953, #63735, #980 ) ;
#26790=AXIS2_PLACEMENT_3D ( 'NONE', #23362, #16595, #22618 ) ;
#26792=ADVANCED_FACE ( 'NONE', ( #21231 ), #3978, .T. ) ;
#26800=ORIENTED_EDGE ( 'NONE', *, *, #14373, .F. ) ;
#26802=EDGE_CURVE ( 'NONE', #58339, #18110, #72727, .T. ) ;
#26819=CARTESIAN_POINT ( 'NONE',  ( 0.000000000000000000, 0.000000000000000000, 0.000000000000000000 ) ) ;
#26822=VERTEX_POINT ( 'NONE', #3618 ) ;
#26831=DIRECTION ( 'NONE',  ( -1.000000000000000000, -0.000000000000000000, 0.000000000000000000 ) ) ;
#26837=EDGE_CURVE ( 'NONE', #70257, #5113, #70596, .T. ) ;
#26842=VERTEX_POINT ( 'NONE', #50171 ) ;
#26844=LINE ( 'NONE', #8822, #63164 ) ;
#26852=VERTEX_POINT ( 'NONE', #26515 ) ;
#26860=FACE_OUTER_BOUND ( 'NONE', #9642, .T. ) ;
#26873=AXIS2_PLACEMENT_3D ( 'NONE', #49788, #26119, #60358 ) ;
#26876=DIRECTION ( 'NONE',  ( 1.000000000000000000, 0.000000000000000000, -0.000000000000000000 ) ) ;
#26884=EDGE_CURVE ( 'NONE', #26649, #22283, #72003, .T. ) ;
#26887=DIRECTION ( 'NONE',  ( -1.000000000000000000, 0.000000000000000000, 0.000000000000000000 ) ) ;
#26897=VERTEX_POINT ( 'NONE', #15233 ) ;
#26910=EDGE_CURVE ( 'NONE', #56201, #42329, #5417, .T. ) ;
#26913=VERTEX_POINT ( 'NONE', #69289 ) ;
#26920=LINE ( 'NONE', #14157, #46248 ) ;
#26923=CYLINDRICAL_SURFACE ( 'NONE', #59119, 42.00000000000000000 ) ;
#26927=ORIENTED_EDGE ( 'NONE', *, *, #59410, .T. ) ;
#26936=ORIENTED_EDGE ( 'NONE', *, *, #23800, .T. ) ;
#26949=CIRCLE ( 'NONE', #8930, 16.00000000000000355 ) ;
#26961=CYLINDRICAL_SURFACE ( 'NONE', #61230, 16.00000000000000000 ) ;
#26982=VERTEX_POINT ( 'NONE', #29059 ) ;
#26998=AXIS2_PLACEMENT_3D ( 'NONE', #17272, #63151, #57502 ) ;
#27011=ORIENTED_EDGE ( 'NONE', *, *, #29050, .T. ) ;
#27013=LINE ( 'NONE', #65773, #23921 ) ;
#27026=FACE_OUTER_BOUND ( 'NONE', #72267, .T. ) ;
#27029=DIRECTION ( 'NONE',  ( 0.000000000000000000, -0.9781476007338070211, 0.2079116908177525425 ) ) ;
#27031=CYLINDRICAL_SURFACE ( 'NONE', #65074, 42.00000000000000000 ) ;
#27043=CIRCLE ( 'NONE', #60667, 16.00000000000000000 ) ;
#27047=DIRECTION ( 'NONE',  ( -1.000000000000000000, -0.000000000000000000, -0.000000000000000000 ) ) ;
#27071=DIRECTION ( 'NONE',  ( 0.000000000000000000, 0.000000000000000000, 1.000000000000000000 ) ) ;
#27072=ORIENTED_EDGE ( 'NONE', *, *, #43047, .T. ) ;
#27079=VERTEX_POINT ( 'NONE', #8354 ) ;
#27107=VERTEX_POINT ( 'NONE', #42943 ) ;
#27109=VERTEX_POINT ( 'NONE', #31641 ) ;
#27119=FACE_OUTER_BOUND ( 'NONE', #59875, .T. ) ;
#27120=EDGE_CURVE ( 'NONE', #15096, #5732, #4437, .T. ) ;
#27123=FACE_OUTER_BOUND ( 'NONE', #52408, .T. ) ;
#27136=CARTESIAN_POINT ( 'NONE',  ( -10.00000000000000000, 0.000000000000000000, 0.000000000000000000 ) ) ;
#27156=CARTESIAN_POINT ( 'NONE',  ( 10.00000000000000000, 33.80338159004307386, -16.23288003029461279 ) ) ;
#27166=CARTESIAN_POINT ( 'NONE',  ( -3.000000000000000000, -14.54903810567676636, 22.19967320028755964 ) ) ;
#27191=CARTESIAN_POINT ( 'NONE',  ( -3.000000000000000000, -4.261787119645322974, 26.19803753235774835 ) ) ;
#27215=VECTOR ( 'NONE', #5779, 999.9999999999998863 ) ;
#27216=FACE_OUTER_BOUND ( 'NONE', #16975, .T. ) ;
#27217=CARTESIAN_POINT ( 'NONE',  ( 10.00000000000000000, 33.80338159004283938, 16.23288003029508886 ) ) ;
#27222=CIRCLE ( 'NONE', #69261, 16.00000000000000000 ) ;
#27227=EDGE_CURVE ( 'NONE', #3283, #10069, #9825, .T. ) ;
#27228=DIRECTION ( 'NONE',  ( 0.000000000000000000, 0.000000000000000000, 1.000000000000000000 ) ) ;
#27237=EDGE_CURVE ( 'NONE', #46924, #48813, #9453, .T. ) ;
#27242=DIRECTION ( 'NONE',  ( 0.000000000000000000, 0.000000000000000000, -1.000000000000000000 ) ) ;
#27250=VERTEX_POINT ( 'NONE', #55694 ) ;
#27258=CIRCLE ( 'NONE', #36872, 37.49900000000000944 ) ;
#27265=VECTOR ( 'NONE', #41373, 1000.000000000000000 ) ;
#27270=CARTESIAN_POINT ( 'NONE',  ( 0.000000000000000000, -37.58145647212455032, 0.6853352020789044152 ) ) ;
#27283=CARTESIAN_POINT ( 'NONE',  ( -10.00000000000000000, 0.000000000000000000, 0.000000000000000000 ) ) ;
#27287=DIRECTION ( 'NONE',  ( 0.000000000000000000, 0.000000000000000000, 1.000000000000000000 ) ) ;
#27291=COLOUR_RGB ( '', 0.31764706, 0.68627451, 0.89019608) ;
#27303=FACE_BOUND ( 'NONE', #3304, .T. ) ;
#27349=ORIENTED_EDGE ( 'NONE', *, *, #68828, .F. ) ;
#27350=CARTESIAN_POINT ( 'NONE',  ( 0.000000000000000000, -30.00120703465189465, -22.64427369931201639 ) ) ;
#27364=DIRECTION ( 'NONE',  ( -1.000000000000000000, -0.000000000000000000, 0.000000000000000000 ) ) ;
#27366=AXIS2_PLACEMENT_3D ( 'NONE', #69533, #34954, #28939 ) ;
#27381=VERTEX_POINT ( 'NONE', #49666 ) ;
#27395=ADVANCED_FACE ( 'NONE', ( #39525 ), #5692, .T. ) ;
#27405=FACE_OUTER_BOUND ( 'NONE', #46259, .T. ) ;
#27408=FACE_OUTER_BOUND ( 'NONE', #59181, .T. ) ;
#27416=ADVANCED_FACE ( 'NONE', ( #28594 ), #16582, .T. ) ;
#27422=DIRECTION ( 'NONE',  ( -1.000000000000000000, -0.000000000000000000, -0.000000000000000000 ) ) ;
#27424=DIRECTION ( 'NONE',  ( 1.000000000000000000, 0.000000000000000000, -0.000000000000000000 ) ) ;
#27438=VECTOR ( 'NONE', #53881, 1000.000000000000000 ) ;
#27439=ORIENTED_EDGE ( 'NONE', *, *, #12589, .F. ) ;
#27440=LINE ( 'NONE', #9791, #64658 ) ;
#27448=DIRECTION ( 'NONE',  ( 0.000000000000000000, 0.000000000000000000, -1.000000000000000000 ) ) ;
#27452=ORIENTED_EDGE ( 'NONE', *, *, #1973, .F. ) ;
#27454=LINE ( 'NONE', #9805, #19194 ) ;
#27461=VERTEX_POINT ( 'NONE', #63573 ) ;
#27476=ORIENTED_EDGE ( 'NONE', *, *, #66313, .F. ) ;
#27484=EDGE_CURVE ( 'NONE', #51707, #39053, #5328, .T. ) ;
#27511=AXIS2_PLACEMENT_3D ( 'NONE', #27350, #38653, #15330 ) ;
#27513=DIRECTION ( 'NONE',  ( 0.000000000000000000, 0.000000000000000000, 1.000000000000000000 ) ) ;
#27516=ORIENTED_EDGE ( 'NONE', *, *, #24273, .T. ) ;
#27521=DIRECTION ( 'NONE',  ( 0.000000000000000000, 0.4067366430758000417, -0.9135454576426009776 ) ) ;
#27523=CARTESIAN_POINT ( 'NONE',  ( 4.999999999999999112, -41.81611651403859042, -3.925862922256606602 ) ) ;
#27537=VERTEX_POINT ( 'NONE', #1196 ) ;
#27540=ORIENTED_EDGE ( 'NONE', *, *, #69841, .F. ) ;
#27544=EDGE_CURVE ( 'NONE', #2465, #57048, #8260, .T. ) ;
#27560=CARTESIAN_POINT ( 'NONE',  ( 0.000000000000000000, 0.000000000000000000, 0.000000000000000000 ) ) ;
#27563=FACE_OUTER_BOUND ( 'NONE', #63542, .T. ) ;
#27585=CARTESIAN_POINT ( 'NONE',  ( 10.00000000000000000, -33.80338159004296017, 16.23288003029484727 ) ) ;
#27592=FACE_OUTER_BOUND ( 'NONE', #69179, .T. ) ;
#27596=CARTESIAN_POINT ( 'NONE',  ( 10.00000000000000000, 0.000000000000000000, 0.000000000000000000 ) ) ;
#27614=CIRCLE ( 'NONE', #69633, 42.00000000000000000 ) ;
#27620=AXIS2_PLACEMENT_3D ( 'NONE', #41084, #51236, #74166 ) ;
#27621=VECTOR ( 'NONE', #73809, 1000.000000000000000 ) ;
#27634=ORIENTED_EDGE ( 'NONE', *, *, #9695, .T. ) ;
#27639=EDGE_CURVE ( 'NONE', #10014, #30392, #58288, .T. ) ;
#27640=LINE ( 'NONE', #73866, #2884 ) ;
#27658=EDGE_LOOP ( 'NONE', ( #41148, #44853, #21707, #11895 ) ) ;
#27669=DIRECTION ( 'NONE',  ( -1.000000000000000000, -0.000000000000000000, -0.000000000000000000 ) ) ;
#27675=DIRECTION ( 'NONE',  ( 0.000000000000000000, 0.9945218953682731788, 0.1045284632676559550 ) ) ;
#27681=VECTOR ( 'NONE', #24574, 1000.000000000000000 ) ;
#27684=CARTESIAN_POINT ( 'NONE',  ( 10.00000000000000000, -12.26510123303234501, -35.53030884539098366 ) ) ;
#27693=FACE_BOUND ( 'NONE', #17791, .T. ) ;
#27719=AXIS2_PLACEMENT_3D ( 'NONE', #54479, #68656, #8628 ) ;
#27720=LINE ( 'NONE', #62320, #50323 ) ;
#27741=ORIENTED_EDGE ( 'NONE', *, *, #69088, .T. ) ;
#27758=CYLINDRICAL_SURFACE ( 'NONE', #23391, 16.00000000000000000 ) ;
#27767=DIRECTION ( 'NONE',  ( 0.000000000000000000, 0.1564344650402244852, 0.9876883405951387696 ) ) ;
#27774=ORIENTED_EDGE ( 'NONE', *, *, #67586, .T. ) ;
#27780=EDGE_CURVE ( 'NONE', #48813, #53009, #37948, .T. ) ;
#27786=VECTOR ( 'NONE', #35929, 1000.000000000000000 ) ;
#27797=CARTESIAN_POINT ( 'NONE',  ( 0.000000000000000000, 4.992566952385522505, -37.16516213103271582 ) ) ;
#27828=FACE_OUTER_BOUND ( 'NONE', #63374, .T. ) ;
#27849=EDGE_LOOP ( 'NONE', ( #15356, #1913, #40969, #51150 ) ) ;
#27861=CARTESIAN_POINT ( 'NONE',  ( -3.000000000000000000, -14.54903810567645195, -22.19967320028775504 ) ) ;
#27866=VERTEX_POINT ( 'NONE', #17244 ) ;
#27872=DIRECTION ( 'NONE',  ( 0.000000000000000000, 0.000000000000000000, 1.000000000000000000 ) ) ;
#27888=DIRECTION ( 'NONE',  ( -1.000000000000000000, -0.000000000000000000, -0.000000000000000000 ) ) ;
#27893=CARTESIAN_POINT ( 'NONE',  ( 10.00000000000000000, 21.40280677340372151, 36.13751322684426981 ) ) ;
#27912=ORIENTED_EDGE ( 'NONE', *, *, #24602, .F. ) ;
#27918=ORIENTED_EDGE ( 'NONE', *, *, #9864, .F. ) ;
#27931=CIRCLE ( 'NONE', #47156, 42.00000000000000000 ) ;
#27934=CARTESIAN_POINT ( 'NONE',  ( 10.00000000000000000, 39.04073710021344112, 15.48615015657596317 ) ) ;
#27935=DIRECTION ( 'NONE',  ( 0.000000000000000000, 0.000000000000000000, 1.000000000000000000 ) ) ;
#27936=DIRECTION ( 'NONE',  ( -1.000000000000000000, 0.000000000000000000, 0.000000000000000000 ) ) ;
#27947=DIRECTION ( 'NONE',  ( 0.000000000000000000, -0.4539904997395540764, 0.8910065241883642351 ) ) ;
#27952=CARTESIAN_POINT ( 'NONE',  ( 10.00000000000000000, 35.53030884539084866, 12.26510123303271982 ) ) ;
#27954=EDGE_LOOP ( 'NONE', ( #71091, #72471, #23485, #12540 ) ) ;
#27956=FACE_OUTER_BOUND ( 'NONE', #73245, .T. ) ;
#27979=CARTESIAN_POINT ( 'NONE',  ( -3.000000000000000000, -26.23277895567245821, -4.042438405570103477 ) ) ;
#27990=VERTEX_POINT ( 'NONE', #25382 ) ;
#27991=DIRECTION ( 'NONE',  ( 0.000000000000000000, 1.000000000000000000, 3.491481338843133750E-15 ) ) ;
#27992=ORIENTED_EDGE ( 'NONE', *, *, #58392, .T. ) ;
#27994=LINE ( 'NONE', #12918, #70587 ) ;
#27997=ORIENTED_EDGE ( 'NONE', *, *, #67078, .F. ) ;
#27999=ORIENTED_EDGE ( 'NONE', *, *, #63190, .F. ) ;
#28011=LINE ( 'NONE', #69350, #16644 ) ;
#28013=CARTESIAN_POINT ( 'NONE',  ( 0.000000000000000000, -41.81611651403864727, 3.925862922256025289 ) ) ;
#28039=CARTESIAN_POINT ( 'NONE',  ( 10.00000000000000000, -33.79645857604501913, -16.45098606841161626 ) ) ;
#28049=ORIENTED_EDGE ( 'NONE', *, *, #25779, .T. ) ;
#28051=ORIENTED_EDGE ( 'NONE', *, *, #48119, .T. ) ;
#28069=VERTEX_POINT ( 'NONE', #53572 ) ;
#28073=VECTOR ( 'NONE', #7397, 999.9999999999998863 ) ;
#28074=EDGE_CURVE ( 'NONE', #32803, #70819, #26102, .T. ) ;
#28077=ORIENTED_EDGE ( 'NONE', *, *, #13811, .T. ) ;
#28117=ORIENTED_EDGE ( 'NONE', *, *, #29923, .F. ) ;
#28122=CARTESIAN_POINT ( 'NONE',  ( -3.000000000000000000, 23.50000000000000000, -1.500000000000001332 ) ) ;
#28124=DIRECTION ( 'NONE',  ( -1.000000000000000000, -0.000000000000000000, -0.000000000000000000 ) ) ;
#28126=DIRECTION ( 'NONE',  ( 0.000000000000000000, -0.1045284632676578285, 0.9945218953682729568 ) ) ;
#28134=AXIS2_PLACEMENT_3D ( 'NONE', #48444, #65743, #15722 ) ;
#28151=CIRCLE ( 'NONE', #30557, 15.99999999999999822 ) ;
#28175=VECTOR ( 'NONE', #71732, 1000.000000000000000 ) ;
#28193=CIRCLE ( 'NONE', #3009, 16.00000000000000355 ) ;
#28229=CARTESIAN_POINT ( 'NONE',  ( 0.000000000000000000, -9.188173127307592836, 40.98264845739746676 ) ) ;
#28231=FACE_OUTER_BOUND ( 'NONE', #23327, .T. ) ;
#28236=CARTESIAN_POINT ( 'NONE',  ( 0.000000000000000000, 38.55633173627010279, 16.65560815589424593 ) ) ;
#28239=LINE ( 'NONE', #35006, #17204 ) ;
#28252=DIRECTION ( 'NONE',  ( 0.000000000000000000, 0.5877852522924741363, -0.8090169943749465631 ) ) ;
#28260=CARTESIAN_POINT ( 'NONE',  ( 10.00000000000000000, 0.000000000000000000, 0.000000000000000000 ) ) ;
#28272=EDGE_CURVE ( 'NONE', #49986, #67800, #47122, .T. ) ;
#28279=CARTESIAN_POINT ( 'NONE',  ( -3.000000000000000000, -3.948201729842348850, 23.21447184625293048 ) ) ;
#28295=CIRCLE ( 'NONE', #19920, 16.00000000000000000 ) ;
#28296=CARTESIAN_POINT ( 'NONE',  ( 0.000000000000000000, -25.88420570971381807, -27.13269053701123212 ) ) ;
#28304=VECTOR ( 'NONE', #43791, 1000.000000000000000 ) ;
#28316=CYLINDRICAL_SURFACE ( 'NONE', #34326, 42.00000000000000000 ) ;
#28335=DIRECTION ( 'NONE',  ( 0.000000000000000000, 0.9781476007338041345, 0.2079116908177664480 ) ) ;
#28337=CARTESIAN_POINT ( 'NONE',  ( 10.00000000000000000, 0.000000000000000000, 0.000000000000000000 ) ) ;
#28357=EDGE_CURVE ( 'NONE', #3072, #72829, #53784, .T. ) ;
#28359=DIRECTION ( 'NONE',  ( -1.000000000000000000, 0.000000000000000000, 0.000000000000000000 ) ) ;
#28387=DIRECTION ( 'NONE',  ( 0.000000000000000000, -0.8910065241883626808, -0.4539904997395570740 ) ) ;
#28392=ORIENTED_EDGE ( 'NONE', *, *, #53043, .T. ) ;
#28395=VERTEX_POINT ( 'NONE', #47482 ) ;
#28407=DIRECTION ( 'NONE',  ( 0.000000000000000000, -0.5877852522924801315, 0.8090169943749421222 ) ) ;
#28409=VECTOR ( 'NONE', #55830, 1000.000000000000000 ) ;
#28410=ORIENTED_EDGE ( 'NONE', *, *, #1235, .F. ) ;
#28412=VECTOR ( 'NONE', #32545, 1000.000000000000000 ) ;
#28417=AXIS2_PLACEMENT_3D ( 'NONE', #66537, #50714, #32671 ) ;
#28445=EDGE_CURVE ( 'NONE', #57981, #14321, #39426, .T. ) ;
#28448=ADVANCED_FACE ( 'NONE', ( #70767 ), #59506, .T. ) ;
#28466=VERTEX_POINT ( 'NONE', #30910 ) ;
#28477=EDGE_CURVE ( 'NONE', #45442, #13480, #40597, .T. ) ;
#28497=ORIENTED_EDGE ( 'NONE', *, *, #33699, .T. ) ;
#28508=EDGE_CURVE ( 'NONE', #57225, #32534, #9396, .T. ) ;
#28524=DIRECTION ( 'NONE',  ( 1.000000000000000000, -0.000000000000000000, 0.000000000000000000 ) ) ;
#28528=STYLED_ITEM ( 'NONE', ( #65735 ), #39004 ) ;
#28538=PLANE ( 'NONE',  #49040 ) ;
#28560=ORIENTED_EDGE ( 'NONE', *, *, #65558, .F. ) ;
#28565=DIRECTION ( 'NONE',  ( -1.000000000000000000, 0.000000000000000000, 0.000000000000000000 ) ) ;
#28567=ADVANCED_FACE ( 'NONE', ( #9843 ), #16591, .T. ) ;
#28573=EDGE_CURVE ( 'NONE', #62140, #52314, #19065, .T. ) ;
#28575=ORIENTED_EDGE ( 'NONE', *, *, #41227, .T. ) ;
#28579=ADVANCED_FACE ( 'NONE', ( #66622 ), #3483, .T. ) ;
#28594=FACE_OUTER_BOUND ( 'NONE', #24089, .T. ) ;
#28610=CIRCLE ( 'NONE', #8168, 37.49900000000000233 ) ;
#28611=VECTOR ( 'NONE', #35012, 1000.000000000000000 ) ;
#28612=EDGE_CURVE ( 'NONE', #27381, #18231, #71863, .T. ) ;
#28613=CARTESIAN_POINT ( 'NONE',  ( 10.00000000000000000, 30.80686688397041451, -21.53537804866048688 ) ) ;
#28614=CARTESIAN_POINT ( 'NONE',  ( 0.000000000000000000, 36.88895765772633695, 6.736453364083687667 ) ) ;
#28615=DIRECTION ( 'NONE',  ( -1.000000000000000000, -0.000000000000000000, -0.000000000000000000 ) ) ;
#28617=LINE ( 'NONE', #51559, #52559 ) ;
#28633=AXIS2_PLACEMENT_3D ( 'NONE', #59056, #6802, #19189 ) ;
#28634=DIRECTION ( 'NONE',  ( -1.000000000000000000, 0.000000000000000000, -0.000000000000000000 ) ) ;
#28637=CARTESIAN_POINT ( 'NONE',  ( -3.000000000000000000, -10.45096189432314837, -21.10159698893440350 ) ) ;
#28650=CIRCLE ( 'NONE', #53888, 21.00000000000000000 ) ;
#28655=DIRECTION ( 'NONE',  ( -1.000000000000000000, -0.000000000000000000, -0.000000000000000000 ) ) ;
#28660=ORIENTED_EDGE ( 'NONE', *, *, #45185, .F. ) ;
#28666=AXIS2_PLACEMENT_3D ( 'NONE', #4222, #38046, #68103 ) ;
#28677=ORIENTED_EDGE ( 'NONE', *, *, #22953, .F. ) ;
#28694=AXIS2_PLACEMENT_3D ( 'NONE', #64281, #13855, #2265 ) ;
#28703=DIRECTION ( 'NONE',  ( 0.000000000000000000, 0.000000000000000000, 1.000000000000000000 ) ) ;
#28707=ORIENTED_EDGE ( 'NONE', *, *, #72184, .T. ) ;
#28709=CARTESIAN_POINT ( 'NONE',  ( 10.00000000000000000, 37.48860685352291000, 0.8828120875901893649 ) ) ;
#28710=ADVANCED_FACE ( 'NONE', ( #6440 ), #63218, .F. ) ;
#28754=EDGE_CURVE ( 'NONE', #68962, #18236, #65885, .T. ) ;
#28767=ORIENTED_EDGE ( 'NONE', *, *, #48033, .F. ) ;
#28778=DIRECTION ( 'NONE',  ( -1.000000000000000000, 0.000000000000000000, 0.000000000000000000 ) ) ;
#28787=PLANE ( 'NONE',  #30124 ) ;
#28795=PLANE ( 'NONE',  #71423 ) ;
#28800=DIRECTION ( 'NONE',  ( 0.000000000000000000, 0.3090169943749410120, 0.9510565162951557516 ) ) ;
#28805=CARTESIAN_POINT ( 'NONE',  ( -3.000000000000000000, -18.13022148937263012, 15.02647892043544608 ) ) ;
#28806=FACE_OUTER_BOUND ( 'NONE', #56676, .T. ) ;
#28814=DIRECTION ( 'NONE',  ( 0.000000000000000000, 0.000000000000000000, 1.000000000000000000 ) ) ;
#28824=VECTOR ( 'NONE', #34290, 1000.000000000000227 ) ;
#28832=ORIENTED_EDGE ( 'NONE', *, *, #22167, .F. ) ;
#28837=CARTESIAN_POINT ( 'NONE',  ( 0.000000000000000000, 0.000000000000000000, 0.000000000000000000 ) ) ;
#28884=DIRECTION ( 'NONE',  ( 0.000000000000000000, 0.000000000000000000, 1.000000000000000000 ) ) ;
#28892=ORIENTED_EDGE ( 'NONE', *, *, #25693, .T. ) ;
#28895=AXIS2_PLACEMENT_3D ( 'NONE', #20167, #71293, #48014 ) ;
#28921=ADVANCED_FACE ( 'NONE', ( #7540 ), #36467, .T. ) ;
#28931=EDGE_CURVE ( 'NONE', #11579, #68891, #4716, .T. ) ;
#28939=DIRECTION ( 'NONE',  ( 0.000000000000000000, 0.000000000000000000, 1.000000000000000000 ) ) ;
#28957=ORIENTED_EDGE ( 'NONE', *, *, #4812, .F. ) ;
#28968=CARTESIAN_POINT ( 'NONE',  ( 0.000000000000000000, -41.91543099594819921, 2.663952781846001816 ) ) ;
#28970=ORIENTED_EDGE ( 'NONE', *, *, #30068, .F. ) ;
#29003=CIRCLE ( 'NONE', #69845, 16.00000000000000000 ) ;
#29008=LINE ( 'NONE', #62509, #39658 ) ;
#29019=DIRECTION ( 'NONE',  ( -1.000000000000000000, -0.000000000000000000, 0.000000000000000000 ) ) ;
#29025=ORIENTED_EDGE ( 'NONE', *, *, #46371, .T. ) ;
#29026=ADVANCED_FACE ( 'NONE', ( #66538 ), #37959, .T. ) ;
#29036=ADVANCED_FACE ( 'NONE', ( #49229 ), #71780, .T. ) ;
#29050=EDGE_CURVE ( 'NONE', #33020, #66879, #56321, .T. ) ;
#29059=CARTESIAN_POINT ( 'NONE',  ( 0.000000000000000000, 15.48615015657581750, 39.04073710021349797 ) ) ;
#29066=VERTEX_POINT ( 'NONE', #72522 ) ;
#29073=LINE ( 'NONE', #70389, #10804 ) ;
#29095=ORIENTED_EDGE ( 'NONE', *, *, #6372, .F. ) ;
#29115=DIRECTION ( 'NONE',  ( -1.000000000000000000, -0.000000000000000000, 0.000000000000000000 ) ) ;
#29121=EDGE_CURVE ( 'NONE', #18110, #69032, #11975, .T. ) ;
#29126=CARTESIAN_POINT ( 'NONE',  ( 10.00000000000000000, 30.84782396557218931, 21.32104025579126017 ) ) ;
#29128=DIRECTION ( 'NONE',  ( -0.000000000000000000, -0.9945218953682741780, 0.1045284632676447834 ) ) ;
#29146=CARTESIAN_POINT ( 'NONE',  ( 0.000000000000000000, -22.48208911017474065, -35.47612816024548721 ) ) ;
#29176=EDGE_CURVE ( 'NONE', #53734, #2347, #5622, .T. ) ;
#29180=ORIENTED_EDGE ( 'NONE', *, *, #43119, .F. ) ;
#29181=CARTESIAN_POINT ( 'NONE',  ( 10.00000000000000000, 17.80606268964585226, -33.00180498840028775 ) ) ;
#29200=ORIENTED_EDGE ( 'NONE', *, *, #27639, .F. ) ;
#29202=AXIS2_PLACEMENT_3D ( 'NONE', #44339, #4885, #5249 ) ;
#29204=PLANE ( 'NONE',  #2247 ) ;
#29217=ORIENTED_EDGE ( 'NONE', *, *, #33699, .F. ) ;
#29228=ORIENTED_EDGE ( 'NONE', *, *, #8987, .F. ) ;
#29235=AXIS2_PLACEMENT_3D ( 'NONE', #50152, #26499, #32866 ) ;
#29247=DIRECTION ( 'NONE',  ( -1.000000000000000000, -0.000000000000000000, 0.000000000000000000 ) ) ;
#29255=DIRECTION ( 'NONE',  ( 0.000000000000000000, 0.8910065241883688980, -0.4539904997395446951 ) ) ;
#29271=ORIENTED_EDGE ( 'NONE', *, *, #65995, .F. ) ;
#29272=ADVANCED_FACE ( 'NONE', ( #46940 ), #29998, .T. ) ;
#29286=FACE_OUTER_BOUND ( 'NONE', #65487, .T. ) ;
#29292=ORIENTED_EDGE ( 'NONE', *, *, #4784, .T. ) ;
#29297=CARTESIAN_POINT ( 'NONE',  ( 0.000000000000000000, 0.000000000000000000, 0.000000000000000000 ) ) ;
#29304=CIRCLE ( 'NONE', #42583, 15.99999999999999822 ) ;
#29318=CARTESIAN_POINT ( 'NONE',  ( 0.000000000000000000, 22.07842321921481243, 8.187992925817422218 ) ) ;
#29323=AXIS2_PLACEMENT_3D ( 'NONE', #11622, #51860, #56406 ) ;
#29337=CYLINDRICAL_SURFACE ( 'NONE', #52781, 16.00000000000000000 ) ;
#29345=VECTOR ( 'NONE', #52093, 1000.000000000000000 ) ;
#29349=DIRECTION ( 'NONE',  ( -1.000000000000000000, -0.000000000000000000, 0.000000000000000000 ) ) ;
#29358=AXIS2_PLACEMENT_3D ( 'NONE', #9652, #39345, #73164 ) ;
#29361=CIRCLE ( 'NONE', #68985, 37.49900000000001654 ) ;
#29370=CARTESIAN_POINT ( 'NONE',  ( 5.000000000000000000, 39.04073710021366139, -15.48615015657542138 ) ) ;
#29372=ORIENTED_EDGE ( 'NONE', *, *, #44740, .F. ) ;
#29391=ORIENTED_EDGE ( 'NONE', *, *, #25330, .T. ) ;
#29396=DIRECTION ( 'NONE',  ( -1.000000000000000000, 0.000000000000000000, -0.000000000000000000 ) ) ;
#29408=CIRCLE ( 'NONE', #73799, 42.00000000000000000 ) ;
#29413=DIRECTION ( 'NONE',  ( 1.000000000000000000, 0.000000000000000000, -0.000000000000000000 ) ) ;
#29416=CARTESIAN_POINT ( 'NONE',  ( 0.000000000000000000, 37.48860685352291000, -0.8828120875901940279 ) ) ;
#29417=CIRCLE ( 'NONE', #71430, 16.00000000000000000 ) ;
#29419=ORIENTED_EDGE ( 'NONE', *, *, #74167, .F. ) ;
#29448=VERTEX_POINT ( 'NONE', #66815 ) ;
#29456=ADVANCED_FACE ( 'NONE', ( #32589 ), #55537, .T. ) ;
#29458=CARTESIAN_POINT ( 'NONE',  ( 10.00000000000000000, 0.000000000000000000, 0.000000000000000000 ) ) ;
#29464=CARTESIAN_POINT ( 'NONE',  ( 0.000000000000000000, 33.80338159004283938, 16.23288003029508886 ) ) ;
#29472=AXIS2_PLACEMENT_3D ( 'NONE', #56164, #39254, #15571 ) ;
#29480=VERTEX_POINT ( 'NONE', #8563 ) ;
#29491=CARTESIAN_POINT ( 'NONE',  ( 0.000000000000000000, 33.79645857604513992, -16.45098606841138178 ) ) ;
#29507=FACE_OUTER_BOUND ( 'NONE', #71169, .T. ) ;
#29514=EDGE_CURVE ( 'NONE', #24241, #23404, #40589, .T. ) ;
#29515=FACE_OUTER_BOUND ( 'NONE', #15812, .T. ) ;
#29517=CARTESIAN_POINT ( 'NONE',  ( 10.00000000000000000, 35.38097989696528600, -12.42422080174602605 ) ) ;
#29527=DIRECTION ( 'NONE',  ( 0.000000000000000000, 0.5877852522924741363, -0.8090169943749465631 ) ) ;
#29529=VECTOR ( 'NONE', #9382, 999.9999999999998863 ) ;
#29564=ORIENTED_EDGE ( 'NONE', *, *, #18354, .F. ) ;
#29577=CIRCLE ( 'NONE', #41569, 42.00000000000000000 ) ;
#29585=CARTESIAN_POINT ( 'NONE',  ( 0.000000000000000000, 16.23288003029497162, 33.80338159004289622 ) ) ;
#29586=EDGE_CURVE ( 'NONE', #16540, #25590, #11921, .T. ) ;
#29606=ORIENTED_EDGE ( 'NONE', *, *, #993, .F. ) ;
#29614=CARTESIAN_POINT ( 'NONE',  ( 0.000000000000000000, 37.16516213103285082, -4.992566952384588141 ) ) ;
#29616=CARTESIAN_POINT ( 'NONE',  ( 0.000000000000000000, -0.6853352020793173072, 37.58145647212453611 ) ) ;
#29620=DIRECTION ( 'NONE',  ( 0.000000000000000000, 0.000000000000000000, -1.000000000000000000 ) ) ;
#29631=FACE_OUTER_BOUND ( 'NONE', #27849, .T. ) ;
#29649=ORIENTED_EDGE ( 'NONE', *, *, #7016, .F. ) ;
#29668=VERTEX_POINT ( 'NONE', #62684 ) ;
#29689=ORIENTED_EDGE ( 'NONE', *, *, #26802, .F. ) ;
#29694=PLANE ( 'NONE',  #11012 ) ;
#29700=DIRECTION ( 'NONE',  ( 0.000000000000000000, 0.2079116908177543743, 0.9781476007338066880 ) ) ;
#29725=DIRECTION ( 'NONE',  ( 0.000000000000000000, 0.000000000000000000, 1.000000000000000000 ) ) ;
#29731=DIRECTION ( 'NONE',  ( 0.000000000000000000, 0.000000000000000000, 1.000000000000000000 ) ) ;
#29733=ORIENTED_EDGE ( 'NONE', *, *, #634, .F. ) ;
#29739=CARTESIAN_POINT ( 'NONE',  ( 0.000000000000000000, 14.60985201121729737, -18.46759930825687945 ) ) ;
#29749=EDGE_LOOP ( 'NONE', ( #2019, #32231, #17190, #12203 ) ) ;
#29753=ADVANCED_FACE ( 'NONE', ( #23916 ), #2514, .F. ) ;
#29760=ORIENTED_EDGE ( 'NONE', *, *, #68828, .T. ) ;
#29780=EDGE_CURVE ( 'NONE', #56518, #15417, #15403, .T. ) ;
#29788=CARTESIAN_POINT ( 'NONE',  ( 10.00000000000000000, -37.48860685352291711, 0.8828120875899322373 ) ) ;
#29807=CIRCLE ( 'NONE', #46670, 16.00000000000000000 ) ;
#29814=DIRECTION ( 'NONE',  ( 0.000000000000000000, 0.9510565162951521989, 0.3090169943749517256 ) ) ;
#29851=ADVANCED_FACE ( 'NONE', ( #41568 ), #30283, .T. ) ;
#29852=VECTOR ( 'NONE', #4120, 1000.000000000000000 ) ;
#29855=ORIENTED_EDGE ( 'NONE', *, *, #63613, .T. ) ;
#29864=CARTESIAN_POINT ( 'NONE',  ( -3.000000000000000000, -4.261787119644969479, -26.19803753235780519 ) ) ;
#29866=CARTESIAN_POINT ( 'NONE',  ( 0.000000000000000000, 41.91543099594818500, 2.663952781846294915 ) ) ;
#29881=CARTESIAN_POINT ( 'NONE',  ( 10.00000000000000000, -35.53030884539094103, 12.26510123303246935 ) ) ;
#29890=LINE ( 'NONE', #17882, #13317 ) ;
#29894=EDGE_LOOP ( 'NONE', ( #18380, #40086, #50935, #42260 ) ) ;
#29902=AXIS2_PLACEMENT_3D ( 'NONE', #30384, #30010, #52962 ) ;
#29903=DIRECTION ( 'NONE',  ( 0.000000000000000000, 0.000000000000000000, 1.000000000000000000 ) ) ;
#29904=DIRECTION ( 'NONE',  ( 0.000000000000000000, 0.000000000000000000, -1.000000000000000000 ) ) ;
#29907=CARTESIAN_POINT ( 'NONE',  ( 10.00000000000000000, 0.000000000000000000, 0.000000000000000000 ) ) ;
#29913=AXIS2_PLACEMENT_3D ( 'NONE', #17318, #40252, #63200 ) ;
#29923=EDGE_CURVE ( 'NONE', #27079, #49481, #20109, .T. ) ;
#29931=ORIENTED_EDGE ( 'NONE', *, *, #62833, .F. ) ;
#29935=CARTESIAN_POINT ( 'NONE',  ( 0.000000000000000000, -10.45096189432344147, 21.10159698893426494 ) ) ;
#29938=ADVANCED_FACE ( 'NONE', ( #73731 ), #16600, .F. ) ;
#29947=ORIENTED_EDGE ( 'NONE', *, *, #14926, .T. ) ;
#29966=CARTESIAN_POINT ( 'NONE',  ( 10.00000000000000000, 36.88895765772642932, -6.736453364083163642 ) ) ;
#29974=CIRCLE ( 'NONE', #66011, 16.00000000000000000 ) ;
#29975=AXIS2_PLACEMENT_3D ( 'NONE', #11492, #62657, #67531 ) ;
#29979=DIRECTION ( 'NONE',  ( 0.000000000000000000, 0.000000000000000000, 1.000000000000000000 ) ) ;
#29981=VECTOR ( 'NONE', #50267, 1000.000000000000114 ) ;
#29996=CARTESIAN_POINT ( 'NONE',  ( 0.000000000000000000, -1.278221433540502217, 26.51162292216071847 ) ) ;
#29997=DIRECTION ( 'NONE',  ( 0.000000000000000000, 0.000000000000000000, 1.000000000000000000 ) ) ;
#29998=CYLINDRICAL_SURFACE ( 'NONE', #16719, 42.00000000000000000 ) ;
#30010=DIRECTION ( 'NONE',  ( -1.000000000000000000, 0.000000000000000000, -0.000000000000000000 ) ) ;
#30014=LINE ( 'NONE', #63153, #16440 ) ;
#30028=ADVANCED_FACE ( 'NONE', ( #16232 ), #39171, .T. ) ;
#30053=( NAMED_UNIT ( * ) PLANE_ANGLE_UNIT ( ) SI_UNIT ( $, .RADIAN. ) );
#30054=EDGE_LOOP ( 'NONE', ( #38743, #53540, #48985, #6677 ) ) ;
#30057=ADVANCED_FACE ( 'NONE', ( #69224 ), #57945, .T. ) ;
#30058=ADVANCED_FACE ( 'NONE', ( #58309 ), #109, .F. ) ;
#30068=EDGE_CURVE ( 'NONE', #11705, #67975, #12990, .T. ) ;
#30070=CARTESIAN_POINT ( 'NONE',  ( 0.000000000000000000, 20.85821328998756385, -10.92862929874494959 ) ) ;
#30074=ORIENTED_EDGE ( 'NONE', *, *, #10015, .T. ) ;
#30080=LINE ( 'NONE', #30442, #65568 ) ;
#30092=DIRECTION ( 'NONE',  ( 0.000000000000000000, 0.000000000000000000, -1.000000000000000000 ) ) ;
#30093=CARTESIAN_POINT ( 'NONE',  ( 0.000000000000000000, 0.000000000000000000, 0.000000000000000000 ) ) ;
#30095=CARTESIAN_POINT ( 'NONE',  ( 0.000000000000000000, -35.95386929396264009, 10.96151621346475658 ) ) ;
#30103=DIRECTION ( 'NONE',  ( -1.000000000000000000, 0.000000000000000000, 0.000000000000000000 ) ) ;
#30115=EDGE_CURVE ( 'NONE', #67482, #1736, #469, .T. ) ;
#30124=AXIS2_PLACEMENT_3D ( 'NONE', #51722, #270, #23162 ) ;
#30127=ORIENTED_EDGE ( 'NONE', *, *, #62895, .F. ) ;
#30131=EDGE_LOOP ( 'NONE', ( #37659, #64076, #40384, #44234 ) ) ;
#30140=ORIENTED_EDGE ( 'NONE', *, *, #70041, .T. ) ;
#30149=CARTESIAN_POINT ( 'NONE',  ( 10.00000000000000000, -0.6853352020793173072, 37.58145647212453611 ) ) ;
#30160=LINE ( 'NONE', #18509, #44352 ) ;
#30175=DIRECTION ( 'NONE',  ( -0.000000000000000000, 0.1045284632676570929, -0.9945218953682730678 ) ) ;
#30198=EDGE_CURVE ( 'NONE', #49339, #57981, #12437, .T. ) ;
#30201=ORIENTED_EDGE ( 'NONE', *, *, #39848, .F. ) ;
#30220=VERTEX_POINT ( 'NONE', #71788 ) ;
#30228=ORIENTED_EDGE ( 'NONE', *, *, #57746, .F. ) ;
#30245=DIRECTION ( 'NONE',  ( -1.000000000000000000, 0.000000000000000000, -0.000000000000000000 ) ) ;
#30253=DIRECTION ( 'NONE',  ( -1.000000000000000000, 0.000000000000000000, -0.000000000000000000 ) ) ;
#30254=CARTESIAN_POINT ( 'NONE',  ( 10.00000000000000000, -26.08949754953005495, -27.05870788708258701 ) ) ;
#30256=DIRECTION ( 'NONE',  ( 0.000000000000000000, 0.000000000000000000, -1.000000000000000000 ) ) ;
#30260=LINE ( 'NONE', #36275, #64819 ) ;
#30265=FACE_OUTER_BOUND ( 'NONE', #18216, .T. ) ;
#30267=DIRECTION ( 'NONE',  ( -1.000000000000000000, 0.000000000000000000, 0.000000000000000000 ) ) ;
#30269=ORIENTED_EDGE ( 'NONE', *, *, #60375, .T. ) ;
#30274=CIRCLE ( 'NONE', #20672, 42.00000000000000000 ) ;
#30275=DIRECTION ( 'NONE',  ( -0.000000000000000000, -0.6691306063588569053, -0.7431448254773954654 ) ) ;
#30280=DIRECTION ( 'NONE',  ( 1.000000000000000000, -0.000000000000000000, -0.000000000000000000 ) ) ;
#30283=CYLINDRICAL_SURFACE ( 'NONE', #35850, 16.00000000000000000 ) ;
#30288=DIRECTION ( 'NONE',  ( 0.000000000000000000, 0.3090169943749482839, -0.9510565162951533091 ) ) ;
#30294=AXIS2_PLACEMENT_3D ( 'NONE', #37004, #8441, #54664 ) ;
#30340=CARTESIAN_POINT ( 'NONE',  ( 0.000000000000000000, -13.04903810567675038, 19.60159698893425428 ) ) ;
#30350=DIRECTION ( 'NONE',  ( -1.000000000000000000, 0.000000000000000000, 0.000000000000000000 ) ) ;
#30365=CARTESIAN_POINT ( 'NONE',  ( 0.000000000000000000, -23.29833615347104825, -3.418703333116803744 ) ) ;
#30372=DIRECTION ( 'NONE',  ( -1.000000000000000000, -0.000000000000000000, -0.000000000000000000 ) ) ;
#30376=CARTESIAN_POINT ( 'NONE',  ( -3.000000000000000000, 26.50000000000000355, 1.500000000000000000 ) ) ;
#30381=VECTOR ( 'NONE', #6537, 1000.000000000000000 ) ;
#30384=CARTESIAN_POINT ( 'NONE',  ( 10.00000000000000000, 27.05870788708267582, -26.08949754952995903 ) ) ;
#30392=VERTEX_POINT ( 'NONE', #15394 ) ;
#30419=SHAPE_REPRESENTATION_RELATIONSHIP ( 'NONE' , 'NONE' ,  #30982, #65097 ) ;
#30420=VERTEX_POINT ( 'NONE', #27797 ) ;
#30442=CARTESIAN_POINT ( 'NONE',  ( -3.000000000000000000, 5.835314593368772229, -22.81335362449846826 ) ) ;
#30458=LINE ( 'NONE', #8659, #58106 ) ;
#30461=DIRECTION ( 'NONE',  ( 0.000000000000000000, 0.4067366430757888285, 0.9135454576426060846 ) ) ;
#30465=CIRCLE ( 'NONE', #72487, 16.00000000000000000 ) ;
#30490=VECTOR ( 'NONE', #41479, 1000.000000000000000 ) ;
#30492=ORIENTED_EDGE ( 'NONE', *, *, #40779, .F. ) ;
#30498=LINE ( 'NONE', #24148, #22126 ) ;
#30501=CARTESIAN_POINT ( 'NONE',  ( 10.00000000000000000, -6.736453364083292428, -36.88895765772640800 ) ) ;
#30509=FACE_OUTER_BOUND ( 'NONE', #65600, .T. ) ;
#30530=LINE ( 'NONE', #66251, #50575 ) ;
#30538=EDGE_CURVE ( 'NONE', #7056, #46924, #57489, .T. ) ;
#30555=DIRECTION ( 'NONE',  ( -1.000000000000000000, -0.000000000000000000, -0.000000000000000000 ) ) ;
#30557=AXIS2_PLACEMENT_3D ( 'NONE', #58672, #53768, #24105 ) ;
#30566=ORIENTED_EDGE ( 'NONE', *, *, #17647, .T. ) ;
#30568=CYLINDRICAL_SURFACE ( 'NONE', #19016, 16.00000000000000000 ) ;
#30570=EDGE_CURVE ( 'NONE', #68033, #22414, #40200, .T. ) ;
#30574=ORIENTED_EDGE ( 'NONE', *, *, #63190, .T. ) ;
#30582=ORIENTED_EDGE ( 'NONE', *, *, #27544, .T. ) ;
#30583=ORIENTED_EDGE ( 'NONE', *, *, #68774, .F. ) ;
#30584=VERTEX_POINT ( 'NONE', #34543 ) ;
#30587=ORIENTED_EDGE ( 'NONE', *, *, #72526, .F. ) ;
#30612=DIRECTION ( 'NONE',  ( 0.000000000000000000, -0.9876883405951361050, -0.1564344650402419989 ) ) ;
#30614=FACE_OUTER_BOUND ( 'NONE', #31721, .T. ) ;
#30616=FACE_OUTER_BOUND ( 'NONE', #58073, .T. ) ;
#30617=CYLINDRICAL_SURFACE ( 'NONE', #5435, 16.00000000000000000 ) ;
#30624=CIRCLE ( 'NONE', #46258, 16.00000000000000355 ) ;
#30630=CARTESIAN_POINT ( 'NONE',  ( 0.000000000000000000, -21.53537804866103045, 30.80686688397002371 ) ) ;
#30636=DIRECTION ( 'NONE',  ( -1.000000000000000000, 0.000000000000000000, -0.000000000000000000 ) ) ;
#30642=CARTESIAN_POINT ( 'NONE',  ( 10.00000000000000000, -17.67226234102801286, -33.17418723428327354 ) ) ;
#30673=LINE ( 'NONE', #64537, #44789 ) ;
#30676=CARTESIAN_POINT ( 'NONE',  ( 10.00000000000000000, 0.000000000000000000, 0.000000000000000000 ) ) ;
#30688=CARTESIAN_POINT ( 'NONE',  ( 10.00000000000000000, -33.00180498840035170, -17.80606268964575278 ) ) ;
#30692=ORIENTED_EDGE ( 'NONE', *, *, #31414, .F. ) ;
#30693=CARTESIAN_POINT ( 'NONE',  ( 5.000000000000000000, 3.925862922256160736, 41.81611651403863306 ) ) ;
#30694=VERTEX_POINT ( 'NONE', #24 ) ;
#30696=EDGE_CURVE ( 'NONE', #49620, #26331, #13158, .T. ) ;
#30706=ORIENTED_EDGE ( 'NONE', *, *, #32725, .T. ) ;
#30713=CARTESIAN_POINT ( 'NONE',  ( 0.000000000000000000, 20.85821328998741109, 10.92862929874522315 ) ) ;
#30744=LINE ( 'NONE', #25490, #73855 ) ;
#30753=EDGE_CURVE ( 'NONE', #62900, #50450, #57562, .T. ) ;
#30754=VERTEX_POINT ( 'NONE', #36024 ) ;
#30756=DIRECTION ( 'NONE',  ( -1.000000000000000000, -0.000000000000000000, -0.000000000000000000 ) ) ;
#30786=( LENGTH_UNIT ( ) NAMED_UNIT ( * ) SI_UNIT ( .MILLI., .METRE. ) );
#30824=UNCERTAINTY_MEASURE_WITH_UNIT (LENGTH_MEASURE( 1.000000000000000082E-05 ), #31507, 'distance_accuracy_value', 'NONE');
#30827=CARTESIAN_POINT ( 'NONE',  ( 0.000000000000000000, -6.736453364083817341, 36.88895765772630142 ) ) ;
#30839=CARTESIAN_POINT ( 'NONE',  ( 0.000000000000000000, 31.52238457039599595, 27.75498641678753842 ) ) ;
#30848=EDGE_CURVE ( 'NONE', #36342, #54986, #22789, .T. ) ;
#30855=EDGE_CURVE ( 'NONE', #26546, #24685, #34739, .T. ) ;
#30865=ORIENTED_EDGE ( 'NONE', *, *, #57236, .F. ) ;
#30877=DIRECTION ( 'NONE',  ( 0.000000000000000000, 0.000000000000000000, -1.000000000000000000 ) ) ;
#30881=PLANE ( 'NONE',  #49779 ) ;
#30888=ORIENTED_EDGE ( 'NONE', *, *, #67264, .T. ) ;
#30910=CARTESIAN_POINT ( 'NONE',  ( -3.000000000000000000, -26.23277895567245821, -4.042438405570103477 ) ) ;
#30914=ORIENTED_EDGE ( 'NONE', *, *, #1737, .T. ) ;
#30921=VECTOR ( 'NONE', #3212, 1000.000000000000000 ) ;
#30927=DIRECTION ( 'NONE',  ( 0.000000000000000000, 0.000000000000000000, 1.000000000000000000 ) ) ;
#30933=CARTESIAN_POINT ( 'NONE',  ( -3.000000000000000000, -20.55727247249748046, 16.78983467731285018 ) ) ;
#30943=DIRECTION ( 'NONE',  ( -1.000000000000000000, 0.000000000000000000, 0.000000000000000000 ) ) ;
#30953=EDGE_CURVE ( 'NONE', #23374, #68543, #70841, .T. ) ;
#30963=ORIENTED_EDGE ( 'NONE', *, *, #36941, .F. ) ;
#30967=LINE ( 'NONE', #59942, #32236 ) ;
#30971=AXIS2_PLACEMENT_3D ( 'NONE', #35093, #58769, #51259 ) ;
#30973=DIRECTION ( 'NONE',  ( -1.000000000000000000, 0.000000000000000000, -0.000000000000000000 ) ) ;
#30982=SHAPE_REPRESENTATION ( 'fast gear_ISO - Spur gear 2M 40T 20PA 10FW ---S40A75H50L38.0N', ( #43395 ), #39845 ) ;
#30989=DIRECTION ( 'NONE',  ( -1.000000000000000000, 0.000000000000000000, -0.000000000000000000 ) ) ;
#30992=EDGE_CURVE ( 'NONE', #42410, #17471, #41936, .T. ) ;
#31009=LINE ( 'NONE', #71227, #61877 ) ;
#31023=CARTESIAN_POINT ( 'NONE',  ( 10.00000000000000000, -41.91543099594819921, 2.663952781846001816 ) ) ;
#31034=VERTEX_POINT ( 'NONE', #2481 ) ;
#31048=CIRCLE ( 'NONE', #8251, 37.49900000000000233 ) ;
#31050=EDGE_CURVE ( 'NONE', #10635, #66514, #7698, .T. ) ;
#31060=CARTESIAN_POINT ( 'NONE',  ( 0.000000000000000000, -35.95386929396248377, -10.96151621346525751 ) ) ;
#31062=EDGE_CURVE ( 'NONE', #57306, #1695, #24619, .T. ) ;
#31063=ORIENTED_EDGE ( 'NONE', *, *, #74327, .T. ) ;
#31068=DIRECTION ( 'NONE',  ( 0.000000000000000000, -0.4067366430757881068, -0.9135454576426063067 ) ) ;
#31080=ADVANCED_FACE ( 'NONE', ( #30614 ), #47923, .T. ) ;
#31083=ORIENTED_EDGE ( 'NONE', *, *, #66895, .T. ) ;
#31089=LINE ( 'NONE', #64573, #8911 ) ;
#31120=EDGE_CURVE ( 'NONE', #3329, #13842, #26465, .T. ) ;
#31132=ORIENTED_EDGE ( 'NONE', *, *, #64527, .T. ) ;
#31139=SURFACE_STYLE_USAGE ( .BOTH. , #72101 ) ;
#31160=ORIENTED_EDGE ( 'NONE', *, *, #73847, .F. ) ;
#31166=CARTESIAN_POINT ( 'NONE',  ( 0.000000000000000000, 0.000000000000000000, 0.000000000000000000 ) ) ;
#31186=DIRECTION ( 'NONE',  ( 0.000000000000000000, 0.9135454576426060846, -0.4067366430757888285 ) ) ;
#31190=DIRECTION ( 'NONE',  ( 0.000000000000000000, -0.7431448254773954654, 0.6691306063588569053 ) ) ;
#31196=EDGE_CURVE ( 'NONE', #35036, #32855, #55786, .T. ) ;
#31202=AXIS2_PLACEMENT_3D ( 'NONE', #7053, #25087, #12688 ) ;
#31205=AXIS2_PLACEMENT_3D ( 'NONE', #37749, #32821, #21931 ) ;
#31226=CARTESIAN_POINT ( 'NONE',  ( 10.00000000000000000, 40.68715046381928602, 10.41901085202092503 ) ) ;
#31235=DIRECTION ( 'NONE',  ( -1.000000000000000000, 0.000000000000000000, 0.000000000000000000 ) ) ;
#31243=ORIENTED_EDGE ( 'NONE', *, *, #27484, .T. ) ;
#31245=DIRECTION ( 'NONE',  ( -1.000000000000000000, -0.000000000000000000, 0.000000000000000000 ) ) ;
#31252=VERTEX_POINT ( 'NONE', #55038 ) ;
#31264=DIRECTION ( 'NONE',  ( 0.000000000000000000, -0.4067366430758009854, 0.9135454576426004225 ) ) ;
#31273=DIRECTION ( 'NONE',  ( -0.000000000000000000, 0.8090169943749498938, -0.5877852522924696954 ) ) ;
#31276=CARTESIAN_POINT ( 'NONE',  ( 10.00000000000000000, 0.000000000000000000, 0.000000000000000000 ) ) ;
#31280=FACE_OUTER_BOUND ( 'NONE', #57463, .T. ) ;
#31283=CARTESIAN_POINT ( 'NONE',  ( 10.00000000000000000, -15.48615015657610883, 39.04073710021339139 ) ) ;
#31287=DIRECTION ( 'NONE',  ( -1.000000000000000000, 0.000000000000000000, 0.000000000000000000 ) ) ;
#31295=CARTESIAN_POINT ( 'NONE',  ( 10.00000000000000000, 16.45098606841173705, -33.79645857604496229 ) ) ;
#31296=DIRECTION ( 'NONE',  ( -1.000000000000000000, 0.000000000000000000, 0.000000000000000000 ) ) ;
#31304=CARTESIAN_POINT ( 'NONE',  ( 0.000000000000000000, 0.6853352020795618893, -37.58145647212453611 ) ) ;
#31308=EDGE_CURVE ( 'NONE', #55937, #67975, #33526, .T. ) ;
#31322=LINE ( 'NONE', #33913, #32781 ) ;
#31323=EDGE_CURVE ( 'NONE', #32002, #20059, #15503, .T. ) ;
#31329=ORIENTED_EDGE ( 'NONE', *, *, #59831, .T. ) ;
#31334=ORIENTED_EDGE ( 'NONE', *, *, #71868, .T. ) ;
#31339=VECTOR ( 'NONE', #61082, 1000.000000000000000 ) ;
#31344=ORIENTED_EDGE ( 'NONE', *, *, #4159, .T. ) ;
#31349=CARTESIAN_POINT ( 'NONE',  ( -3.000000000000000000, -19.89357724624987256, -12.59942793731086041 ) ) ;
#31359=DIRECTION ( 'NONE',  ( -0.000000000000000000, 0.9510565162951539753, -0.3090169943749460635 ) ) ;
#31367=VERTEX_POINT ( 'NONE', #27893 ) ;
#31377=ORIENTED_EDGE ( 'NONE', *, *, #11205, .F. ) ;
#31391=EDGE_CURVE ( 'NONE', #15350, #47006, #22265, .T. ) ;
#31395=ORIENTED_EDGE ( 'NONE', *, *, #52474, .F. ) ;
#31397=( GEOMETRIC_REPRESENTATION_CONTEXT ( 3 ) GLOBAL_UNCERTAINTY_ASSIGNED_CONTEXT ( ( #39185 ) ) GLOBAL_UNIT_ASSIGNED_CONTEXT ( ( #30786, #19513, #13133 ) ) REPRESENTATION_CONTEXT ( 'NONE', 'WORKASPACE' ) );
#31406=CIRCLE ( 'NONE', #61427, 16.00000000000000000 ) ;
#31409=EDGE_CURVE ( 'NONE', #23719, #68440, #20774, .T. ) ;
#31414=EDGE_CURVE ( 'NONE', #1375, #49986, #28295, .T. ) ;
#31421=DIRECTION ( 'NONE',  ( 0.000000000000000000, -0.7071067811865535679, 0.7071067811865413555 ) ) ;
#31422=EDGE_CURVE ( 'NONE', #14697, #16651, #42749, .T. ) ;
#31430=ORIENTED_EDGE ( 'NONE', *, *, #24602, .T. ) ;
#31441=VERTEX_POINT ( 'NONE', #16998 ) ;
#31468=ADVANCED_FACE ( 'NONE', ( #45585 ), #69959, .F. ) ;
#31477=DIRECTION ( 'NONE',  ( 0.000000000000000000, 0.000000000000000000, 1.000000000000000000 ) ) ;
#31493=DIRECTION ( 'NONE',  ( -1.000000000000000000, -0.000000000000000000, 0.000000000000000000 ) ) ;
#31496=EDGE_CURVE ( 'NONE', #24127, #67018, #4339, .T. ) ;
#31500=ORIENTED_EDGE ( 'NONE', *, *, #45860, .T. ) ;
#31505=DIRECTION ( 'NONE',  ( -1.000000000000000000, -0.000000000000000000, -0.000000000000000000 ) ) ;
#31507=( LENGTH_UNIT ( ) NAMED_UNIT ( * ) SI_UNIT ( .MILLI., .METRE. ) );
#31542=FACE_OUTER_BOUND ( 'NONE', #55315, .T. ) ;
#31553=DIRECTION ( 'NONE',  ( -0.000000000000000000, 0.9781476007338069101, -0.2079116908177532363 ) ) ;
#31567=LINE ( 'NONE', #15019, #16342 ) ;
#31578=DIRECTION ( 'NONE',  ( 0.000000000000000000, -0.5000000000000046629, 0.8660254037844359321 ) ) ;
#31579=EDGE_CURVE ( 'NONE', #32561, #1816, #72718, .T. ) ;
#31617=CIRCLE ( 'NONE', #14835, 37.49900000000001654 ) ;
#31624=ORIENTED_EDGE ( 'NONE', *, *, #3434, .F. ) ;
#31625=CARTESIAN_POINT ( 'NONE',  ( -3.000000000000000000, 0.000000000000000000, 0.000000000000000000 ) ) ;
#31630=CARTESIAN_POINT ( 'NONE',  ( 10.00000000000000000, 0.000000000000000000, 0.000000000000000000 ) ) ;
#31640=CARTESIAN_POINT ( 'NONE',  ( -3.000000000000000000, -25.60904388321925396, 6.976881207771172377 ) ) ;
#31641=CARTESIAN_POINT ( 'NONE',  ( 10.00000000000000000, -16.23288003029521320, 33.80338159004277543 ) ) ;
#31645=LINE ( 'NONE', #20375, #42702 ) ;
#31648=EDGE_LOOP ( 'NONE', ( #6404, #13062, #18858, #42146 ) ) ;
#31651=CARTESIAN_POINT ( 'NONE',  ( 0.000000000000000000, 0.000000000000000000, 0.000000000000000000 ) ) ;
#31653=CARTESIAN_POINT ( 'NONE',  ( 10.00000000000000000, 33.79645857604513992, 16.45098606841138178 ) ) ;
#31666=DIRECTION ( 'NONE',  ( 0.000000000000000000, 0.000000000000000000, 1.000000000000000000 ) ) ;
#31677=ORIENTED_EDGE ( 'NONE', *, *, #55750, .T. ) ;
#31691=CARTESIAN_POINT ( 'NONE',  ( 4.999999999999999112, 36.13751322684449008, -21.40280677340332716 ) ) ;
#31698=AXIS2_PLACEMENT_3D ( 'NONE', #13437, #41635, #18335 ) ;
#31705=ADVANCED_FACE ( 'NONE', ( #42154 ), #26599, .T. ) ;
#31712=CARTESIAN_POINT ( 'NONE',  ( -3.000000000000000000, 23.50000000000000000, -1.500000000000001332 ) ) ;
#31719=EDGE_CURVE ( 'NONE', #40423, #44983, #63157, .T. ) ;
#31721=EDGE_LOOP ( 'NONE', ( #46454, #25586, #32783, #6204 ) ) ;
#31730=CARTESIAN_POINT ( 'NONE',  ( 10.00000000000000000, 0.000000000000000000, 0.000000000000000000 ) ) ;
#31736=CYLINDRICAL_SURFACE ( 'NONE', #68309, 16.00000000000000000 ) ;
#31740=DIRECTION ( 'NONE',  ( -1.000000000000000000, 0.000000000000000000, 0.000000000000000000 ) ) ;
#31744=LINE ( 'NONE', #47934, #36356 ) ;
#31768=AXIS2_PLACEMENT_3D ( 'NONE', #32254, #14603, #26621 ) ;
#31780=CARTESIAN_POINT ( 'NONE',  ( 10.00000000000000000, -35.38097989696503021, -12.42422080174676147 ) ) ;
#31785=CARTESIAN_POINT ( 'NONE',  ( 0.000000000000000000, -37.22597642581153821, -5.202137450156795850 ) ) ;
#31789=EDGE_CURVE ( 'NONE', #26822, #52685, #27720, .T. ) ;
#31799=CARTESIAN_POINT ( 'NONE',  ( -3.000000000000000000, 0.000000000000000000, 0.000000000000000000 ) ) ;
#31817=ORIENTED_EDGE ( 'NONE', *, *, #19629, .F. ) ;
#31845=CARTESIAN_POINT ( 'NONE',  ( 0.000000000000000000, 0.000000000000000000, 0.000000000000000000 ) ) ;
#31859=CIRCLE ( 'NONE', #73462, 16.00000000000000355 ) ;
#31872=CARTESIAN_POINT ( 'NONE',  ( 10.00000000000000000, 0.000000000000000000, 0.000000000000000000 ) ) ;
#31875=FACE_OUTER_BOUND ( 'NONE', #53263, .T. ) ;
#31877=EDGE_LOOP ( 'NONE', ( #52211, #56713, #52410, #33786 ) ) ;
#31882=ORIENTED_EDGE ( 'NONE', *, *, #30992, .T. ) ;
#31910=ORIENTED_EDGE ( 'NONE', *, *, #61726, .T. ) ;
#31921=VERTEX_POINT ( 'NONE', #70506 ) ;
#31923=CARTESIAN_POINT ( 'NONE',  ( -3.000000000000000000, -0.9646360437372163421, -23.52805723605591126 ) ) ;
#31933=FACE_OUTER_BOUND ( 'NONE', #24523, .T. ) ;
#31952=CARTESIAN_POINT ( 'NONE',  ( 0.000000000000000000, 12.42422080174638310, 35.38097989696515810 ) ) ;
#31955=FACE_OUTER_BOUND ( 'NONE', #44019, .T. ) ;
#31957=ORIENTED_EDGE ( 'NONE', *, *, #41430, .F. ) ;
#31965=ORIENTED_EDGE ( 'NONE', *, *, #47630, .T. ) ;
#31976=DIRECTION ( 'NONE',  ( 1.000000000000000000, 0.000000000000000000, 0.000000000000000000 ) ) ;
#31977=EDGE_CURVE ( 'NONE', #27109, #46417, #63549, .T. ) ;
#31980=VERTEX_POINT ( 'NONE', #18646 ) ;
#31995=VERTEX_POINT ( 'NONE', #2148 ) ;
#32002=VERTEX_POINT ( 'NONE', #63428 ) ;
#32004=VERTEX_POINT ( 'NONE', #11902 ) ;
#32005=CARTESIAN_POINT ( 'NONE',  ( 10.00000000000000000, -39.04073710021356192, 15.48615015657568250 ) ) ;
#32016=EDGE_CURVE ( 'NONE', #47415, #26822, #9222, .T. ) ;
#32018=EDGE_LOOP ( 'NONE', ( #42066, #15619, #9251, #68570 ) ) ;
#32020=DIRECTION ( 'NONE',  ( -1.000000000000000000, 0.000000000000000000, 0.000000000000000000 ) ) ;
#32033=CARTESIAN_POINT ( 'NONE',  ( 10.00000000000000000, 0.000000000000000000, 0.000000000000000000 ) ) ;
#32034=AXIS2_PLACEMENT_3D ( 'NONE', #45459, #35269, #52547 ) ;
#32055=CIRCLE ( 'NONE', #74089, 42.00000000000000000 ) ;
#32062=ADVANCED_FACE ( 'NONE', ( #37449 ), #3620, .T. ) ;
#32082=DIRECTION ( 'NONE',  ( 0.000000000000000000, 0.000000000000000000, 1.000000000000000000 ) ) ;
#32122=DIRECTION ( 'NONE',  ( -1.000000000000000000, -0.000000000000000000, -0.000000000000000000 ) ) ;
#32139=CARTESIAN_POINT ( 'NONE',  ( 5.000000000000000000, -27.75498641678720446, -31.52238457039628727 ) ) ;
#32147=VECTOR ( 'NONE', #63967, 1000.000000000000000 ) ;
#32153=EDGE_CURVE ( 'NONE', #41196, #63433, #40565, .T. ) ;
#32163=CARTESIAN_POINT ( 'NONE',  ( 4.999999999999999112, 41.81611651403861885, 3.925862922256313503 ) ) ;
#32164=VECTOR ( 'NONE', #18683, 1000.000000000000000 ) ;
#32167=CIRCLE ( 'NONE', #15383, 42.00000000000000000 ) ;
#32169=CIRCLE ( 'NONE', #6965, 16.00000000000000000 ) ;
#32187=CARTESIAN_POINT ( 'NONE',  ( -10.00000000000000000, 0.000000000000000000, 0.000000000000000000 ) ) ;
#32191=LINE ( 'NONE', #27585, #22311 ) ;
#32200=AXIS2_PLACEMENT_3D ( 'NONE', #62103, #69589, #23001 ) ;
#32216=EDGE_CURVE ( 'NONE', #41287, #58363, #62226, .T. ) ;
#32221=DIRECTION ( 'NONE',  ( 1.000000000000000000, -0.000000000000000000, -0.000000000000000000 ) ) ;
#32224=CARTESIAN_POINT ( 'NONE',  ( 5.000000000000000000, 15.48615015657581750, 39.04073710021349797 ) ) ;
#32225=CYLINDRICAL_SURFACE ( 'NONE', #2400, 37.49900000000000233 ) ;
#32231=ORIENTED_EDGE ( 'NONE', *, *, #25693, .F. ) ;
#32232=CARTESIAN_POINT ( 'NONE',  ( 0.000000000000000000, 0.000000000000000000, 0.000000000000000000 ) ) ;
#32236=VECTOR ( 'NONE', #13680, 1000.000000000000000 ) ;
#32238=DIRECTION ( 'NONE',  ( -1.000000000000000000, 0.000000000000000000, 0.000000000000000000 ) ) ;
#32248=CARTESIAN_POINT ( 'NONE',  ( -3.000000000000000000, -22.67460108101774807, -6.353146135318215038 ) ) ;
#32254=CARTESIAN_POINT ( 'NONE',  ( 0.000000000000000000, 30.80686688397010542, 21.53537804866092387 ) ) ;
#32275=DIRECTION ( 'NONE',  ( -1.000000000000000000, -0.000000000000000000, 0.000000000000000000 ) ) ;
#32306=EDGE_CURVE ( 'NONE', #68440, #69078, #27994, .T. ) ;
#32310=VECTOR ( 'NONE', #6713, 1000.000000000000000 ) ;
#32319=DIRECTION ( 'NONE',  ( -1.000000000000000000, -0.000000000000000000, 0.000000000000000000 ) ) ;
#32323=VECTOR ( 'NONE', #23144, 1000.000000000000000 ) ;
#32331=VERTEX_POINT ( 'NONE', #29464 ) ;
#32335=ORIENTED_EDGE ( 'NONE', *, *, #47392, .F. ) ;
#32337=ORIENTED_EDGE ( 'NONE', *, *, #3686, .F. ) ;
#32352=VERTEX_POINT ( 'NONE', #24582 ) ;
#32355=VERTEX_POINT ( 'NONE', #13297 ) ;
#32359=ORIENTED_EDGE ( 'NONE', *, *, #64968, .T. ) ;
#32376=CARTESIAN_POINT ( 'NONE',  ( 10.00000000000000000, -21.53537804866103045, 30.80686688397002371 ) ) ;
#32377=DIRECTION ( 'NONE',  ( 1.000000000000000000, -0.000000000000000000, 0.000000000000000000 ) ) ;
#32403=ADVANCED_FACE ( 'NONE', ( #47516 ), #584, .T. ) ;
#32410=FACE_OUTER_BOUND ( 'NONE', #52330, .T. ) ;
#32417=CARTESIAN_POINT ( 'NONE',  ( 0.000000000000000000, 26.08949754953062694, -27.05870788708203989 ) ) ;
#32431=CIRCLE ( 'NONE', #2447, 42.00000000000000000 ) ;
#32435=AXIS2_PLACEMENT_3D ( 'NONE', #38501, #72334, #43786 ) ;
#32455=DIRECTION ( 'NONE',  ( 0.000000000000000000, 0.1564344650402313408, -0.9876883405951376593 ) ) ;
#32465=ORIENTED_EDGE ( 'NONE', *, *, #12545, .T. ) ;
#32474=CARTESIAN_POINT ( 'NONE',  ( 10.00000000000000000, -21.32104025579135964, 30.84782396557210760 ) ) ;
#32477=CIRCLE ( 'NONE', #28895, 16.00000000000000355 ) ;
#32493=LINE ( 'NONE', #26491, #54681 ) ;
#32496=EDGE_CURVE ( 'NONE', #70917, #51144, #53805, .T. ) ;
#32499=CARTESIAN_POINT ( 'NONE',  ( 10.00000000000000000, 22.74946021919175720, -29.81001611430984255 ) ) ;
#32534=VERTEX_POINT ( 'NONE', #20788 ) ;
#32539=AXIS2_PLACEMENT_3D ( 'NONE', #46832, #12601, #18245 ) ;
#32545=DIRECTION ( 'NONE',  ( -1.000000000000000000, 0.000000000000000000, 0.000000000000000000 ) ) ;
#32548=ORIENTED_EDGE ( 'NONE', *, *, #8498, .T. ) ;
#32558=DIRECTION ( 'NONE',  ( 0.000000000000000000, 0.5877852522924689183, 0.8090169943749504489 ) ) ;
#32561=VERTEX_POINT ( 'NONE', #25690 ) ;
#32564=ORIENTED_EDGE ( 'NONE', *, *, #2727, .T. ) ;
#32573=CYLINDRICAL_SURFACE ( 'NONE', #15303, 16.00000000000000000 ) ;
#32586=LINE ( 'NONE', #2949, #48153 ) ;
#32589=FACE_OUTER_BOUND ( 'NONE', #59374, .T. ) ;
#32592=EDGE_CURVE ( 'NONE', #31980, #74050, #65555, .T. ) ;
#32602=EDGE_CURVE ( 'NONE', #15417, #8203, #14408, .T. ) ;
#32616=DIRECTION ( 'NONE',  ( 0.000000000000000000, 0.000000000000000000, 1.000000000000000000 ) ) ;
#32621=EDGE_LOOP ( 'NONE', ( #10576, #33100, #65847, #12761 ) ) ;
#32627=ORIENTED_EDGE ( 'NONE', *, *, #39463, .F. ) ;
#32633=CIRCLE ( 'NONE', #291, 15.99999999999999645 ) ;
#32636=ORIENTED_EDGE ( 'NONE', *, *, #10502, .T. ) ;
#32655=CYLINDRICAL_SURFACE ( 'NONE', #3488, 16.00000000000000000 ) ;
#32665=LINE ( 'NONE', #22143, #10221 ) ;
#32670=CYLINDRICAL_SURFACE ( 'NONE', #53218, 37.49900000000000233 ) ;
#32671=DIRECTION ( 'NONE',  ( 0.000000000000000000, 0.000000000000000000, 1.000000000000000000 ) ) ;
#32674=DIRECTION ( 'NONE',  ( -0.000000000000000000, 0.7431448254773946882, -0.6691306063588577935 ) ) ;
#32677=CARTESIAN_POINT ( 'NONE',  ( 0.000000000000000000, -10.74501242461307982, 35.92658777277507198 ) ) ;
#32681=CIRCLE ( 'NONE', #15899, 16.00000000000000355 ) ;
#32684=EDGE_CURVE ( 'NONE', #73246, #26822, #9510, .T. ) ;
#32685=AXIS2_PLACEMENT_3D ( 'NONE', #73526, #15660, #66784 ) ;
#32688=FACE_OUTER_BOUND ( 'NONE', #64645, .T. ) ;
#32715=DIRECTION ( 'NONE',  ( 1.000000000000000000, -0.000000000000000000, -0.000000000000000000 ) ) ;
#32716=ORIENTED_EDGE ( 'NONE', *, *, #13261, .T. ) ;
#32720=VERTEX_POINT ( 'NONE', #62133 ) ;
#32725=EDGE_CURVE ( 'NONE', #55313, #24224, #32167, .T. ) ;
#32731=DIRECTION ( 'NONE',  ( 0.000000000000000000, 0.4539904997395414754, 0.8910065241883706744 ) ) ;
#32733=ORIENTED_EDGE ( 'NONE', *, *, #31496, .F. ) ;
#32750=ORIENTED_EDGE ( 'NONE', *, *, #68176, .F. ) ;
#32757=CARTESIAN_POINT ( 'NONE',  ( 10.00000000000000000, 0.000000000000000000, 0.000000000000000000 ) ) ;
#32776=ORIENTED_EDGE ( 'NONE', *, *, #2499, .T. ) ;
#32780=DIRECTION ( 'NONE',  ( -1.000000000000000000, 0.000000000000000000, 0.000000000000000000 ) ) ;
#32781=VECTOR ( 'NONE', #40298, 1000.000000000000000 ) ;
#32782=CARTESIAN_POINT ( 'NONE',  ( 5.000000000000000000, 22.48208911017551870, -35.47612816024499693 ) ) ;
#32783=ORIENTED_EDGE ( 'NONE', *, *, #29514, .T. ) ;
#32784=CARTESIAN_POINT ( 'NONE',  ( 10.00000000000000000, -35.95386929396264009, 10.96151621346475658 ) ) ;
#32788=DIRECTION ( 'NONE',  ( 0.000000000000000000, -0.9876883405951393247, 0.1564344650402204329 ) ) ;
#32789=CARTESIAN_POINT ( 'NONE',  ( -3.000000000000000000, -4.261787119644969479, -26.19803753235780519 ) ) ;
#32803=VERTEX_POINT ( 'NONE', #6828 ) ;
#32810=EDGE_CURVE ( 'NONE', #33855, #51707, #33454, .T. ) ;
#32821=DIRECTION ( 'NONE',  ( -1.000000000000000000, 0.000000000000000000, -0.000000000000000000 ) ) ;
#32824=EDGE_CURVE ( 'NONE', #33925, #37934, #6476, .T. ) ;
#32828=AXIS2_PLACEMENT_3D ( 'NONE', #59470, #36160, #18861 ) ;
#32832=DIRECTION ( 'NONE',  ( 0.000000000000000000, -0.8910065241883721177, 0.4539904997395382003 ) ) ;
#32833=CARTESIAN_POINT ( 'NONE',  ( 10.00000000000000000, 0.000000000000000000, 0.000000000000000000 ) ) ;
#32840=CARTESIAN_POINT ( 'NONE',  ( 0.000000000000000000, -32.34446384429989507, 26.79245525562703278 ) ) ;
#32847=CARTESIAN_POINT ( 'NONE',  ( 10.00000000000000000, -31.52238457039619490, 27.75498641678731104 ) ) ;
#32853=CIRCLE ( 'NONE', #61682, 42.00000000000000000 ) ;
#32854=DIRECTION ( 'NONE',  ( 0.000000000000000000, -0.9510565162951565288, 0.3090169943749383474 ) ) ;
#32855=VERTEX_POINT ( 'NONE', #34288 ) ;
#32857=CARTESIAN_POINT ( 'NONE',  ( 10.00000000000000000, 0.000000000000000000, 0.000000000000000000 ) ) ;
#32862=CARTESIAN_POINT ( 'NONE',  ( 10.00000000000000000, -35.95386929396248377, -10.96151621346525751 ) ) ;
#32863=DIRECTION ( 'NONE',  ( 0.000000000000000000, -0.8090169943749422332, -0.5877852522924803536 ) ) ;
#32866=DIRECTION ( 'NONE',  ( 0.000000000000000000, 0.8090169943749447867, 0.5877852522924769119 ) ) ;
#32881=ORIENTED_EDGE ( 'NONE', *, *, #42354, .T. ) ;
#32882=DIRECTION ( 'NONE',  ( -1.000000000000000000, 0.000000000000000000, -0.000000000000000000 ) ) ;
#32891=DIRECTION ( 'NONE',  ( -1.000000000000000000, 0.000000000000000000, 0.000000000000000000 ) ) ;
#32899=EDGE_CURVE ( 'NONE', #65222, #13949, #7074, .T. ) ;
#32917=EDGE_CURVE ( 'NONE', #44329, #26982, #61065, .T. ) ;
#32926=ORIENTED_EDGE ( 'NONE', *, *, #19362, .F. ) ;
#32927=PLANE ( 'NONE',  #26678 ) ;
#32928=DIRECTION ( 'NONE',  ( -1.000000000000000000, -0.000000000000000000, 0.000000000000000000 ) ) ;
#32931=ORIENTED_EDGE ( 'NONE', *, *, #33528, .T. ) ;
#32935=CARTESIAN_POINT ( 'NONE',  ( -3.000000000000000000, 18.84667830672579925, 18.68964196561269020 ) ) ;
#32938=ORIENTED_EDGE ( 'NONE', *, *, #66617, .F. ) ;
#32940=ORIENTED_EDGE ( 'NONE', *, *, #66656, .F. ) ;
#32954=CIRCLE ( 'NONE', #40169, 16.00000000000000000 ) ;
#32963=DIRECTION ( 'NONE',  ( -1.000000000000000000, -0.000000000000000000, -0.000000000000000000 ) ) ;
#32972=VECTOR ( 'NONE', #63839, 1000.000000000000000 ) ;
#32976=EDGE_CURVE ( 'NONE', #16651, #27107, #18838, .T. ) ;
#32977=ORIENTED_EDGE ( 'NONE', *, *, #37621, .F. ) ;
#32983=DIRECTION ( 'NONE',  ( -1.000000000000000000, -0.000000000000000000, 0.000000000000000000 ) ) ;
#32987=EDGE_CURVE ( 'NONE', #20918, #39053, #57479, .T. ) ;
#32998=CYLINDRICAL_SURFACE ( 'NONE', #18564, 21.00000000000000000 ) ;
#33003=ORIENTED_EDGE ( 'NONE', *, *, #24936, .F. ) ;
#33005=ORIENTED_EDGE ( 'NONE', *, *, #7958, .F. ) ;
#33012=ORIENTED_EDGE ( 'NONE', *, *, #4812, .T. ) ;
#33020=VERTEX_POINT ( 'NONE', #66924 ) ;
#33025=EDGE_CURVE ( 'NONE', #44604, #46613, #27440, .T. ) ;
#33043=CARTESIAN_POINT ( 'NONE',  ( 10.00000000000000000, 0.000000000000000000, 0.000000000000000000 ) ) ;
#33045=DIRECTION ( 'NONE',  ( -1.000000000000000000, 0.000000000000000000, 0.000000000000000000 ) ) ;
#33055=AXIS2_PLACEMENT_3D ( 'NONE', #46492, #40867, #35207 ) ;
#33075=VECTOR ( 'NONE', #29413, 1000.000000000000000 ) ;
#33086=ORIENTED_EDGE ( 'NONE', *, *, #50737, .T. ) ;
#33100=ORIENTED_EDGE ( 'NONE', *, *, #43379, .F. ) ;
#33115=CIRCLE ( 'NONE', #60777, 37.49900000000000944 ) ;
#33122=CARTESIAN_POINT ( 'NONE',  ( -3.000000000000000000, 14.60985201121704513, 18.46759930825707841 ) ) ;
#33128=DIRECTION ( 'NONE',  ( 0.000000000000000000, 1.000000000000000000, 3.491481338843133750E-15 ) ) ;
#33137=FACE_OUTER_BOUND ( 'NONE', #43323, .T. ) ;
#33141=AXIS2_PLACEMENT_3D ( 'NONE', #8679, #72544, #25958 ) ;
#33147=DIRECTION ( 'NONE',  ( -1.000000000000000000, -0.000000000000000000, -0.000000000000000000 ) ) ;
#33150=ORIENTED_EDGE ( 'NONE', *, *, #23673, .F. ) ;
#33172=ORIENTED_EDGE ( 'NONE', *, *, #66617, .T. ) ;
#33174=ORIENTED_EDGE ( 'NONE', *, *, #61681, .T. ) ;
#33196=CARTESIAN_POINT ( 'NONE',  ( 10.00000000000000000, 37.22597642581158084, -5.202137450156524068 ) ) ;
#33207=FACE_OUTER_BOUND ( 'NONE', #18774, .T. ) ;
#33238=DIRECTION ( 'NONE',  ( 0.000000000000000000, 0.000000000000000000, 1.000000000000000000 ) ) ;
#33243=EDGE_CURVE ( 'NONE', #64733, #74246, #64709, .T. ) ;
#33248=ORIENTED_EDGE ( 'NONE', *, *, #53324, .T. ) ;
#33251=EDGE_LOOP ( 'NONE', ( #27741, #32776, #74201, #16266 ) ) ;
#33269=ORIENTED_EDGE ( 'NONE', *, *, #7478, .T. ) ;
#33278=VECTOR ( 'NONE', #46023, 1000.000000000000000 ) ;
#33284=EDGE_LOOP ( 'NONE', ( #35495, #65230, #25506, #35086 ) ) ;
#33292=DIRECTION ( 'NONE',  ( 0.000000000000000000, 0.5877852522924744694, -0.8090169943749465631 ) ) ;
#33297=FACE_OUTER_BOUND ( 'NONE', #6023, .T. ) ;
#33313=CARTESIAN_POINT ( 'NONE',  ( 10.00000000000000000, 35.92658777277525672, -10.74501242461245809 ) ) ;
#33330=VECTOR ( 'NONE', #12438, 1000.000000000000000 ) ;
#33335=CARTESIAN_POINT ( 'NONE',  ( 0.000000000000000000, 30.84782396557248418, -21.32104025579081252 ) ) ;
#33367=ORIENTED_EDGE ( 'NONE', *, *, #50751, .T. ) ;
#33372=CARTESIAN_POINT ( 'NONE',  ( 10.00000000000000000, -22.74946021919110706, -29.81001611431033282 ) ) ;
#33378=CIRCLE ( 'NONE', #16596, 15.99999999999999822 ) ;
#33379=AXIS2_PLACEMENT_3D ( 'NONE', #43162, #3314, #14936 ) ;
#33392=CARTESIAN_POINT ( 'NONE',  ( -3.000000000000000000, -11.95096189432345390, 23.69967320028757385 ) ) ;
#33402=DIRECTION ( 'NONE',  ( -1.000000000000000000, 0.000000000000000000, 0.000000000000000000 ) ) ;
#33406=CARTESIAN_POINT ( 'NONE',  ( 0.000000000000000000, -10.45096189432314837, -21.10159698893440350 ) ) ;
#33408=AXIS2_PLACEMENT_3D ( 'NONE', #42995, #24949, #71167 ) ;
#33426=DIRECTION ( 'NONE',  ( -1.000000000000000000, 0.000000000000000000, 0.000000000000000000 ) ) ;
#33431=CARTESIAN_POINT ( 'NONE',  ( 10.00000000000000000, 0.000000000000000000, 0.000000000000000000 ) ) ;
#33434=DIRECTION ( 'NONE',  ( 0.000000000000000000, 0.8660254037844363761, 0.5000000000000039968 ) ) ;
#33454=CIRCLE ( 'NONE', #53870, 42.00000000000000000 ) ;
#33462=EDGE_LOOP ( 'NONE', ( #7110, #6129, #39435, #1620 ) ) ;
#33469=DIRECTION ( 'NONE',  ( 0.000000000000000000, 0.8660254037844432595, -0.4999999999999920064 ) ) ;
#33496=DIRECTION ( 'NONE',  ( 0.000000000000000000, 0.9945218953682729568, 0.1045284632676578424 ) ) ;
#33515=CIRCLE ( 'NONE', #27511, 15.99999999999999822 ) ;
#33516=CARTESIAN_POINT ( 'NONE',  ( 10.00000000000000000, -26.79245525562738095, 32.34446384429961796 ) ) ;
#33526=LINE ( 'NONE', #27523, #14389 ) ;
#33528=EDGE_CURVE ( 'NONE', #6686, #1439, #33515, .T. ) ;
#33537=VERTEX_POINT ( 'NONE', #39020 ) ;
#33549=ORIENTED_EDGE ( 'NONE', *, *, #31120, .T. ) ;
#33569=DIRECTION ( 'NONE',  ( -1.000000000000000000, 0.000000000000000000, 0.000000000000000000 ) ) ;
#33570=CARTESIAN_POINT ( 'NONE',  ( 10.00000000000000000, -16.65560815589439159, 38.55633173627004595 ) ) ;
#33572=DIRECTION ( 'NONE',  ( 0.000000000000000000, 0.000000000000000000, -1.000000000000000000 ) ) ;
#33590=EDGE_LOOP ( 'NONE', ( #20641, #1224, #66440, #72442 ) ) ;
#33601=DIRECTION ( 'NONE',  ( -1.000000000000000000, -0.000000000000000000, 0.000000000000000000 ) ) ;
#33607=CIRCLE ( 'NONE', #26413, 42.00000000000000000 ) ;
#33612=VECTOR ( 'NONE', #37567, 1000.000000000000000 ) ;
#33626=VECTOR ( 'NONE', #28524, 1000.000000000000000 ) ;
#33647=CARTESIAN_POINT ( 'NONE',  ( 0.000000000000000000, 0.000000000000000000, 0.000000000000000000 ) ) ;
#33648=DIRECTION ( 'NONE',  ( -1.000000000000000000, 0.000000000000000000, 0.000000000000000000 ) ) ;
#33653=ORIENTED_EDGE ( 'NONE', *, *, #66562, .T. ) ;
#33663=DIRECTION ( 'NONE',  ( -1.000000000000000000, 0.000000000000000000, 0.000000000000000000 ) ) ;
#33665=ORIENTED_EDGE ( 'NONE', *, *, #66280, .T. ) ;
#33675=CARTESIAN_POINT ( 'NONE',  ( 10.00000000000000000, -0.8828120875903202602, 37.48860685352291000 ) ) ;
#33685=CARTESIAN_POINT ( 'NONE',  ( 0.000000000000000000, 16.45098606841173705, -33.79645857604496229 ) ) ;
#33688=ORIENTED_EDGE ( 'NONE', *, *, #47541, .T. ) ;
#33699=EDGE_CURVE ( 'NONE', #5557, #67207, #12568, .T. ) ;
#33722=ADVANCED_FACE ( 'NONE', ( #36240 ), #41153, .T. ) ;
#33732=AXIS2_PLACEMENT_3D ( 'NONE', #36274, #20470, #25372 ) ;
#33786=ORIENTED_EDGE ( 'NONE', *, *, #30198, .T. ) ;
#33793=CIRCLE ( 'NONE', #66213, 42.00000000000000000 ) ;
#33794=DIRECTION ( 'NONE',  ( 0.000000000000000000, 0.000000000000000000, 1.000000000000000000 ) ) ;
#33797=AXIS2_PLACEMENT_3D ( 'NONE', #2519, #59243, #30288 ) ;
#33802=LINE ( 'NONE', #72521, #12797 ) ;
#33815=DIRECTION ( 'NONE',  ( -1.000000000000000000, -0.000000000000000000, -0.000000000000000000 ) ) ;
#33823=ORIENTED_EDGE ( 'NONE', *, *, #37301, .T. ) ;
#33826=ORIENTED_EDGE ( 'NONE', *, *, #20644, .T. ) ;
#33832=VERTEX_POINT ( 'NONE', #48267 ) ;
#33836=ORIENTED_EDGE ( 'NONE', *, *, #6771, .F. ) ;
#33852=ORIENTED_EDGE ( 'NONE', *, *, #47517, .T. ) ;
#33855=VERTEX_POINT ( 'NONE', #3539 ) ;
#33861=EDGE_CURVE ( 'NONE', #45442, #11526, #42631, .T. ) ;
#33865=VECTOR ( 'NONE', #11166, 999.9999999999998863 ) ;
#33873=CARTESIAN_POINT ( 'NONE',  ( -10.00000000000000000, 0.000000000000000000, 0.000000000000000000 ) ) ;
#33906=CARTESIAN_POINT ( 'NONE',  ( 0.000000000000000000, -27.05870788708213226, -26.08949754953053102 ) ) ;
#33911=DIRECTION ( 'NONE',  ( 0.000000000000000000, -0.9876883405951358830, -0.1564344650402420822 ) ) ;
#33913=CARTESIAN_POINT ( 'NONE',  ( -3.000000000000000000, 20.85821328998756385, -10.92862929874494959 ) ) ;
#33916=EDGE_CURVE ( 'NONE', #50573, #32331, #66670, .T. ) ;
#33925=VERTEX_POINT ( 'NONE', #65200 ) ;
#33936=CYLINDRICAL_SURFACE ( 'NONE', #74147, 37.49900000000000233 ) ;
#33949=DIRECTION ( 'NONE',  ( -1.000000000000000000, 0.000000000000000000, 0.000000000000000000 ) ) ;
#33957=ORIENTED_EDGE ( 'NONE', *, *, #55444, .F. ) ;
#33977=CARTESIAN_POINT ( 'NONE',  ( 0.000000000000000000, -22.67460108101774807, -6.353146135318215038 ) ) ;
#33978=CARTESIAN_POINT ( 'NONE',  ( -3.000000000000000000, 14.60985201121704513, 18.46759930825707841 ) ) ;
#33979=EDGE_CURVE ( 'NONE', #67669, #31441, #55200, .T. ) ;
#33984=DIRECTION ( 'NONE',  ( -0.000000000000000000, -1.000000000000000000, -0.000000000000000000 ) ) ;
#34000=AXIS2_PLACEMENT_3D ( 'NONE', #37955, #37226, #73269 ) ;
#34017=CARTESIAN_POINT ( 'NONE',  ( 10.00000000000000000, -25.88420570971419821, 27.13269053701087330 ) ) ;
#34022=ORIENTED_EDGE ( 'NONE', *, *, #12545, .F. ) ;
#34032=DIRECTION ( 'NONE',  ( -1.000000000000000000, 0.000000000000000000, 0.000000000000000000 ) ) ;
#34038=ORIENTED_EDGE ( 'NONE', *, *, #56224, .F. ) ;
#34068=ORIENTED_EDGE ( 'NONE', *, *, #58978, .T. ) ;
#34078=DIRECTION ( 'NONE',  ( 0.000000000000000000, 0.7071067811865437980, 0.7071067811865512365 ) ) ;
#34086=VERTEX_POINT ( 'NONE', #21159 ) ;
#34118=VERTEX_POINT ( 'NONE', #51963 ) ;
#34138=DIRECTION ( 'NONE',  ( -0.000000000000000000, -1.000000000000000000, -0.000000000000000000 ) ) ;
#34153=CARTESIAN_POINT ( 'NONE',  ( 10.00000000000000000, -37.58145647212455032, 0.6853352020789044152 ) ) ;
#34166=FACE_OUTER_BOUND ( 'NONE', #61, .T. ) ;
#34175=LINE ( 'NONE', #69494, #19477 ) ;
#34190=AXIS2_PLACEMENT_3D ( 'NONE', #31799, #55110, #26537 ) ;
#34198=ORIENTED_EDGE ( 'NONE', *, *, #55949, .F. ) ;
#34231=DIRECTION ( 'NONE',  ( 0.000000000000000000, -0.8090169943749403458, -0.5877852522924830181 ) ) ;
#34232=CARTESIAN_POINT ( 'NONE',  ( 10.00000000000000000, -37.58145647212455032, 0.6853352020789044152 ) ) ;
#34248=CARTESIAN_POINT ( 'NONE',  ( 10.00000000000000000, 0.000000000000000000, 0.000000000000000000 ) ) ;
#34249=CARTESIAN_POINT ( 'NONE',  ( 0.000000000000000000, -17.67226234102849958, 33.17418723428301774 ) ) ;
#34253=DIRECTION ( 'NONE',  ( 1.000000000000000000, 0.000000000000000000, 0.000000000000000000 ) ) ;
#34260=DIRECTION ( 'NONE',  ( 0.000000000000000000, -0.1564344650402380854, 0.9876883405951365491 ) ) ;
#34285=ORIENTED_EDGE ( 'NONE', *, *, #14170, .T. ) ;
#34288=CARTESIAN_POINT ( 'NONE',  ( 10.00000000000000000, -36.13751322684404244, -21.40280677340410165 ) ) ;
#34290=DIRECTION ( 'NONE',  ( -0.000000000000000000, 0.5877852522924696954, 0.8090169943749498938 ) ) ;
#34291=ORIENTED_EDGE ( 'NONE', *, *, #17918, .T. ) ;
#34326=AXIS2_PLACEMENT_3D ( 'NONE', #35081, #36545, #35446 ) ;
#34338=CIRCLE ( 'NONE', #11522, 37.49900000000000233 ) ;
#34352=FACE_OUTER_BOUND ( 'NONE', #20559, .T. ) ;
#34353=DIRECTION ( 'NONE',  ( 0.000000000000000000, 0.000000000000000000, 1.000000000000000000 ) ) ;
#34358=CIRCLE ( 'NONE', #63206, 15.99999999999999822 ) ;
#34365=DIRECTION ( 'NONE',  ( 0.000000000000000000, -0.8090169943749531134, 0.5877852522924653655 ) ) ;
#34377=LINE ( 'NONE', #62984, #20719 ) ;
#34382=ORIENTED_EDGE ( 'NONE', *, *, #20442, .F. ) ;
#34401=LINE ( 'NONE', #29864, #58801 ) ;
#34410=ORIENTED_EDGE ( 'NONE', *, *, #20442, .T. ) ;
#34413=CARTESIAN_POINT ( 'NONE',  ( 10.00000000000000000, -27.05870788708250885, 26.08949754953014022 ) ) ;
#34416=FACE_OUTER_BOUND ( 'NONE', #3534, .T. ) ;
#34417=EDGE_LOOP ( 'NONE', ( #20358, #13667, #26642, #64815 ) ) ;
#34419=DIRECTION ( 'NONE',  ( -0.000000000000000000, 0.2079116908177543743, 0.9781476007338066880 ) ) ;
#34428=CIRCLE ( 'NONE', #28417, 42.00000000000000000 ) ;
#34433=ORIENTED_EDGE ( 'NONE', *, *, #45185, .T. ) ;
#34436=AXIS2_PLACEMENT_3D ( 'NONE', #70151, #58900, #63438 ) ;
#34460=CARTESIAN_POINT ( 'NONE',  ( 10.00000000000000000, 0.000000000000000000, 0.000000000000000000 ) ) ;
#34472=EDGE_CURVE ( 'NONE', #50309, #21580, #27454, .T. ) ;
#34485=( GEOMETRIC_REPRESENTATION_CONTEXT ( 3 ) GLOBAL_UNCERTAINTY_ASSIGNED_CONTEXT ( ( #30824 ) ) GLOBAL_UNIT_ASSIGNED_CONTEXT ( ( #31507, #4080, #71350 ) ) REPRESENTATION_CONTEXT ( 'NONE', 'WORKASPACE' ) );
#34487=CARTESIAN_POINT ( 'NONE',  ( 10.00000000000000000, 6.555932627142418312, 37.01155633439060466 ) ) ;
#34505=ORIENTED_EDGE ( 'NONE', *, *, #47643, .F. ) ;
#34518=DIRECTION ( 'NONE',  ( -1.000000000000000000, 0.000000000000000000, 0.000000000000000000 ) ) ;
#34537=DIRECTION ( 'NONE',  ( 0.000000000000000000, 0.000000000000000000, 1.000000000000000000 ) ) ;
#34543=CARTESIAN_POINT ( 'NONE',  ( -3.000000000000000000, -20.55727247249748046, 16.78983467731285018 ) ) ;
#34553=CARTESIAN_POINT ( 'NONE',  ( 0.000000000000000000, 0.000000000000000000, 0.000000000000000000 ) ) ;
#34559=EDGE_CURVE ( 'NONE', #26707, #1365, #63184, .T. ) ;
#34563=LINE ( 'NONE', #18376, #35208 ) ;
#34565=ORIENTED_EDGE ( 'NONE', *, *, #16027, .F. ) ;
#34575=VECTOR ( 'NONE', #5795, 1000.000000000000000 ) ;
#34587=EDGE_LOOP ( 'NONE', ( #14731, #54008, #46245, #16563 ) ) ;
#34630=CARTESIAN_POINT ( 'NONE',  ( -10.00000000000000000, 0.000000000000000000, 0.000000000000000000 ) ) ;
#34636=VECTOR ( 'NONE', #54976, 1000.000000000000000 ) ;
#34639=DIRECTION ( 'NONE',  ( -1.000000000000000000, 0.000000000000000000, -0.000000000000000000 ) ) ;
#34640=EDGE_CURVE ( 'NONE', #63672, #1816, #58050, .T. ) ;
#34641=CYLINDRICAL_SURFACE ( 'NONE', #41880, 42.00000000000000000 ) ;
#34643=DIRECTION ( 'NONE',  ( 0.000000000000000000, 0.4539904997395477482, -0.8910065241883673437 ) ) ;
#34650=AXIS2_PLACEMENT_3D ( 'NONE', #11335, #34639, #28252 ) ;
#34654=ORIENTED_EDGE ( 'NONE', *, *, #22929, .F. ) ;
#34682=AXIS2_PLACEMENT_3D ( 'NONE', #41382, #64319, #64684 ) ;
#34683=DIRECTION ( 'NONE',  ( -1.000000000000000000, -0.000000000000000000, -0.000000000000000000 ) ) ;
#34701=DIRECTION ( 'NONE',  ( 0.000000000000000000, 0.000000000000000000, 1.000000000000000000 ) ) ;
#34702=AXIS2_PLACEMENT_3D ( 'NONE', #52638, #13523, #64303 ) ;
#34705=DIRECTION ( 'NONE',  ( 0.000000000000000000, 0.000000000000000000, 1.000000000000000000 ) ) ;
#34726=CARTESIAN_POINT ( 'NONE',  ( 10.00000000000000000, -33.79645857604525361, 16.45098606841114730 ) ) ;
#34729=LINE ( 'NONE', #58031, #30381 ) ;
#34739=CIRCLE ( 'NONE', #38335, 42.00000000000000000 ) ;
#34756=DIRECTION ( 'NONE',  ( 0.000000000000000000, -0.8660254037844363761, -0.5000000000000039968 ) ) ;
#34758=AXIS2_PLACEMENT_3D ( 'NONE', #22890, #57461, #28884 ) ;
#34760=CIRCLE ( 'NONE', #20830, 15.99999999999999645 ) ;
#34763=ORIENTED_EDGE ( 'NONE', *, *, #47024, .F. ) ;
#34764=VECTOR ( 'NONE', #48637, 1000.000000000000000 ) ;
#34768=ORIENTED_EDGE ( 'NONE', *, *, #74167, .T. ) ;
#34772=EDGE_LOOP ( 'NONE', ( #37769, #41184, #3060, #50073 ) ) ;
#34788=ORIENTED_EDGE ( 'NONE', *, *, #66787, .F. ) ;
#34801=EDGE_LOOP ( 'NONE', ( #71658, #74191, #22104, #33172 ) ) ;
#34803=CARTESIAN_POINT ( 'NONE',  ( 10.00000000000000000, 12.26510123303259725, 35.53030884539089840 ) ) ;
#34823=DIRECTION ( 'NONE',  ( -1.000000000000000000, 0.000000000000000000, -0.000000000000000000 ) ) ;
#34830=EDGE_CURVE ( 'NONE', #913, #66848, #2792, .T. ) ;
#34846=CARTESIAN_POINT ( 'NONE',  ( 0.000000000000000000, -37.48860685352291711, 0.8828120875899322373 ) ) ;
#34847=AXIS2_PLACEMENT_3D ( 'NONE', #31166, #4107, #14244 ) ;
#34863=ORIENTED_EDGE ( 'NONE', *, *, #26415, .T. ) ;
#34881=DIRECTION ( 'NONE',  ( -1.000000000000000000, 0.000000000000000000, 0.000000000000000000 ) ) ;
#34891=CARTESIAN_POINT ( 'NONE',  ( -3.000000000000000000, -3.948201729842348850, 23.21447184625293048 ) ) ;
#34907=VECTOR ( 'NONE', #13452, 999.9999999999998863 ) ;
#34917=CARTESIAN_POINT ( 'NONE',  ( 10.00000000000000000, -12.42422080174663712, 35.38097989696507994 ) ) ;
#34920=CARTESIAN_POINT ( 'NONE',  ( 0.000000000000000000, 35.95386929396241271, 10.96151621346552751 ) ) ;
#34921=EDGE_CURVE ( 'NONE', #44983, #70418, #45101, .T. ) ;
#34922=EDGE_CURVE ( 'NONE', #18301, #61409, #16904, .T. ) ;
#34924=AXIS2_PLACEMENT_3D ( 'NONE', #34248, #5699, #45556 ) ;
#34933=DIRECTION ( 'NONE',  ( -1.000000000000000000, 0.000000000000000000, 0.000000000000000000 ) ) ;
#34936=CARTESIAN_POINT ( 'NONE',  ( 10.00000000000000000, 0.000000000000000000, 37.49900000000000233 ) ) ;
#34954=DIRECTION ( 'NONE',  ( -1.000000000000000000, 0.000000000000000000, 0.000000000000000000 ) ) ;
#34992=CARTESIAN_POINT ( 'NONE',  ( 5.000000000000000000, -39.04073710021332744, -15.48615015657624205 ) ) ;
#34994=DIRECTION ( 'NONE',  ( 0.000000000000000000, 0.000000000000000000, 1.000000000000000000 ) ) ;
#34997=DIRECTION ( 'NONE',  ( 0.000000000000000000, 0.000000000000000000, 1.000000000000000000 ) ) ;
#35006=CARTESIAN_POINT ( 'NONE',  ( 10.00000000000000000, 22.74946021919133088, 29.81001611431016229 ) ) ;
#35012=DIRECTION ( 'NONE',  ( 1.000000000000000000, -0.000000000000000000, 0.000000000000000000 ) ) ;
#35013=CARTESIAN_POINT ( 'NONE',  ( 4.999999999999999112, 9.188173127307294408, 40.98264845739752360 ) ) ;
#35018=CARTESIAN_POINT ( 'NONE',  ( 0.000000000000000000, -39.04073710021356192, 15.48615015657568073 ) ) ;
#35019=EDGE_LOOP ( 'NONE', ( #29855, #23656, #29689, #25499 ) ) ;
#35034=EDGE_CURVE ( 'NONE', #26649, #72759, #73277, .T. ) ;
#35036=VERTEX_POINT ( 'NONE', #14000 ) ;
#35052=STYLED_ITEM ( 'NONE', ( #24790 ), #65097 ) ;
#35053=CIRCLE ( 'NONE', #17024, 37.49900000000000233 ) ;
#35054=ORIENTED_EDGE ( 'NONE', *, *, #3770, .T. ) ;
#35081=CARTESIAN_POINT ( 'NONE',  ( -10.00000000000000000, 0.000000000000000000, 0.000000000000000000 ) ) ;
#35085=PLANE ( 'NONE',  #3487 ) ;
#35086=ORIENTED_EDGE ( 'NONE', *, *, #28573, .T. ) ;
#35093=CARTESIAN_POINT ( 'NONE',  ( 0.000000000000000000, 6.555932627142418312, 37.01155633439060466 ) ) ;
#35095=CARTESIAN_POINT ( 'NONE',  ( -3.000000000000000000, -1.278221433540145391, -26.51162292216073979 ) ) ;
#35125=DIRECTION ( 'NONE',  ( 0.000000000000000000, 0.000000000000000000, 1.000000000000000000 ) ) ;
#35126=AXIS2_PLACEMENT_3D ( 'NONE', #69933, #2302, #47390 ) ;
#35137=ORIENTED_EDGE ( 'NONE', *, *, #15148, .F. ) ;
#35142=ORIENTED_EDGE ( 'NONE', *, *, #28272, .T. ) ;
#35170=CARTESIAN_POINT ( 'NONE',  ( -10.00000000000000000, 0.000000000000000000, 0.000000000000000000 ) ) ;
#35181=CARTESIAN_POINT ( 'NONE',  ( 0.000000000000000000, 21.40280677340421889, -36.13751322684397138 ) ) ;
#35183=AXIS2_PLACEMENT_3D ( 'NONE', #31845, #54788, #26205 ) ;
#35200=CIRCLE ( 'NONE', #41219, 42.00000000000000000 ) ;
#35203=VERTEX_POINT ( 'NONE', #69143 ) ;
#35207=DIRECTION ( 'NONE',  ( 0.000000000000000000, 0.9945218953682742891, -0.1045284632676436315 ) ) ;
#35208=VECTOR ( 'NONE', #6384, 1000.000000000000000 ) ;
#35216=VECTOR ( 'NONE', #19585, 1000.000000000000000 ) ;
#35218=DIRECTION ( 'NONE',  ( 1.000000000000000000, -0.000000000000000000, -0.000000000000000000 ) ) ;
#35225=ORIENTED_EDGE ( 'NONE', *, *, #25057, .F. ) ;
#35230=VECTOR ( 'NONE', #60628, 1000.000000000000000 ) ;
#35258=VERTEX_POINT ( 'NONE', #70962 ) ;
#35259=ORIENTED_EDGE ( 'NONE', *, *, #45361, .F. ) ;
#35260=CYLINDRICAL_SURFACE ( 'NONE', #25377, 37.49900000000000233 ) ;
#35269=DIRECTION ( 'NONE',  ( -1.000000000000000000, 0.000000000000000000, 0.000000000000000000 ) ) ;
#35271=AXIS2_PLACEMENT_3D ( 'NONE', #59900, #18907, #8382 ) ;
#35282=CARTESIAN_POINT ( 'NONE',  ( 10.00000000000000000, 0.000000000000000000, 0.000000000000000000 ) ) ;
#35284=DIRECTION ( 'NONE',  ( 0.000000000000000000, -0.5877852522924624790, -0.8090169943749553338 ) ) ;
#35289=AXIS2_PLACEMENT_3D ( 'NONE', #22055, #63049, #50620 ) ;
#35296=EDGE_CURVE ( 'NONE', #37933, #28395, #39762, .T. ) ;
#35320=VERTEX_POINT ( 'NONE', #65348 ) ;
#35345=CIRCLE ( 'NONE', #47364, 42.00000000000000000 ) ;
#35349=ORIENTED_EDGE ( 'NONE', *, *, #50637, .F. ) ;
#35364=DIRECTION ( 'NONE',  ( -1.000000000000000000, -0.000000000000000000, -0.000000000000000000 ) ) ;
#35367=DIRECTION ( 'NONE',  ( 1.000000000000000000, -0.000000000000000000, 0.000000000000000000 ) ) ;
#35419=EDGE_CURVE ( 'NONE', #41967, #20003, #20587, .T. ) ;
#35445=CARTESIAN_POINT ( 'NONE',  ( 0.000000000000000000, 27.05870788708231700, 26.08949754953034272 ) ) ;
#35446=DIRECTION ( 'NONE',  ( 0.000000000000000000, 0.000000000000000000, 1.000000000000000000 ) ) ;
#35447=PLANE ( 'NONE',  #41888 ) ;
#35458=DIRECTION ( 'NONE',  ( 1.000000000000000000, -0.000000000000000000, 0.000000000000000000 ) ) ;
#35468=CARTESIAN_POINT ( 'NONE',  ( -10.00000000000000000, 0.000000000000000000, 0.000000000000000000 ) ) ;
#35484=FACE_OUTER_BOUND ( 'NONE', #4465, .T. ) ;
#35495=ORIENTED_EDGE ( 'NONE', *, *, #20488, .F. ) ;
#35507=ORIENTED_EDGE ( 'NONE', *, *, #7962, .T. ) ;
#35517=DIRECTION ( 'NONE',  ( 0.000000000000000000, 0.000000000000000000, -1.000000000000000000 ) ) ;
#35528=CARTESIAN_POINT ( 'NONE',  ( 4.999999999999999112, 40.98264845739763018, -9.188173127306860977 ) ) ;
#35558=VECTOR ( 'NONE', #56463, 1000.000000000000000 ) ;
#35577=ORIENTED_EDGE ( 'NONE', *, *, #44985, .F. ) ;
#35593=VECTOR ( 'NONE', #18010, 1000.000000000000000 ) ;
#35602=DIRECTION ( 'NONE',  ( 0.000000000000000000, 0.9135454576426063067, -0.4067366430757881068 ) ) ;
#35614=CARTESIAN_POINT ( 'NONE',  ( 10.00000000000000000, 6.736453364084091788, -36.88895765772625879 ) ) ;
#35645=CIRCLE ( 'NONE', #5678, 16.00000000000000000 ) ;
#35653=VECTOR ( 'NONE', #45484, 1000.000000000000000 ) ;
#35659=VECTOR ( 'NONE', #54729, 1000.000000000000000 ) ;
#35666=VERTEX_POINT ( 'NONE', #19742 ) ;
#35671=ORIENTED_EDGE ( 'NONE', *, *, #45409, .F. ) ;
#35679=VERTEX_POINT ( 'NONE', #58878 ) ;
#35683=EDGE_LOOP ( 'NONE', ( #72030, #22962, #28707, #62446 ) ) ;
#35688=ORIENTED_EDGE ( 'NONE', *, *, #31308, .F. ) ;
#35693=ORIENTED_EDGE ( 'NONE', *, *, #44412, .F. ) ;
#35700=EDGE_LOOP ( 'NONE', ( #70932, #7606, #66856, #17092 ) ) ;
#35705=CARTESIAN_POINT ( 'NONE',  ( -3.000000000000000000, 8.688484142253939169, 21.88630264137371029 ) ) ;
#35726=LINE ( 'NONE', #3773, #10011 ) ;
#35731=CARTESIAN_POINT ( 'NONE',  ( -3.000000000000000000, 16.61724383029390140, -20.69703378468903665 ) ) ;
#35733=EDGE_CURVE ( 'NONE', #4438, #5103, #41573, .T. ) ;
#35736=ORIENTED_EDGE ( 'NONE', *, *, #19629, .T. ) ;
#35737=CIRCLE ( 'NONE', #74177, 16.00000000000000000 ) ;
#35754=VERTEX_POINT ( 'NONE', #31023 ) ;
#35755=DIRECTION ( 'NONE',  ( -0.000000000000000000, -0.6691306063588671194, 0.7431448254773862505 ) ) ;
#35779=SHAPE_DEFINITION_REPRESENTATION ( #15781, #30982 ) ;
#35783=EDGE_CURVE ( 'NONE', #5732, #5518, #7391, .T. ) ;
#35789=ORIENTED_EDGE ( 'NONE', *, *, #12569, .F. ) ;
#35802=CARTESIAN_POINT ( 'NONE',  ( -3.000000000000000000, -14.54903810567645195, -22.19967320028775504 ) ) ;
#35815=CARTESIAN_POINT ( 'NONE',  ( 0.000000000000000000, -14.54903810567676636, 22.19967320028756319 ) ) ;
#35817=ORIENTED_EDGE ( 'NONE', *, *, #68781, .T. ) ;
#35850=AXIS2_PLACEMENT_3D ( 'NONE', #24650, #53228, #1763 ) ;
#35859=VERTEX_POINT ( 'NONE', #48692 ) ;
#35870=ORIENTED_EDGE ( 'NONE', *, *, #37665, .F. ) ;
#35882=EDGE_CURVE ( 'NONE', #39410, #23684, #15595, .T. ) ;
#35892=DIRECTION ( 'NONE',  ( -0.000000000000000000, -0.8660254037844427044, 0.4999999999999929501 ) ) ;
#35897=DIRECTION ( 'NONE',  ( 0.000000000000000000, -0.1045284632676578285, 0.9945218953682729568 ) ) ;
#35906=LINE ( 'NONE', #7355, #54120 ) ;
#35911=AXIS2_PLACEMENT_3D ( 'NONE', #57606, #62514, #130 ) ;
#35922=CYLINDRICAL_SURFACE ( 'NONE', #474, 37.49900000000000233 ) ;
#35929=DIRECTION ( 'NONE',  ( -1.000000000000000000, 0.000000000000000000, 0.000000000000000000 ) ) ;
#35946=ORIENTED_EDGE ( 'NONE', *, *, #29586, .T. ) ;
#35963=ADVANCED_FACE ( 'NONE', ( #72361 ), #38152, .F. ) ;
#35972=DIRECTION ( 'NONE',  ( 1.000000000000000000, -0.000000000000000000, -0.000000000000000000 ) ) ;
#35983=ADVANCED_FACE ( 'NONE', ( #20113 ), #14480, .T. ) ;
#35985=ORIENTED_EDGE ( 'NONE', *, *, #15553, .F. ) ;
#36012=LINE ( 'NONE', #42037, #34907 ) ;
#36015=DIRECTION ( 'NONE',  ( -1.000000000000000000, -0.000000000000000000, -0.000000000000000000 ) ) ;
#36024=CARTESIAN_POINT ( 'NONE',  ( 0.000000000000000000, 35.92658777277510040, 10.74501242461294659 ) ) ;
#36029=DIRECTION ( 'NONE',  ( 0.000000000000000000, 0.9945218953682742891, -0.1045284632676436315 ) ) ;
#36051=AXIS2_PLACEMENT_3D ( 'NONE', #19103, #48055, #2608 ) ;
#36053=CARTESIAN_POINT ( 'NONE',  ( 10.00000000000000000, -35.92658777277517856, 10.74501242461269257 ) ) ;
#36062=ORIENTED_EDGE ( 'NONE', *, *, #53449, .F. ) ;
#36091=ORIENTED_EDGE ( 'NONE', *, *, #47979, .T. ) ;
#36112=CYLINDRICAL_SURFACE ( 'NONE', #28633, 16.00000000000000000 ) ;
#36120=DIRECTION ( 'NONE',  ( -0.000000000000000000, 0.9781476007338069101, -0.2079116908177532363 ) ) ;
#36133=EDGE_CURVE ( 'NONE', #28466, #64719, #11072, .T. ) ;
#36149=CARTESIAN_POINT ( 'NONE',  ( 10.00000000000000000, 26.08949754953062694, -27.05870788708203989 ) ) ;
#36156=ORIENTED_EDGE ( 'NONE', *, *, #61280, .T. ) ;
#36160=DIRECTION ( 'NONE',  ( -1.000000000000000000, -0.000000000000000000, 0.000000000000000000 ) ) ;
#36178=DIRECTION ( 'NONE',  ( 0.000000000000000000, 0.3090169943749480619, -0.9510565162951533091 ) ) ;
#36189=CIRCLE ( 'NONE', #3789, 15.99999999999999822 ) ;
#36190=ORIENTED_EDGE ( 'NONE', *, *, #6161, .F. ) ;
#36193=AXIS2_PLACEMENT_3D ( 'NONE', #996, #51717, #30256 ) ;
#36214=DIRECTION ( 'NONE',  ( 0.000000000000000000, -0.9945218953682741780, 0.1045284632676447972 ) ) ;
#36240=FACE_OUTER_BOUND ( 'NONE', #33284, .T. ) ;
#36241=EDGE_CURVE ( 'NONE', #60133, #7308, #2657, .T. ) ;
#36252=DIRECTION ( 'NONE',  ( 0.000000000000000000, -0.8660254037844432595, 0.4999999999999919509 ) ) ;
#36265=ORIENTED_EDGE ( 'NONE', *, *, #65438, .F. ) ;
#36274=CARTESIAN_POINT ( 'NONE',  ( 10.00000000000000000, 37.01155633439068282, -6.555932627142014191 ) ) ;
#36275=CARTESIAN_POINT ( 'NONE',  ( 10.00000000000000000, -17.80606268964516659, -33.00180498840066434 ) ) ;
#36276=VERTEX_POINT ( 'NONE', #53510 ) ;
#36283=ORIENTED_EDGE ( 'NONE', *, *, #60682, .F. ) ;
#36297=VECTOR ( 'NONE', #63471, 1000.000000000000000 ) ;
#36302=CARTESIAN_POINT ( 'NONE',  ( 0.000000000000000000, 0.000000000000000000, 0.000000000000000000 ) ) ;
#36306=AXIS2_PLACEMENT_3D ( 'NONE', #56462, #32020, #33128 ) ;
#36311=ORIENTED_EDGE ( 'NONE', *, *, #53646, .F. ) ;
#36335=DIRECTION ( 'NONE',  ( 0.000000000000000000, 0.4539904997395479702, -0.8910065241883673437 ) ) ;
#36342=VERTEX_POINT ( 'NONE', #66996 ) ;
#36356=VECTOR ( 'NONE', #2495, 1000.000000000000000 ) ;
#36376=LINE ( 'NONE', #13454, #58471 ) ;
#36388=EDGE_CURVE ( 'NONE', #62438, #57306, #41794, .T. ) ;
#36396=ADVANCED_FACE ( 'NONE', ( #32410 ), #3874, .F. ) ;
#36418=CARTESIAN_POINT ( 'NONE',  ( 0.000000000000000000, -4.992566952385247170, 37.16516213103275845 ) ) ;
#36467=CYLINDRICAL_SURFACE ( 'NONE', #67099, 42.00000000000000000 ) ;
#36470=AXIS2_PLACEMENT_3D ( 'NONE', #10844, #57085, #16480 ) ;
#36472=DIRECTION ( 'NONE',  ( 0.000000000000000000, 0.9510565162951503115, 0.3090169943749573878 ) ) ;
#36473=CARTESIAN_POINT ( 'NONE',  ( 10.00000000000000000, 0.000000000000000000, 0.000000000000000000 ) ) ;
#36477=DIRECTION ( 'NONE',  ( -1.000000000000000000, -0.000000000000000000, 0.000000000000000000 ) ) ;
#36487=AXIS2_PLACEMENT_3D ( 'NONE', #73307, #11278, #56787 ) ;
#36524=FACE_OUTER_BOUND ( 'NONE', #45228, .T. ) ;
#36527=CARTESIAN_POINT ( 'NONE',  ( 0.000000000000000000, 6.736453364083555329, 36.88895765772635116 ) ) ;
#36544=DIRECTION ( 'NONE',  ( 0.000000000000000000, 0.000000000000000000, 1.000000000000000000 ) ) ;
#36545=DIRECTION ( 'NONE',  ( -1.000000000000000000, -0.000000000000000000, -0.000000000000000000 ) ) ;
#36554=DIRECTION ( 'NONE',  ( -1.000000000000000000, 0.000000000000000000, -0.000000000000000000 ) ) ;
#36560=VERTEX_POINT ( 'NONE', #57218 ) ;
#36563=EDGE_CURVE ( 'NONE', #15251, #53901, #54991, .T. ) ;
#36569=CARTESIAN_POINT ( 'NONE',  ( 0.000000000000000000, 0.6853352020790449695, 37.58145647212454321 ) ) ;
#36572=EDGE_CURVE ( 'NONE', #31367, #71534, #52578, .T. ) ;
#36573=CARTESIAN_POINT ( 'NONE',  ( 10.00000000000000000, 0.000000000000000000, 0.000000000000000000 ) ) ;
#36587=ADVANCED_FACE ( 'NONE', ( #4615 ), #51189, .T. ) ;
#36591=PLANE ( 'NONE',  #23962 ) ;
#36593=VERTEX_POINT ( 'NONE', #59068 ) ;
#36598=EDGE_CURVE ( 'NONE', #67030, #8551, #8146, .T. ) ;
#36599=CIRCLE ( 'NONE', #70227, 37.49900000000000233 ) ;
#36614=ORIENTED_EDGE ( 'NONE', *, *, #6372, .T. ) ;
#36625=DIRECTION ( 'NONE',  ( 1.000000000000000000, -0.000000000000000000, -0.000000000000000000 ) ) ;
#36636=CYLINDRICAL_SURFACE ( 'NONE', #43519, 16.00000000000000000 ) ;
#36640=FACE_OUTER_BOUND ( 'NONE', #65849, .T. ) ;
#36643=ORIENTED_EDGE ( 'NONE', *, *, #9585, .T. ) ;
#36648=CARTESIAN_POINT ( 'NONE',  ( -3.000000000000000000, -22.67460108101783334, 6.353146135317912169 ) ) ;
#36663=CARTESIAN_POINT ( 'NONE',  ( -3.000000000000000000, 9.615535125378775305, 24.73947219025917121 ) ) ;
#36666=VECTOR ( 'NONE', #18288, 1000.000000000000000 ) ;
#36668=VECTOR ( 'NONE', #17501, 1000.000000000000000 ) ;
#36673=CARTESIAN_POINT ( 'NONE',  ( 10.00000000000000000, -10.96151621346514382, 35.95386929396252640 ) ) ;
#36681=EDGE_CURVE ( 'NONE', #61245, #70917, #4629, .T. ) ;
#36691=DIRECTION ( 'NONE',  ( 0.000000000000000000, 1.000000000000000000, 3.469446951953614189E-15 ) ) ;
#36736=CIRCLE ( 'NONE', #5585, 37.49900000000000944 ) ;
#36761=DIRECTION ( 'NONE',  ( 0.000000000000000000, -6.938893903907228378E-15, 1.000000000000000000 ) ) ;
#36764=CARTESIAN_POINT ( 'NONE',  ( 0.000000000000000000, -36.88895765772628010, -6.736453364083947015 ) ) ;
#36773=AXIS2_PLACEMENT_3D ( 'NONE', #65798, #19911, #20288 ) ;
#36775=DIRECTION ( 'NONE',  ( 0.000000000000000000, 0.000000000000000000, 1.000000000000000000 ) ) ;
#36778=DIRECTION ( 'NONE',  ( 0.000000000000000000, -0.5877852522924802425, 0.8090169943749422332 ) ) ;
#36779=CIRCLE ( 'NONE', #51067, 42.00000000000000000 ) ;
#36789=CIRCLE ( 'NONE', #13983, 42.00000000000000000 ) ;
#36791=ORIENTED_EDGE ( 'NONE', *, *, #39108, .T. ) ;
#36811=DIRECTION ( 'NONE',  ( 0.000000000000000000, -0.6691306063588672304, 0.7431448254773862505 ) ) ;
#36820=DIRECTION ( 'NONE',  ( 0.000000000000000000, -0.4539904997395351471, -0.8910065241883737830 ) ) ;
#36824=VECTOR ( 'NONE', #3027, 1000.000000000000114 ) ;
#36826=CARTESIAN_POINT ( 'NONE',  ( 10.00000000000000000, -6.736453364083817341, 36.88895765772630142 ) ) ;
#36828=VECTOR ( 'NONE', #31245, 1000.000000000000000 ) ;
#36829=EDGE_CURVE ( 'NONE', #2929, #67800, #44222, .T. ) ;
#36836=CARTESIAN_POINT ( 'NONE',  ( 0.000000000000000000, -33.00180498840035170, -17.80606268964575278 ) ) ;
#36842=ADVANCED_FACE ( 'NONE', ( #73657 ), #11258, .T. ) ;
#36843=DIRECTION ( 'NONE',  ( -1.000000000000000000, -0.000000000000000000, -0.000000000000000000 ) ) ;
#36845=ADVANCED_FACE ( 'NONE', ( #68417 ), #28538, .F. ) ;
#36872=AXIS2_PLACEMENT_3D ( 'NONE', #46995, #22964, #16943 ) ;
#36874=CARTESIAN_POINT ( 'NONE',  ( 10.00000000000000000, -35.53030884539077050, -12.26510123303296851 ) ) ;
#36880=AXIS2_PLACEMENT_3D ( 'NONE', #28337, #73080, #21586 ) ;
#36883=LINE ( 'NONE', #59835, #36828 ) ;
#36899=VECTOR ( 'NONE', #21329, 1000.000000000000000 ) ;
#36906=ADVANCED_FACE ( 'NONE', ( #32688 ), #73286, .T. ) ;
#36925=ORIENTED_EDGE ( 'NONE', *, *, #20207, .F. ) ;
#36928=CARTESIAN_POINT ( 'NONE',  ( -3.000000000000000000, -18.13022148937263012, 15.02647892043544608 ) ) ;
#36941=EDGE_CURVE ( 'NONE', #21073, #74280, #63518, .T. ) ;
#36957=PLANE ( 'NONE',  #55721 ) ;
#36970=AXIS2_PLACEMENT_3D ( 'NONE', #38061, #55724, #4243 ) ;
#36974=ORIENTED_EDGE ( 'NONE', *, *, #45241, .T. ) ;
#36985=ORIENTED_EDGE ( 'NONE', *, *, #62775, .T. ) ;
#36998=PLANE ( 'NONE',  #59471 ) ;
#37004=CARTESIAN_POINT ( 'NONE',  ( 0.000000000000000000, 0.000000000000000000, 0.000000000000000000 ) ) ;
#37011=CARTESIAN_POINT ( 'NONE',  ( -3.000000000000000000, -14.54903810567645195, -22.19967320028775504 ) ) ;
#37019=ORIENTED_EDGE ( 'NONE', *, *, #31977, .T. ) ;
#37048=AXIS2_PLACEMENT_3D ( 'NONE', #11328, #6088, #62870 ) ;
#37061=ORIENTED_EDGE ( 'NONE', *, *, #60793, .T. ) ;
#37072=CIRCLE ( 'NONE', #74318, 37.49900000000000944 ) ;
#37082=ORIENTED_EDGE ( 'NONE', *, *, #48443, .F. ) ;
#37088=FACE_OUTER_BOUND ( 'NONE', #13915, .T. ) ;
#37090=CARTESIAN_POINT ( 'NONE',  ( 0.000000000000000000, -22.32062822937469804, -14.36278369418829826 ) ) ;
#37093=AXIS2_PLACEMENT_3D ( 'NONE', #19977, #66598, #66237 ) ;
#37112=ORIENTED_EDGE ( 'NONE', *, *, #27227, .T. ) ;
#37116=CARTESIAN_POINT ( 'NONE',  ( 10.00000000000000000, -37.22597642581161637, 5.202137450156258502 ) ) ;
#37124=VERTEX_POINT ( 'NONE', #66745 ) ;
#37146=ORIENTED_EDGE ( 'NONE', *, *, #70682, .T. ) ;
#37159=VECTOR ( 'NONE', #18147, 1000.000000000000114 ) ;
#37183=CARTESIAN_POINT ( 'NONE',  ( 4.999999999999999112, -10.41901085202050581, -40.68715046381939970 ) ) ;
#37194=ORIENTED_EDGE ( 'NONE', *, *, #22670, .F. ) ;
#37213=ORIENTED_EDGE ( 'NONE', *, *, #58767, .T. ) ;
#37222=CARTESIAN_POINT ( 'NONE',  ( 0.000000000000000000, -22.67460108101783334, 6.353146135317912169 ) ) ;
#37226=DIRECTION ( 'NONE',  ( -1.000000000000000000, 0.000000000000000000, 0.000000000000000000 ) ) ;
#37231=DIRECTION ( 'NONE',  ( -1.000000000000000000, 0.000000000000000000, 0.000000000000000000 ) ) ;
#37236=DIRECTION ( 'NONE',  ( 0.000000000000000000, 0.3090169943749573878, -0.9510565162951503115 ) ) ;
#37241=LINE ( 'NONE', #48143, #7642 ) ;
#37256=CARTESIAN_POINT ( 'NONE',  ( 0.000000000000000000, 37.01155633439068282, -6.555932627142014191 ) ) ;
#37266=CARTESIAN_POINT ( 'NONE',  ( 0.000000000000000000, 26.08949754953024325, 27.05870788708241648 ) ) ;
#37268=AXIS2_PLACEMENT_3D ( 'NONE', #67180, #3681, #31477 ) ;
#37284=ORIENTED_EDGE ( 'NONE', *, *, #21892, .T. ) ;
#37301=EDGE_CURVE ( 'NONE', #10228, #21580, #5917, .T. ) ;
#37310=DIRECTION ( 'NONE',  ( -1.000000000000000000, 0.000000000000000000, -0.000000000000000000 ) ) ;
#37314=CARTESIAN_POINT ( 'NONE',  ( -10.00000000000000000, 0.000000000000000000, 0.000000000000000000 ) ) ;
#37322=CYLINDRICAL_SURFACE ( 'NONE', #227, 16.00000000000000000 ) ;
#37327=VECTOR ( 'NONE', #35458, 1000.000000000000000 ) ;
#37338=DIRECTION ( 'NONE',  ( -1.000000000000000000, -0.000000000000000000, 0.000000000000000000 ) ) ;
#37340=VECTOR ( 'NONE', #45839, 1000.000000000000000 ) ;
#37345=CIRCLE ( 'NONE', #9747, 37.49900000000000944 ) ;
#37358=EDGE_CURVE ( 'NONE', #47235, #26707, #37072, .T. ) ;
#37367=EDGE_CURVE ( 'NONE', #31034, #19670, #31048, .T. ) ;
#37391=EDGE_CURVE ( 'NONE', #15251, #18236, #41869, .T. ) ;
#37401=DIRECTION ( 'NONE',  ( -1.000000000000000000, 0.000000000000000000, -0.000000000000000000 ) ) ;
#37412=LINE ( 'NONE', #60339, #28304 ) ;
#37422=DIRECTION ( 'NONE',  ( -0.000000000000000000, 0.000000000000000000, 1.000000000000000000 ) ) ;
#37427=DIRECTION ( 'NONE',  ( 0.000000000000000000, 0.8090169943749432324, 0.5877852522924789103 ) ) ;
#37449=FACE_OUTER_BOUND ( 'NONE', #48226, .T. ) ;
#37450=CIRCLE ( 'NONE', #2653, 16.00000000000000000 ) ;
#37465=ORIENTED_EDGE ( 'NONE', *, *, #67078, .T. ) ;
#37466=CARTESIAN_POINT ( 'NONE',  ( 10.00000000000000000, 22.64427369931212297, -30.00120703465181293 ) ) ;
#37467=ADVANCED_FACE ( 'NONE', ( #35484 ), #24221, .T. ) ;
#37470=DIRECTION ( 'NONE',  ( 0.000000000000000000, 0.000000000000000000, 1.000000000000000000 ) ) ;
#37478=VERTEX_POINT ( 'NONE', #14766 ) ;
#37502=CARTESIAN_POINT ( 'NONE',  ( 10.00000000000000000, 35.95386929396241271, 10.96151621346552751 ) ) ;
#37504=DIRECTION ( 'NONE',  ( -0.000000000000000000, -0.9510565162951506446, -0.3090169943749562220 ) ) ;
#37529=DIRECTION ( 'NONE',  ( 0.000000000000000000, 0.000000000000000000, 1.000000000000000000 ) ) ;
#37550=EDGE_CURVE ( 'NONE', #58611, #26913, #9870, .T. ) ;
#37567=DIRECTION ( 'NONE',  ( 0.000000000000000000, -0.2079116908177532363, -0.9781476007338069101 ) ) ;
#37571=ORIENTED_EDGE ( 'NONE', *, *, #66459, .T. ) ;
#37599=VECTOR ( 'NONE', #49712, 1000.000000000000000 ) ;
#37617=LINE ( 'NONE', #66909, #44294 ) ;
#37621=EDGE_CURVE ( 'NONE', #41342, #30420, #73937, .T. ) ;
#37626=AXIS2_PLACEMENT_3D ( 'NONE', #6268, #63053, #34078 ) ;
#37641=CARTESIAN_POINT ( 'NONE',  ( 0.000000000000000000, 37.48860685352291000, 0.8828120875901893649 ) ) ;
#37658=EDGE_LOOP ( 'NONE', ( #64114, #31063, #46073, #31334 ) ) ;
#37659=ORIENTED_EDGE ( 'NONE', *, *, #31323, .T. ) ;
#37665=EDGE_CURVE ( 'NONE', #8585, #24685, #57109, .T. ) ;
#37668=ORIENTED_EDGE ( 'NONE', *, *, #72526, .T. ) ;
#37688=FACE_OUTER_BOUND ( 'NONE', #9530, .T. ) ;
#37690=ORIENTED_EDGE ( 'NONE', *, *, #31391, .T. ) ;
#37696=DIRECTION ( 'NONE',  ( -1.000000000000000000, 0.000000000000000000, -0.000000000000000000 ) ) ;
#37748=CARTESIAN_POINT ( 'NONE',  ( 10.00000000000000000, 0.000000000000000000, 0.000000000000000000 ) ) ;
#37749=CARTESIAN_POINT ( 'NONE',  ( 10.00000000000000000, 0.000000000000000000, 0.000000000000000000 ) ) ;
#37766=DIRECTION ( 'NONE',  ( -1.000000000000000000, 0.000000000000000000, 0.000000000000000000 ) ) ;
#37768=CARTESIAN_POINT ( 'NONE',  ( 0.000000000000000000, 6.736453364084091788, -36.88895765772625879 ) ) ;
#37769=ORIENTED_EDGE ( 'NONE', *, *, #25057, .T. ) ;
#37787=CARTESIAN_POINT ( 'NONE',  ( 0.000000000000000000, -18.13022148937243472, -15.02647892043568767 ) ) ;
#37791=DIRECTION ( 'NONE',  ( 0.000000000000000000, 0.000000000000000000, 1.000000000000000000 ) ) ;
#37801=LINE ( 'NONE', #72363, #2894 ) ;
#37812=DIRECTION ( 'NONE',  ( 0.000000000000000000, 0.000000000000000000, 1.000000000000000000 ) ) ;
#37828=EDGE_LOOP ( 'NONE', ( #23941, #47691, #21644, #10300 ) ) ;
#37829=ORIENTED_EDGE ( 'NONE', *, *, #19786, .T. ) ;
#37830=ORIENTED_EDGE ( 'NONE', *, *, #63263, .F. ) ;
#37833=AXIS2_PLACEMENT_3D ( 'NONE', #6177, #69308, #56934 ) ;
#37838=ORIENTED_EDGE ( 'NONE', *, *, #38720, .T. ) ;
#37844=ORIENTED_EDGE ( 'NONE', *, *, #22953, .T. ) ;
#37851=ADVANCED_FACE ( 'NONE', ( #57961 ), #2338, .T. ) ;
#37863=EDGE_CURVE ( 'NONE', #11526, #29066, #10338, .T. ) ;
#37870=FACE_BOUND ( 'NONE', #39771, .T. ) ;
#37889=DIRECTION ( 'NONE',  ( 0.000000000000000000, -0.1564344650402382242, 0.9876883405951366601 ) ) ;
#37891=DIRECTION ( 'NONE',  ( -1.000000000000000000, 0.000000000000000000, -0.000000000000000000 ) ) ;
#37905=CARTESIAN_POINT ( 'NONE',  ( -3.000000000000000000, -19.89357724624987256, -12.59942793731086041 ) ) ;
#37911=ORIENTED_EDGE ( 'NONE', *, *, #20876, .F. ) ;
#37914=AXIS2_PLACEMENT_3D ( 'NONE', #58694, #55178, #37529 ) ;
#37933=VERTEX_POINT ( 'NONE', #31226 ) ;
#37934=VERTEX_POINT ( 'NONE', #49990 ) ;
#37935=EDGE_CURVE ( 'NONE', #58363, #29480, #55965, .T. ) ;
#37941=ORIENTED_EDGE ( 'NONE', *, *, #25740, .F. ) ;
#37948=LINE ( 'NONE', #21012, #72920 ) ;
#37953=FACE_OUTER_BOUND ( 'NONE', #53939, .T. ) ;
#37955=CARTESIAN_POINT ( 'NONE',  ( 10.00000000000000000, 0.000000000000000000, 0.000000000000000000 ) ) ;
#37957=CARTESIAN_POINT ( 'NONE',  ( 0.000000000000000000, 8.688484142253939169, 21.88630264137371029 ) ) ;
#37959=CYLINDRICAL_SURFACE ( 'NONE', #43135, 16.00000000000000000 ) ;
#37963=DIRECTION ( 'NONE',  ( 0.000000000000000000, 0.000000000000000000, 1.000000000000000000 ) ) ;
#37994=ORIENTED_EDGE ( 'NONE', *, *, #11186, .T. ) ;
#38007=EDGE_CURVE ( 'NONE', #10617, #23374, #34338, .T. ) ;
#38030=DIRECTION ( 'NONE',  ( -1.000000000000000000, 0.000000000000000000, 0.000000000000000000 ) ) ;
#38046=DIRECTION ( 'NONE',  ( -1.000000000000000000, 0.000000000000000000, -0.000000000000000000 ) ) ;
#38057=CARTESIAN_POINT ( 'NONE',  ( 4.999999999999999112, -2.663952781845850826, -41.91543099594819921 ) ) ;
#38061=CARTESIAN_POINT ( 'NONE',  ( 0.000000000000000000, 0.000000000000000000, 0.000000000000000000 ) ) ;
#38070=ORIENTED_EDGE ( 'NONE', *, *, #32216, .F. ) ;
#38073=ORIENTED_EDGE ( 'NONE', *, *, #2246, .F. ) ;
#38087=LINE ( 'NONE', #27156, #46767 ) ;
#38142=MECHANICAL_DESIGN_GEOMETRIC_PRESENTATION_REPRESENTATION('',(#28528),#34485);
#38144=DIRECTION ( 'NONE',  ( 0.000000000000000000, -0.5877852522924803536, 0.8090169943749422332 ) ) ;
#38152=PLANE ( 'NONE',  #44651 ) ;
#38205=DIRECTION ( 'NONE',  ( 0.000000000000000000, 0.000000000000000000, -1.000000000000000000 ) ) ;
#38207=CARTESIAN_POINT ( 'NONE',  ( 10.00000000000000000, -22.74946021919110706, -29.81001611431033282 ) ) ;
#38228=FACE_OUTER_BOUND ( 'NONE', #41975, .T. ) ;
#38259=EDGE_LOOP ( 'NONE', ( #72373, #24496, #15783, #62746 ) ) ;
#38260=EDGE_CURVE ( 'NONE', #49339, #7677, #39226, .T. ) ;
#38264=CARTESIAN_POINT ( 'NONE',  ( 0.000000000000000000, 29.81001611431009479, 22.74946021919143391 ) ) ;
#38270=VECTOR ( 'NONE', #63247, 1000.000000000000000 ) ;
#38281=ORIENTED_EDGE ( 'NONE', *, *, #55423, .T. ) ;
#38282=DIRECTION ( 'NONE',  ( -1.000000000000000000, -0.000000000000000000, 0.000000000000000000 ) ) ;
#38306=CARTESIAN_POINT ( 'NONE',  ( 10.00000000000000000, 0.000000000000000000, 0.000000000000000000 ) ) ;
#38307=ORIENTED_EDGE ( 'NONE', *, *, #50908, .T. ) ;
#38319=DIRECTION ( 'NONE',  ( 0.000000000000000000, 0.3090169943749482839, -0.9510565162951533091 ) ) ;
#38335=AXIS2_PLACEMENT_3D ( 'NONE', #60454, #32963, #61561 ) ;
#38336=DIRECTION ( 'NONE',  ( -1.000000000000000000, 0.000000000000000000, 0.000000000000000000 ) ) ;
#38350=EDGE_CURVE ( 'NONE', #27866, #42410, #54827, .T. ) ;
#38356=EDGE_CURVE ( 'NONE', #67975, #63433, #36789, .T. ) ;
#38357=DIRECTION ( 'NONE',  ( 0.000000000000000000, 0.9876883405951382144, -0.1564344650402276493 ) ) ;
#38393=AXIS2_PLACEMENT_3D ( 'NONE', #21573, #1203, #62184 ) ;
#38430=CARTESIAN_POINT ( 'NONE',  ( -10.00000000000000000, 0.000000000000000000, 0.000000000000000000 ) ) ;
#38474=ORIENTED_EDGE ( 'NONE', *, *, #41843, .F. ) ;
#38484=DIRECTION ( 'NONE',  ( -1.000000000000000000, -0.000000000000000000, -0.000000000000000000 ) ) ;
#38500=AXIS2_PLACEMENT_3D ( 'NONE', #59606, #46471, #7727 ) ;
#38501=CARTESIAN_POINT ( 'NONE',  ( 0.000000000000000000, -22.64427369931148348, -30.00120703465229965 ) ) ;
#38515=DIRECTION ( 'NONE',  ( -1.000000000000000000, 0.000000000000000000, 0.000000000000000000 ) ) ;
#38516=VECTOR ( 'NONE', #34419, 1000.000000000000000 ) ;
#38519=DIRECTION ( 'NONE',  ( 0.000000000000000000, 0.7431448254773862505, 0.6691306063588671194 ) ) ;
#38534=CARTESIAN_POINT ( 'NONE',  ( 10.00000000000000000, 0.000000000000000000, 0.000000000000000000 ) ) ;
#38550=ORIENTED_EDGE ( 'NONE', *, *, #38792, .T. ) ;
#38553=EDGE_CURVE ( 'NONE', #30220, #7439, #54883, .T. ) ;
#38555=EDGE_CURVE ( 'NONE', #70364, #70056, #24883, .T. ) ;
#38567=CARTESIAN_POINT ( 'NONE',  ( 0.000000000000000000, 23.50000000000000000, 1.499999999999997780 ) ) ;
#38570=DIRECTION ( 'NONE',  ( -1.000000000000000000, -0.000000000000000000, 0.000000000000000000 ) ) ;
#38579=CARTESIAN_POINT ( 'NONE',  ( 0.000000000000000000, -33.17418723428319538, 17.67226234102814431 ) ) ;
#38583=ORIENTED_EDGE ( 'NONE', *, *, #13005, .F. ) ;
#38587=PLANE ( 'NONE',  #8611 ) ;
#38628=AXIS2_PLACEMENT_3D ( 'NONE', #20739, #73715, #66610 ) ;
#38635=CARTESIAN_POINT ( 'NONE',  ( 10.00000000000000000, -33.17418723428294669, -17.67226234102862747 ) ) ;
#38643=EDGE_CURVE ( 'NONE', #67018, #23136, #52495, .T. ) ;
#38645=CARTESIAN_POINT ( 'NONE',  ( 0.000000000000000000, 23.59884966291538078, -12.14883922797231541 ) ) ;
#38653=DIRECTION ( 'NONE',  ( -1.000000000000000000, 0.000000000000000000, 0.000000000000000000 ) ) ;
#38663=CARTESIAN_POINT ( 'NONE',  ( -3.000000000000000000, 8.688484142254221609, -21.88630264137359660 ) ) ;
#38677=CIRCLE ( 'NONE', #67438, 42.00000000000000000 ) ;
#38697=CARTESIAN_POINT ( 'NONE',  ( 0.000000000000000000, -0.9646360437372163421, -23.52805723605591126 ) ) ;
#38720=EDGE_CURVE ( 'NONE', #17753, #70426, #70479, .T. ) ;
#38723=CARTESIAN_POINT ( 'NONE',  ( -3.000000000000000000, -0.9646360437375307573, 23.52805723605590060 ) ) ;
#38731=ADVANCED_FACE ( 'NONE', ( #54000 ), #2158, .T. ) ;
#38743=ORIENTED_EDGE ( 'NONE', *, *, #18607, .T. ) ;
#38760=ORIENTED_EDGE ( 'NONE', *, *, #60793, .F. ) ;
#38769=CARTESIAN_POINT ( 'NONE',  ( 10.00000000000000000, 33.17418723428333749, -17.67226234102790272 ) ) ;
#38772=DIRECTION ( 'NONE',  ( -1.000000000000000000, 0.000000000000000000, 0.000000000000000000 ) ) ;
#38791=DIRECTION ( 'NONE',  ( 0.000000000000000000, 0.000000000000000000, 1.000000000000000000 ) ) ;
#38792=EDGE_CURVE ( 'NONE', #54369, #17536, #8867, .T. ) ;
#38794=DIRECTION ( 'NONE',  ( 0.000000000000000000, -0.7431448254773856954, -0.6691306063588676745 ) ) ;
#38797=DIRECTION ( 'NONE',  ( -1.000000000000000000, -0.000000000000000000, 0.000000000000000000 ) ) ;
#38800=CARTESIAN_POINT ( 'NONE',  ( 10.00000000000000000, 21.40280677340421533, -36.13751322684397138 ) ) ;
#38808=DIRECTION ( 'NONE',  ( 0.000000000000000000, 0.000000000000000000, -1.000000000000000000 ) ) ;
#38809=CARTESIAN_POINT ( 'NONE',  ( 10.00000000000000000, 0.000000000000000000, 0.000000000000000000 ) ) ;
#38822=AXIS2_PLACEMENT_3D ( 'NONE', #58682, #42143, #53411 ) ;
#38833=ORIENTED_EDGE ( 'NONE', *, *, #153, .T. ) ;
#38850=FACE_OUTER_BOUND ( 'NONE', #3248, .T. ) ;
#38862=CARTESIAN_POINT ( 'NONE',  ( -3.000000000000000000, -3.948201729842348850, 23.21447184625293048 ) ) ;
#38902=ORIENTED_EDGE ( 'NONE', *, *, #6160, .F. ) ;
#38907=EDGE_CURVE ( 'NONE', #8315, #69599, #52509, .T. ) ;
#38916=ORIENTED_EDGE ( 'NONE', *, *, #36598, .F. ) ;
#38917=VECTOR ( 'NONE', #19285, 1000.000000000000000 ) ;
#38938=CIRCLE ( 'NONE', #58144, 16.00000000000000000 ) ;
#38939=CARTESIAN_POINT ( 'NONE',  ( 0.000000000000000000, 0.000000000000000000, 0.000000000000000000 ) ) ;
#38941=DIRECTION ( 'NONE',  ( 0.000000000000000000, -6.982962677686267499E-15, 1.000000000000000000 ) ) ;
#38970=CARTESIAN_POINT ( 'NONE',  ( -3.000000000000000000, 8.688484142253939169, 21.88630264137371029 ) ) ;
#38971=VECTOR ( 'NONE', #70474, 1000.000000000000000 ) ;
#38975=VERTEX_POINT ( 'NONE', #51587 ) ;
#38981=DIRECTION ( 'NONE',  ( 1.000000000000000000, 0.000000000000000000, 0.000000000000000000 ) ) ;
#38989=ADVANCED_FACE ( 'NONE', ( #72737 ), #55843, .T. ) ;
#38993=AXIS2_PLACEMENT_3D ( 'NONE', #48554, #25263, #30877 ) ;
#39000=DIRECTION ( 'NONE',  ( -1.000000000000000000, 0.000000000000000000, -0.000000000000000000 ) ) ;
#39004=MANIFOLD_SOLID_BREP ( 'CirPattern1', #4367 ) ;
#39005=LINE ( 'NONE', #74320, #29981 ) ;
#39014=DIRECTION ( 'NONE',  ( -0.000000000000000000, -0.4067366430757898277, -0.9135454576426055295 ) ) ;
#39015=DIRECTION ( 'NONE',  ( 0.000000000000000000, 0.9510565162951503115, 0.3090169943749573878 ) ) ;
#39020=CARTESIAN_POINT ( 'NONE',  ( 0.000000000000000000, -15.48615015657610527, 39.04073710021338428 ) ) ;
#39036=ORIENTED_EDGE ( 'NONE', *, *, #61280, .F. ) ;
#39053=VERTEX_POINT ( 'NONE', #60477 ) ;
#39054=AXIS2_PLACEMENT_3D ( 'NONE', #37502, #42031, #43149 ) ;
#39055=DIRECTION ( 'NONE',  ( -1.000000000000000000, 0.000000000000000000, 0.000000000000000000 ) ) ;
#39061=ORIENTED_EDGE ( 'NONE', *, *, #49915, .T. ) ;
#39080=ADVANCED_FACE ( 'NONE', ( #31875 ), #14966, .F. ) ;
#39083=EDGE_CURVE ( 'NONE', #53177, #22210, #44283, .T. ) ;
#39085=CARTESIAN_POINT ( 'NONE',  ( -3.000000000000000000, 20.85821328998741109, 10.92862929874522315 ) ) ;
#39095=CIRCLE ( 'NONE', #64324, 37.49900000000001654 ) ;
#39108=EDGE_CURVE ( 'NONE', #70987, #28395, #72827, .T. ) ;
#39121=VERTEX_POINT ( 'NONE', #22849 ) ;
#39132=VERTEX_POINT ( 'NONE', #11181 ) ;
#39146=ADVANCED_FACE ( 'NONE', ( #4828 ), #51396, .T. ) ;
#39156=ORIENTED_EDGE ( 'NONE', *, *, #35882, .T. ) ;
#39160=CARTESIAN_POINT ( 'NONE',  ( -3.000000000000000000, 18.84667830672579925, 18.68964196561269020 ) ) ;
#39166=AXIS2_PLACEMENT_3D ( 'NONE', #19535, #20277, #53756 ) ;
#39171=CYLINDRICAL_SURFACE ( 'NONE', #32200, 16.00000000000000000 ) ;
#39180=CARTESIAN_POINT ( 'NONE',  ( -10.00000000000000000, 0.000000000000000000, 0.000000000000000000 ) ) ;
#39185=UNCERTAINTY_MEASURE_WITH_UNIT (LENGTH_MEASURE( 1.000000000000000082E-05 ), #30786, 'distance_accuracy_value', 'NONE');
#39226=CIRCLE ( 'NONE', #3240, 15.99999999999999822 ) ;
#39250=ORIENTED_EDGE ( 'NONE', *, *, #70760, .F. ) ;
#39254=DIRECTION ( 'NONE',  ( -1.000000000000000000, -0.000000000000000000, -0.000000000000000000 ) ) ;
#39260=CARTESIAN_POINT ( 'NONE',  ( 0.000000000000000000, 0.000000000000000000, 0.000000000000000000 ) ) ;
#39269=CARTESIAN_POINT ( 'NONE',  ( 10.00000000000000000, 31.52238457039638320, -27.75498641678709788 ) ) ;
#39271=VECTOR ( 'NONE', #58867, 1000.000000000000000 ) ;
#39274=AXIS2_PLACEMENT_3D ( 'NONE', #35282, #7076, #58577 ) ;
#39285=EDGE_LOOP ( 'NONE', ( #32627, #18255, #61718, #23483 ) ) ;
#39295=ORIENTED_EDGE ( 'NONE', *, *, #17146, .F. ) ;
#39299=CARTESIAN_POINT ( 'NONE',  ( 10.00000000000000000, 41.91543099594818500, 2.663952781846293139 ) ) ;
#39312=DIRECTION ( 'NONE',  ( 0.000000000000000000, 0.000000000000000000, 1.000000000000000000 ) ) ;
#39330=DIRECTION ( 'NONE',  ( -1.000000000000000000, 0.000000000000000000, 0.000000000000000000 ) ) ;
#39345=DIRECTION ( 'NONE',  ( -1.000000000000000000, 0.000000000000000000, -0.000000000000000000 ) ) ;
#39367=ORIENTED_EDGE ( 'NONE', *, *, #32306, .T. ) ;
#39382=CIRCLE ( 'NONE', #16564, 15.99999999999999822 ) ;
#39395=ORIENTED_EDGE ( 'NONE', *, *, #3082, .F. ) ;
#39396=ORIENTED_EDGE ( 'NONE', *, *, #4591, .T. ) ;
#39401=LINE ( 'NONE', #10446, #41387 ) ;
#39404=EDGE_CURVE ( 'NONE', #24232, #50309, #4563, .T. ) ;
#39410=VERTEX_POINT ( 'NONE', #17932 ) ;
#39423=EDGE_CURVE ( 'NONE', #65777, #65222, #45399, .T. ) ;
#39426=CIRCLE ( 'NONE', #72983, 15.99999999999999822 ) ;
#39435=ORIENTED_EDGE ( 'NONE', *, *, #48707, .F. ) ;
#39436=CARTESIAN_POINT ( 'NONE',  ( 0.000000000000000000, 0.000000000000000000, 0.000000000000000000 ) ) ;
#39437=DIRECTION ( 'NONE',  ( -1.000000000000000000, 0.000000000000000000, 0.000000000000000000 ) ) ;
#39463=EDGE_CURVE ( 'NONE', #12105, #1365, #59779, .T. ) ;
#39487=EDGE_LOOP ( 'NONE', ( #60784, #25140, #29372, #63448 ) ) ;
#39494=ORIENTED_EDGE ( 'NONE', *, *, #27227, .F. ) ;
#39500=FACE_OUTER_BOUND ( 'NONE', #1417, .T. ) ;
#39513=ORIENTED_EDGE ( 'NONE', *, *, #20287, .F. ) ;
#39515=CARTESIAN_POINT ( 'NONE',  ( 0.000000000000000000, 0.000000000000000000, 0.000000000000000000 ) ) ;
#39519=ORIENTED_EDGE ( 'NONE', *, *, #42313, .T. ) ;
#39525=FACE_OUTER_BOUND ( 'NONE', #6290, .T. ) ;
#39540=DIRECTION ( 'NONE',  ( 0.000000000000000000, 0.4067366430758017626, -0.9135454576426003115 ) ) ;
#39543=AXIS2_PLACEMENT_3D ( 'NONE', #21729, #6314, #73229 ) ;
#39552=ORIENTED_EDGE ( 'NONE', *, *, #27780, .T. ) ;
#39588=CIRCLE ( 'NONE', #26376, 16.00000000000000000 ) ;
#39600=CYLINDRICAL_SURFACE ( 'NONE', #13958, 37.49900000000000233 ) ;
#39611=DIRECTION ( 'NONE',  ( 0.000000000000000000, 0.000000000000000000, 1.000000000000000000 ) ) ;
#39617=DIRECTION ( 'NONE',  ( 1.000000000000000000, 0.000000000000000000, 0.000000000000000000 ) ) ;
#39632=ORIENTED_EDGE ( 'NONE', *, *, #32306, .F. ) ;
#39634=VECTOR ( 'NONE', #35892, 1000.000000000000000 ) ;
#39648=CARTESIAN_POINT ( 'NONE',  ( -3.000000000000000000, -23.29833615347104825, -3.418703333116803744 ) ) ;
#39658=VECTOR ( 'NONE', #51572, 1000.000000000000000 ) ;
#39667=ORIENTED_EDGE ( 'NONE', *, *, #64343, .F. ) ;
#39671=VERTEX_POINT ( 'NONE', #16362 ) ;
#39673=ORIENTED_EDGE ( 'NONE', *, *, #9187, .T. ) ;
#39682=EDGE_LOOP ( 'NONE', ( #65182, #18470, #22379, #43599 ) ) ;
#39691=CARTESIAN_POINT ( 'NONE',  ( 10.00000000000000000, -37.16516213103273714, -4.992566952385376844 ) ) ;
#39714=AXIS2_PLACEMENT_3D ( 'NONE', #74076, #11297, #34231 ) ;
#39718=VECTOR ( 'NONE', #12908, 1000.000000000000000 ) ;
#39722=CARTESIAN_POINT ( 'NONE',  ( 10.00000000000000000, 0.000000000000000000, 0.000000000000000000 ) ) ;
#39736=CARTESIAN_POINT ( 'NONE',  ( -3.000000000000000000, 0.000000000000000000, 0.000000000000000000 ) ) ;
#39745=VECTOR ( 'NONE', #30280, 1000.000000000000000 ) ;
#39755=AXIS2_PLACEMENT_3D ( 'NONE', #28039, #32928, #21660 ) ;
#39762=CIRCLE ( 'NONE', #2555, 42.00000000000000000 ) ;
#39771=EDGE_LOOP ( 'NONE', ( #8778, #44496, #65486, #34038 ) ) ;
#39772=DIRECTION ( 'NONE',  ( 1.000000000000000000, -0.000000000000000000, -0.000000000000000000 ) ) ;
#39781=VERTEX_POINT ( 'NONE', #30501 ) ;
#39805=ORIENTED_EDGE ( 'NONE', *, *, #63941, .F. ) ;
#39810=CARTESIAN_POINT ( 'NONE',  ( 4.999999999999999112, 2.663952781846732343, -41.91543099594814947 ) ) ;
#39832=CARTESIAN_POINT ( 'NONE',  ( 5.000000000000000000, 31.52238457039637609, -27.75498641678709788 ) ) ;
#39844=DIRECTION ( 'NONE',  ( 0.000000000000000000, 0.000000000000000000, 1.000000000000000000 ) ) ;
#39845=( GEOMETRIC_REPRESENTATION_CONTEXT ( 3 ) GLOBAL_UNCERTAINTY_ASSIGNED_CONTEXT ( ( #67759 ) ) GLOBAL_UNIT_ASSIGNED_CONTEXT ( ( #52252, #30053, #59381 ) ) REPRESENTATION_CONTEXT ( 'NONE', 'WORKASPACE' ) );
#39848=EDGE_CURVE ( 'NONE', #17509, #7975, #52625, .T. ) ;
#39867=CIRCLE ( 'NONE', #49451, 16.00000000000000000 ) ;
#39880=CARTESIAN_POINT ( 'NONE',  ( 10.00000000000000000, 25.88420570971438650, -27.13269053701069566 ) ) ;
#39884=ORIENTED_EDGE ( 'NONE', *, *, #36241, .T. ) ;
#39887=DIRECTION ( 'NONE',  ( -1.000000000000000000, 0.000000000000000000, 0.000000000000000000 ) ) ;
#39914=CYLINDRICAL_SURFACE ( 'NONE', #73417, 16.00000000000000000 ) ;
#39918=DIRECTION ( 'NONE',  ( -1.000000000000000000, 0.000000000000000000, 0.000000000000000000 ) ) ;
#39930=DIRECTION ( 'NONE',  ( -1.000000000000000000, 0.000000000000000000, 0.000000000000000000 ) ) ;
#39931=CARTESIAN_POINT ( 'NONE',  ( -3.000000000000000000, -25.60904388321925396, 6.976881207771172377 ) ) ;
#39947=VECTOR ( 'NONE', #40799, 1000.000000000000227 ) ;
#39948=ORIENTED_EDGE ( 'NONE', *, *, #60609, .F. ) ;
#39966=PRODUCT_CONTEXT ( 'NONE', #56557, 'mechanical' ) ;
#39979=EDGE_LOOP ( 'NONE', ( #72695, #2899, #44098, #53362 ) ) ;
#39982=CARTESIAN_POINT ( 'NONE',  ( 0.000000000000000000, 0.000000000000000000, 0.000000000000000000 ) ) ;
#39985=FACE_OUTER_BOUND ( 'NONE', #33590, .T. ) ;
#39990=CARTESIAN_POINT ( 'NONE',  ( -3.000000000000000000, 9.615535125379096826, -24.73947219025905042 ) ) ;
#39991=VERTEX_POINT ( 'NONE', #49278 ) ;
#39992=ORIENTED_EDGE ( 'NONE', *, *, #26706, .T. ) ;
#39998=CARTESIAN_POINT ( 'NONE',  ( 0.000000000000000000, 36.13751322684449008, -21.40280677340332716 ) ) ;
#40006=AXIS2_PLACEMENT_3D ( 'NONE', #65552, #25687, #32788 ) ;
#40007=CARTESIAN_POINT ( 'NONE',  ( -3.000000000000000000, -23.29833615347104825, -3.418703333116803744 ) ) ;
#40009=CARTESIAN_POINT ( 'NONE',  ( 10.00000000000000000, 37.22597642581158084, 10.79786254984347593 ) ) ;
#40010=DIRECTION ( 'NONE',  ( 0.000000000000000000, -0.7431448254773954654, 0.6691306063588569053 ) ) ;
#40012=VECTOR ( 'NONE', #22761, 1000.000000000000000 ) ;
#40018=ORIENTED_EDGE ( 'NONE', *, *, #32899, .T. ) ;
#40030=DIRECTION ( 'NONE',  ( -1.000000000000000000, 0.000000000000000000, 0.000000000000000000 ) ) ;
#40035=ORIENTED_EDGE ( 'NONE', *, *, #61681, .F. ) ;
#40041=VERTEX_POINT ( 'NONE', #44020 ) ;
#40062=AXIS2_PLACEMENT_3D ( 'NONE', #5295, #5661, #74053 ) ;
#40068=FACE_OUTER_BOUND ( 'NONE', #34772, .T. ) ;
#40069=DIRECTION ( 'NONE',  ( -1.000000000000000000, 0.000000000000000000, 0.000000000000000000 ) ) ;
#40070=EDGE_CURVE ( 'NONE', #44983, #40423, #64653, .T. ) ;
#40073=AXIS2_PLACEMENT_3D ( 'NONE', #12978, #57759, #29903 ) ;
#40076=DIRECTION ( 'NONE',  ( -1.000000000000000000, 0.000000000000000000, 0.000000000000000000 ) ) ;
#40078=ORIENTED_EDGE ( 'NONE', *, *, #2702, .F. ) ;
#40082=CARTESIAN_POINT ( 'NONE',  ( 10.00000000000000000, -29.81001611430991360, -22.74946021919165418 ) ) ;
#40086=ORIENTED_EDGE ( 'NONE', *, *, #52474, .T. ) ;
#40103=AXIS2_PLACEMENT_3D ( 'NONE', #36573, #8008, #30927 ) ;
#40115=DIRECTION ( 'NONE',  ( -1.000000000000000000, -0.000000000000000000, 0.000000000000000000 ) ) ;
#40117=CIRCLE ( 'NONE', #50901, 16.00000000000000000 ) ;
#40127=CARTESIAN_POINT ( 'NONE',  ( 5.000000000000000000, 27.75498641678742473, 31.52238457039609187 ) ) ;
#40142=ADVANCED_FACE ( 'NONE', ( #39500 ), #62442, .T. ) ;
#40157=CARTESIAN_POINT ( 'NONE',  ( 10.00000000000000000, 16.45098606841173705, -33.79645857604496229 ) ) ;
#40169=AXIS2_PLACEMENT_3D ( 'NONE', #13406, #69806, #36335 ) ;
#40174=AXIS2_PLACEMENT_3D ( 'NONE', #3057, #8292, #42511 ) ;
#40176=DIRECTION ( 'NONE',  ( 1.000000000000000000, -0.000000000000000000, 0.000000000000000000 ) ) ;
#40181=AXIS2_PLACEMENT_3D ( 'NONE', #23368, #17713, #40655 ) ;
#40185=DIRECTION ( 'NONE',  ( -1.000000000000000000, -0.000000000000000000, -0.000000000000000000 ) ) ;
#40200=LINE ( 'NONE', #69145, #45552 ) ;
#40202=CARTESIAN_POINT ( 'NONE',  ( -10.00000000000000000, 0.000000000000000000, 0.000000000000000000 ) ) ;
#40223=CARTESIAN_POINT ( 'NONE',  ( 10.00000000000000000, 37.58145647212453611, 0.6853352020791767529 ) ) ;
#40228=CYLINDRICAL_SURFACE ( 'NONE', #36487, 16.00000000000000000 ) ;
#40252=DIRECTION ( 'NONE',  ( 1.000000000000000000, 0.000000000000000000, 0.000000000000000000 ) ) ;
#40256=ORIENTED_EDGE ( 'NONE', *, *, #30538, .T. ) ;
#40279=CARTESIAN_POINT ( 'NONE',  ( 10.00000000000000000, 37.16516213103277977, 4.992566952385115719 ) ) ;
#40281=CARTESIAN_POINT ( 'NONE',  ( 0.000000000000000000, 26.50000000000000711, 1.500000000000000000 ) ) ;
#40298=DIRECTION ( 'NONE',  ( -0.000000000000000000, -0.9135454576426059736, 0.4067366430757887730 ) ) ;
#40307=CARTESIAN_POINT ( 'NONE',  ( -3.000000000000000000, -20.55727247249748046, 16.78983467731285018 ) ) ;
#40309=EDGE_CURVE ( 'NONE', #50450, #18578, #10664, .T. ) ;
#40312=ORIENTED_EDGE ( 'NONE', *, *, #67019, .F. ) ;
#40342=VECTOR ( 'NONE', #19625, 1000.000000000000000 ) ;
#40343=VERTEX_POINT ( 'NONE', #53354 ) ;
#40361=DIRECTION ( 'NONE',  ( 0.000000000000000000, -0.7071067811865536790, 0.7071067811865413555 ) ) ;
#40365=LINE ( 'NONE', #28709, #65562 ) ;
#40368=CARTESIAN_POINT ( 'NONE',  ( -3.000000000000000000, 0.000000000000000000, 0.000000000000000000 ) ) ;
#40371=VECTOR ( 'NONE', #54224, 1000.000000000000000 ) ;
#40384=ORIENTED_EDGE ( 'NONE', *, *, #30953, .F. ) ;
#40391=ORIENTED_EDGE ( 'NONE', *, *, #53289, .F. ) ;
#40402=EDGE_CURVE ( 'NONE', #37124, #44604, #54834, .T. ) ;
#40417=ORIENTED_EDGE ( 'NONE', *, *, #67264, .F. ) ;
#40421=DIRECTION ( 'NONE',  ( 1.000000000000000000, 0.000000000000000000, 0.000000000000000000 ) ) ;
#40423=VERTEX_POINT ( 'NONE', #19871 ) ;
#40434=ORIENTED_EDGE ( 'NONE', *, *, #1133, .F. ) ;
#40436=LINE ( 'NONE', #41185, #38516 ) ;
#40449=ORIENTED_EDGE ( 'NONE', *, *, #13670, .T. ) ;
#40461=AXIS2_PLACEMENT_3D ( 'NONE', #46801, #29115, #6575 ) ;
#40468=DIRECTION ( 'NONE',  ( 1.000000000000000000, 0.000000000000000000, -0.000000000000000000 ) ) ;
#40470=ADVANCED_FACE ( 'NONE', ( #2996 ), #55207, .T. ) ;
#40484=ORIENTED_EDGE ( 'NONE', *, *, #54773, .F. ) ;
#40496=ORIENTED_EDGE ( 'NONE', *, *, #13754, .T. ) ;
#40500=DIRECTION ( 'NONE',  ( 0.000000000000000000, 0.9781476007338044676, 0.2079116908177653100 ) ) ;
#40509=LINE ( 'NONE', #16852, #1156 ) ;
#40519=CARTESIAN_POINT ( 'NONE',  ( 0.000000000000000000, 16.83928648764923253, 16.46020748918050458 ) ) ;
#40544=FACE_OUTER_BOUND ( 'NONE', #31648, .T. ) ;
#40554=ADVANCED_FACE ( 'NONE', ( #20987 ), #67231, .F. ) ;
#40565=CIRCLE ( 'NONE', #50151, 16.00000000000000000 ) ;
#40570=CYLINDRICAL_SURFACE ( 'NONE', #5946, 16.00000000000000000 ) ;
#40574=DIRECTION ( 'NONE',  ( -1.000000000000000000, 0.000000000000000000, 0.000000000000000000 ) ) ;
#40577=ORIENTED_EDGE ( 'NONE', *, *, #18607, .F. ) ;
#40578=DIRECTION ( 'NONE',  ( 0.000000000000000000, 0.1564344650402311743, -0.9876883405951377704 ) ) ;
#40580=ADVANCED_FACE ( 'NONE', ( #56709 ), #50296, .T. ) ;
#40589=CIRCLE ( 'NONE', #33379, 37.49900000000001654 ) ;
#40597=CIRCLE ( 'NONE', #8172, 37.49900000000001654 ) ;
#40600=ORIENTED_EDGE ( 'NONE', *, *, #47858, .T. ) ;
#40601=CARTESIAN_POINT ( 'NONE',  ( -3.000000000000000000, -19.89357724625003598, 12.59942793731059574 ) ) ;
#40617=VECTOR ( 'NONE', #45728, 999.9999999999998863 ) ;
#40638=DIRECTION ( 'NONE',  ( -1.000000000000000000, 0.000000000000000000, 0.000000000000000000 ) ) ;
#40641=DIRECTION ( 'NONE',  ( 0.000000000000000000, -0.5000000000000046629, 0.8660254037844359321 ) ) ;
#40652=AXIS2_PLACEMENT_3D ( 'NONE', #66978, #54960, #67355 ) ;
#40653=EDGE_CURVE ( 'NONE', #56198, #43284, #40509, .T. ) ;
#40655=DIRECTION ( 'NONE',  ( 0.000000000000000000, -1.156482317317870936E-15, -1.000000000000000000 ) ) ;
#40662=DIRECTION ( 'NONE',  ( -1.000000000000000000, -0.000000000000000000, -0.000000000000000000 ) ) ;
#40668=AXIS2_PLACEMENT_3D ( 'NONE', #37266, #3071, #60569 ) ;
#40672=AXIS2_PLACEMENT_3D ( 'NONE', #57594, #40662, #63233 ) ;
#40681=CARTESIAN_POINT ( 'NONE',  ( 10.00000000000000000, -22.74946021919153694, 29.81001611431000597 ) ) ;
#40686=EDGE_CURVE ( 'NONE', #10365, #8213, #47628, .T. ) ;
#40692=CIRCLE ( 'NONE', #4702, 37.49900000000000944 ) ;
#40693=EDGE_LOOP ( 'NONE', ( #15794, #4624, #41408, #20351 ) ) ;
#40704=CARTESIAN_POINT ( 'NONE',  ( 10.00000000000000000, 25.88420570971438650, -27.13269053701069566 ) ) ;
#40726=CARTESIAN_POINT ( 'NONE',  ( 10.00000000000000000, 27.05870788708231700, 26.08949754953034272 ) ) ;
#40739=DIRECTION ( 'NONE',  ( 0.000000000000000000, 0.000000000000000000, 1.000000000000000000 ) ) ;
#40749=CARTESIAN_POINT ( 'NONE',  ( 10.00000000000000000, 0.000000000000000000, 0.000000000000000000 ) ) ;
#40760=ORIENTED_EDGE ( 'NONE', *, *, #9400, .F. ) ;
#40779=EDGE_CURVE ( 'NONE', #12946, #41342, #13050, .T. ) ;
#40799=DIRECTION ( 'NONE',  ( 0.000000000000000000, 0.3090169943749580539, -0.9510565162951500895 ) ) ;
#40811=ORIENTED_EDGE ( 'NONE', *, *, #42973, .T. ) ;
#40817=CARTESIAN_POINT ( 'NONE',  ( -3.000000000000000000, -22.67460108101774807, -6.353146135318215038 ) ) ;
#40830=DIRECTION ( 'NONE',  ( -0.000000000000000000, -0.7431448254773870277, -0.6691306063588662312 ) ) ;
#40841=EDGE_CURVE ( 'NONE', #57048, #16540, #53983, .T. ) ;
#40848=FACE_OUTER_BOUND ( 'NONE', #4482, .T. ) ;
#40866=CIRCLE ( 'NONE', #8455, 16.00000000000000000 ) ;
#40867=DIRECTION ( 'NONE',  ( 0.000000000000000000, -0.1045284632676436454, -0.9945218953682744001 ) ) ;
#40872=DIRECTION ( 'NONE',  ( -1.000000000000000000, -0.000000000000000000, 0.000000000000000000 ) ) ;
#40875=LINE ( 'NONE', #40127, #71122 ) ;
#40881=ORIENTED_EDGE ( 'NONE', *, *, #62775, .F. ) ;
#40894=CARTESIAN_POINT ( 'NONE',  ( 10.00000000000000000, 37.58145647212453611, 0.6853352020791767529 ) ) ;
#40909=ORIENTED_EDGE ( 'NONE', *, *, #42973, .F. ) ;
#40928=DIRECTION ( 'NONE',  ( 0.000000000000000000, 0.000000000000000000, 1.000000000000000000 ) ) ;
#40934=CARTESIAN_POINT ( 'NONE',  ( 4.999999999999999112, 10.41901085202135491, -40.68715046381917944 ) ) ;
#40936=DIRECTION ( 'NONE',  ( -1.000000000000000000, -0.000000000000000000, -0.000000000000000000 ) ) ;
#40962=CARTESIAN_POINT ( 'NONE',  ( -3.000000000000000000, -11.95096189432345390, 23.69967320028757385 ) ) ;
#40969=ORIENTED_EDGE ( 'NONE', *, *, #47541, .F. ) ;
#40976=DIRECTION ( 'NONE',  ( 0.000000000000000000, -0.8090169943749508930, 0.5877852522924683631 ) ) ;
#40993=ORIENTED_EDGE ( 'NONE', *, *, #6807, .T. ) ;
#41002=ORIENTED_EDGE ( 'NONE', *, *, #56090, .T. ) ;
#41020=DIRECTION ( 'NONE',  ( 0.000000000000000000, 0.8660254037844359321, 0.5000000000000046629 ) ) ;
#41039=EDGE_CURVE ( 'NONE', #24232, #35666, #62418, .T. ) ;
#41055=VERTEX_POINT ( 'NONE', #73901 ) ;
#41060=ORIENTED_EDGE ( 'NONE', *, *, #12449, .F. ) ;
#41073=EDGE_CURVE ( 'NONE', #3179, #12067, #48019, .T. ) ;
#41080=CIRCLE ( 'NONE', #8662, 16.00000000000000000 ) ;
#41084=CARTESIAN_POINT ( 'NONE',  ( 0.000000000000000000, 0.000000000000000000, 0.000000000000000000 ) ) ;
#41097=DIRECTION ( 'NONE',  ( 0.000000000000000000, 0.000000000000000000, -1.000000000000000000 ) ) ;
#41101=CARTESIAN_POINT ( 'NONE',  ( -3.000000000000000000, 23.59884966291521380, 12.14883922797262805 ) ) ;
#41103=VECTOR ( 'NONE', #1747, 1000.000000000000000 ) ;
#41111=CYLINDRICAL_SURFACE ( 'NONE', #62611, 42.00000000000000000 ) ;
#41120=CARTESIAN_POINT ( 'NONE',  ( 10.00000000000000000, 21.53537804866126137, -30.80686688396986028 ) ) ;
#41121=DIRECTION ( 'NONE',  ( 1.000000000000000000, -0.000000000000000000, -0.000000000000000000 ) ) ;
#41148=ORIENTED_EDGE ( 'NONE', *, *, #12033, .T. ) ;
#41153=CYLINDRICAL_SURFACE ( 'NONE', #49185, 42.00000000000000000 ) ;
#41160=ORIENTED_EDGE ( 'NONE', *, *, #68411, .F. ) ;
#41171=EDGE_LOOP ( 'NONE', ( #49374, #18113, #66783, #72686 ) ) ;
#41177=EDGE_CURVE ( 'NONE', #26852, #24224, #63647, .T. ) ;
#41178=ORIENTED_EDGE ( 'NONE', *, *, #59831, .F. ) ;
#41184=ORIENTED_EDGE ( 'NONE', *, *, #64279, .T. ) ;
#41185=CARTESIAN_POINT ( 'NONE',  ( 0.000000000000000000, -25.60904388321925396, 6.976881207771172377 ) ) ;
#41186=DIRECTION ( 'NONE',  ( -1.000000000000000000, -0.000000000000000000, -0.000000000000000000 ) ) ;
#41196=VERTEX_POINT ( 'NONE', #630 ) ;
#41202=DIRECTION ( 'NONE',  ( -1.000000000000000000, -0.000000000000000000, -0.000000000000000000 ) ) ;
#41218=ORIENTED_EDGE ( 'NONE', *, *, #32987, .F. ) ;
#41219=AXIS2_PLACEMENT_3D ( 'NONE', #73925, #46856, #28814 ) ;
#41227=EDGE_CURVE ( 'NONE', #51481, #6686, #30260, .T. ) ;
#41231=EDGE_CURVE ( 'NONE', #12484, #60926, #59586, .T. ) ;
#41240=EDGE_LOOP ( 'NONE', ( #37284, #10309, #9806, #66577 ) ) ;
#41260=DIRECTION ( 'NONE',  ( 0.000000000000000000, 1.000000000000000000, 3.469446951953614189E-15 ) ) ;
#41287=VERTEX_POINT ( 'NONE', #23894 ) ;
#41288=DIRECTION ( 'NONE',  ( 0.000000000000000000, -0.8090169943749403458, -0.5877852522924830181 ) ) ;
#41295=DIRECTION ( 'NONE',  ( -1.000000000000000000, 0.000000000000000000, -0.000000000000000000 ) ) ;
#41296=CARTESIAN_POINT ( 'NONE',  ( -10.00000000000000000, 0.000000000000000000, 0.000000000000000000 ) ) ;
#41315=ADVANCED_FACE ( 'NONE', ( #36640 ), #12959, .T. ) ;
#41323=DIRECTION ( 'NONE',  ( 1.000000000000000000, -0.000000000000000000, -0.000000000000000000 ) ) ;
#41342=VERTEX_POINT ( 'NONE', #37768 ) ;
#41348=ORIENTED_EDGE ( 'NONE', *, *, #6161, .T. ) ;
#41353=DIRECTION ( 'NONE',  ( -1.000000000000000000, 0.000000000000000000, 0.000000000000000000 ) ) ;
#41362=ORIENTED_EDGE ( 'NONE', *, *, #8199, .T. ) ;
#41373=DIRECTION ( 'NONE',  ( 1.000000000000000000, -0.000000000000000000, -0.000000000000000000 ) ) ;
#41376=FACE_OUTER_BOUND ( 'NONE', #14597, .T. ) ;
#41382=CARTESIAN_POINT ( 'NONE',  ( 10.00000000000000000, 37.22597642581150268, 5.202137450157037435 ) ) ;
#41387=VECTOR ( 'NONE', #73967, 1000.000000000000000 ) ;
#41400=EDGE_CURVE ( 'NONE', #12406, #60338, #67062, .T. ) ;
#41408=ORIENTED_EDGE ( 'NONE', *, *, #27484, .F. ) ;
#41415=ORIENTED_EDGE ( 'NONE', *, *, #69328, .F. ) ;
#41416=CARTESIAN_POINT ( 'NONE',  ( 0.000000000000000000, 0.000000000000000000, 0.000000000000000000 ) ) ;
#41421=LINE ( 'NONE', #42532, #35216 ) ;
#41430=EDGE_CURVE ( 'NONE', #55748, #35036, #51489, .T. ) ;
#41450=FACE_OUTER_BOUND ( 'NONE', #62379, .T. ) ;
#41472=ORIENTED_EDGE ( 'NONE', *, *, #15971, .T. ) ;
#41477=CYLINDRICAL_SURFACE ( 'NONE', #53738, 37.49900000000000233 ) ;
#41479=DIRECTION ( 'NONE',  ( -1.000000000000000000, 0.000000000000000000, 0.000000000000000000 ) ) ;
#41488=FACE_OUTER_BOUND ( 'NONE', #2562, .T. ) ;
#41491=ADVANCED_FACE ( 'NONE', ( #8816 ), #31736, .T. ) ;
#41506=ORIENTED_EDGE ( 'NONE', *, *, #24012, .T. ) ;
#41519=ORIENTED_EDGE ( 'NONE', *, *, #50554, .T. ) ;
#41524=EDGE_CURVE ( 'NONE', #10838, #11647, #50424, .T. ) ;
#41526=AXIS2_PLACEMENT_3D ( 'NONE', #45208, #17003, #33911 ) ;
#41527=CYLINDRICAL_SURFACE ( 'NONE', #18259, 16.00000000000000000 ) ;
#41547=DIRECTION ( 'NONE',  ( 0.000000000000000000, 0.7071067811865486830, -0.7071067811865463515 ) ) ;
#41568=FACE_OUTER_BOUND ( 'NONE', #55170, .T. ) ;
#41569=AXIS2_PLACEMENT_3D ( 'NONE', #31651, #54958, #3481 ) ;
#41570=AXIS2_PLACEMENT_3D ( 'NONE', #72514, #21014, #43967 ) ;
#41573=LINE ( 'NONE', #2135, #27786 ) ;
#41574=EDGE_LOOP ( 'NONE', ( #402, #44765, #25257, #6121 ) ) ;
#41582=EDGE_CURVE ( 'NONE', #19435, #13842, #16308, .T. ) ;
#41589=AXIS2_PLACEMENT_3D ( 'NONE', #10457, #15733, #55582 ) ;
#41598=AXIS2_PLACEMENT_3D ( 'NONE', #33873, #45165, #50784 ) ;
#41633=CARTESIAN_POINT ( 'NONE',  ( 10.00000000000000000, 0.000000000000000000, 0.000000000000000000 ) ) ;
#41635=DIRECTION ( 'NONE',  ( -1.000000000000000000, 0.000000000000000000, -0.000000000000000000 ) ) ;
#41638=VERTEX_POINT ( 'NONE', #32840 ) ;
#41654=AXIS2_PLACEMENT_3D ( 'NONE', #69839, #39437, #5240 ) ;
#41668=EDGE_LOOP ( 'NONE', ( #44386, #66080, #23259, #36091 ) ) ;
#41674=DIRECTION ( 'NONE',  ( 0.000000000000000000, 0.000000000000000000, 1.000000000000000000 ) ) ;
#41684=CARTESIAN_POINT ( 'NONE',  ( -3.000000000000000000, 23.59884966291538078, -12.14883922797231541 ) ) ;
#41685=ORIENTED_EDGE ( 'NONE', *, *, #2426, .F. ) ;
#41693=ADVANCED_FACE ( 'NONE', ( #17781 ), #42213, .T. ) ;
#41710=SURFACE_STYLE_FILL_AREA ( #53004 ) ;
#41728=LINE ( 'NONE', #19899, #36824 ) ;
#41736=ADVANCED_FACE ( 'NONE', ( #58758 ), #35085, .F. ) ;
#41743=DIRECTION ( 'NONE',  ( 0.000000000000000000, 0.000000000000000000, 1.000000000000000000 ) ) ;
#41756=ADVANCED_FACE ( 'NONE', ( #19261 ), #35447, .F. ) ;
#41762=AXIS2_PLACEMENT_3D ( 'NONE', #71234, #52861, #46858 ) ;
#41783=ORIENTED_EDGE ( 'NONE', *, *, #26210, .F. ) ;
#41787=ORIENTED_EDGE ( 'NONE', *, *, #70496, .F. ) ;
#41794=CIRCLE ( 'NONE', #36970, 42.00000000000000000 ) ;
#41796=ORIENTED_EDGE ( 'NONE', *, *, #39848, .T. ) ;
#41797=ORIENTED_EDGE ( 'NONE', *, *, #4377, .T. ) ;
#41814=CARTESIAN_POINT ( 'NONE',  ( -3.000000000000000000, -20.55727247249748046, 16.78983467731285018 ) ) ;
#41815=AXIS2_PLACEMENT_3D ( 'NONE', #44585, #3633, #39312 ) ;
#41842=CIRCLE ( 'NONE', #9410, 16.00000000000000355 ) ;
#41843=EDGE_CURVE ( 'NONE', #62834, #51153, #20427, .T. ) ;
#41846=DIRECTION ( 'NONE',  ( 0.000000000000000000, 0.000000000000000000, -1.000000000000000000 ) ) ;
#41866=EDGE_CURVE ( 'NONE', #2618, #48989, #19992, .T. ) ;
#41868=CARTESIAN_POINT ( 'NONE',  ( -3.000000000000000000, -18.13022148937263012, 15.02647892043544608 ) ) ;
#41869=LINE ( 'NONE', #13658, #48710 ) ;
#41880=AXIS2_PLACEMENT_3D ( 'NONE', #57595, #27888, #16610 ) ;
#41882=DIRECTION ( 'NONE',  ( 0.000000000000000000, 1.000000000000000000, 3.491481338843133750E-15 ) ) ;
#41886=DIRECTION ( 'NONE',  ( -1.000000000000000000, -0.000000000000000000, -0.000000000000000000 ) ) ;
#41888=AXIS2_PLACEMENT_3D ( 'NONE', #7617, #6162, #6516 ) ;
#41894=ORIENTED_EDGE ( 'NONE', *, *, #33528, .F. ) ;
#41927=CIRCLE ( 'NONE', #37093, 42.00000000000000000 ) ;
#41936=CIRCLE ( 'NONE', #19110, 15.99999999999999822 ) ;
#41937=ADVANCED_FACE ( 'NONE', ( #42572 ), #26744, .T. ) ;
#41943=CARTESIAN_POINT ( 'NONE',  ( -3.000000000000000000, 23.59884966291538078, -12.14883922797231541 ) ) ;
#41958=CARTESIAN_POINT ( 'NONE',  ( -3.000000000000000000, -22.67460108101783334, 6.353146135317912169 ) ) ;
#41967=VERTEX_POINT ( 'NONE', #26380 ) ;
#41969=EDGE_LOOP ( 'NONE', ( #54810, #30127, #5322, #24695 ) ) ;
#41971=ADVANCED_FACE ( 'NONE', ( #31280 ), #54232, .F. ) ;
#41975=EDGE_LOOP ( 'NONE', ( #38833, #65376, #71865, #794, #56135, #43908, #66583, #26446, #44021, #38281, #69319, #60140, #21938, #73980, #48778, #48456, #358, #53244, #36062, #60594, #32564, #70161, #55133, #9033, #5127, #72918, #62535, #29292, #67336, #33367, #64374, #68141, #9689, #60506, #32881, #54642, #50660, #68819, #4056, #66748, #64199, #1978, #21552, #25686, #74145, #20363, #67691, #61191, #23653, #66625, #14525, #32465, #24305, #5123, #1414, #59251, #13937, #34291, #39884, #48531, #42463, #59121, #46413, #24222, #8426, #71198, #55030, #32359, #15145, #55948, #1071, #55, #30692, #233, #12931, #12290, #29733, #54182, #495, #30706, #51634, #20528, #22583, #72276, #55363, #43787, #67678, #43737, #57184, #846, #31882, #73124, #68251, #30574, #32931, #61707, #12452, #27011, #52587, #17611, #46784, #37838, #56697, #22180, #10977, #21234, #37994, #36614, #31957, #57835, #24425, #56227, #2569, #25622, #51066, #54591, #72200, #24626, #10704, #12464, #50027, #7572, #50316, #9132, #37941, #41002, #6928, #7515, #73155, #58192, #40496, #46494, #64447, #49616, #46093, #31965, #12775, #36985, #56214, #7506, #24684, #17656, #20331, #924, #1889, #21438, #46701, #22960, #22290, #51482, #35870, #26153, #65751, #25749, #40760, #61747, #5296, #59099, #33005, #42437, #35946, #8850, #25466, #60219, #40449 ) ) ;
#41976=DIRECTION ( 'NONE',  ( -1.000000000000000000, 0.000000000000000000, 0.000000000000000000 ) ) ;
#41982=DIRECTION ( 'NONE',  ( 1.000000000000000000, 0.000000000000000000, -0.000000000000000000 ) ) ;
#41986=AXIS2_PLACEMENT_3D ( 'NONE', #31730, #49021, #54674 ) ;
#41987=ORIENTED_EDGE ( 'NONE', *, *, #31308, .T. ) ;
#42003=ORIENTED_EDGE ( 'NONE', *, *, #37391, .T. ) ;
#42006=CARTESIAN_POINT ( 'NONE',  ( 0.000000000000000000, -29.81001611430991360, -22.74946021919165418 ) ) ;
#42012=EDGE_LOOP ( 'NONE', ( #53625, #28560, #27452, #57621 ) ) ;
#42031=DIRECTION ( 'NONE',  ( -1.000000000000000000, -0.000000000000000000, 0.000000000000000000 ) ) ;
#42037=CARTESIAN_POINT ( 'NONE',  ( -3.000000000000000000, -0.9646360437375307573, 23.52805723605590060 ) ) ;
#42038=DIRECTION ( 'NONE',  ( 0.000000000000000000, 0.8910065241883657894, 0.4539904997395509678 ) ) ;
#42045=DIRECTION ( 'NONE',  ( 0.000000000000000000, 0.000000000000000000, 1.000000000000000000 ) ) ;
#42047=CIRCLE ( 'NONE', #7203, 42.00000000000000000 ) ;
#42059=AXIS2_PLACEMENT_3D ( 'NONE', #44436, #4588, #72598 ) ;
#42066=ORIENTED_EDGE ( 'NONE', *, *, #66333, .F. ) ;
#42074=EDGE_LOOP ( 'NONE', ( #65420, #45144, #39632, #45225 ) ) ;
#42077=CIRCLE ( 'NONE', #36051, 37.49900000000000233 ) ;
#42087=CARTESIAN_POINT ( 'NONE',  ( -10.00000000000000000, 0.000000000000000000, 0.000000000000000000 ) ) ;
#42118=CARTESIAN_POINT ( 'NONE',  ( 10.00000000000000000, -27.13269053701114331, 25.88420570971391754 ) ) ;
#42136=DIRECTION ( 'NONE',  ( 1.000000000000000000, 0.000000000000000000, 0.000000000000000000 ) ) ;
#42143=DIRECTION ( 'NONE',  ( 0.000000000000000000, 0.9945218953682744001, -0.1045284632676436454 ) ) ;
#42145=DIRECTION ( 'NONE',  ( -1.000000000000000000, 0.000000000000000000, 0.000000000000000000 ) ) ;
#42146=ORIENTED_EDGE ( 'NONE', *, *, #17184, .F. ) ;
#42154=FACE_OUTER_BOUND ( 'NONE', #21139, .T. ) ;
#42161=EDGE_LOOP ( 'NONE', ( #50180, #341, #15411, #51680 ) ) ;
#42174=VECTOR ( 'NONE', #14745, 1000.000000000000227 ) ;
#42177=ADVANCED_FACE ( 'NONE', ( #4408, #43529, #67923, #61174, #66806, #55528, #27303, #38228, #21676, #66442, #67548, #27693, #10775, #14925, #16039, #37870, #49508 ), #50616, .F. ) ;
#42188=DIRECTION ( 'NONE',  ( -1.000000000000000000, 0.000000000000000000, 0.000000000000000000 ) ) ;
#42213=CYLINDRICAL_SURFACE ( 'NONE', #13065, 16.00000000000000000 ) ;
#42241=DIRECTION ( 'NONE',  ( -0.000000000000000000, 0.9781476007338042455, 0.2079116908177664758 ) ) ;
#42255=ORIENTED_EDGE ( 'NONE', *, *, #11631, .T. ) ;
#42260=ORIENTED_EDGE ( 'NONE', *, *, #5539, .F. ) ;
#42271=DIRECTION ( 'NONE',  ( -1.000000000000000000, 0.000000000000000000, 0.000000000000000000 ) ) ;
#42286=DIRECTION ( 'NONE',  ( -1.000000000000000000, 0.000000000000000000, 0.000000000000000000 ) ) ;
#42298=CARTESIAN_POINT ( 'NONE',  ( 5.000000000000000000, -26.79245525562738095, 32.34446384429961796 ) ) ;
#42299=CARTESIAN_POINT ( 'NONE',  ( 10.00000000000000000, 30.80686688397041451, -21.53537804866048688 ) ) ;
#42313=EDGE_CURVE ( 'NONE', #55375, #44604, #68670, .T. ) ;
#42318=DIRECTION ( 'NONE',  ( 0.000000000000000000, 0.000000000000000000, 1.000000000000000000 ) ) ;
#42329=VERTEX_POINT ( 'NONE', #281 ) ;
#42341=FACE_OUTER_BOUND ( 'NONE', #39682, .T. ) ;
#42342=EDGE_CURVE ( 'NONE', #766, #46613, #31009, .T. ) ;
#42344=DIRECTION ( 'NONE',  ( -1.000000000000000000, -0.000000000000000000, 0.000000000000000000 ) ) ;
#42354=EDGE_CURVE ( 'NONE', #33832, #62989, #30624, .T. ) ;
#42368=DIRECTION ( 'NONE',  ( 0.000000000000000000, 0.000000000000000000, -1.000000000000000000 ) ) ;
#42372=AXIS2_PLACEMENT_3D ( 'NONE', #56685, #73951, #16077 ) ;
#42381=AXIS2_PLACEMENT_3D ( 'NONE', #15012, #65788, #65429 ) ;
#42386=DIRECTION ( 'NONE',  ( -0.000000000000000000, -1.156482317317870936E-15, -1.000000000000000000 ) ) ;
#42396=DIRECTION ( 'NONE',  ( 0.000000000000000000, 0.000000000000000000, 1.000000000000000000 ) ) ;
#42406=DIRECTION ( 'NONE',  ( -1.000000000000000000, -0.000000000000000000, -0.000000000000000000 ) ) ;
#42410=VERTEX_POINT ( 'NONE', #18621 ) ;
#42416=AXIS2_PLACEMENT_3D ( 'NONE', #33647, #61493, #58340 ) ;
#42420=DIRECTION ( 'NONE',  ( -0.000000000000000000, -1.156482317317870936E-15, -1.000000000000000000 ) ) ;
#42437=ORIENTED_EDGE ( 'NONE', *, *, #40841, .T. ) ;
#42446=VERTEX_POINT ( 'NONE', #65250 ) ;
#42461=ADVANCED_FACE ( 'NONE', ( #26860 ), #67086, .F. ) ;
#42463=ORIENTED_EDGE ( 'NONE', *, *, #24044, .F. ) ;
#42469=ORIENTED_EDGE ( 'NONE', *, *, #56561, .F. ) ;
#42485=CARTESIAN_POINT ( 'NONE',  ( -3.000000000000000000, 14.60985201121704513, 18.46759930825707841 ) ) ;
#42500=FACE_OUTER_BOUND ( 'NONE', #21798, .T. ) ;
#42511=DIRECTION ( 'NONE',  ( 0.000000000000000000, 0.8660254037844432595, -0.4999999999999920064 ) ) ;
#42532=CARTESIAN_POINT ( 'NONE',  ( 4.999999999999999112, -21.40280677340345505, -36.13751322684441192 ) ) ;
#42536=ADVANCED_FACE ( 'NONE', ( #55059 ), #3590, .T. ) ;
#42544=ORIENTED_EDGE ( 'NONE', *, *, #3119, .F. ) ;
#42547=FACE_OUTER_BOUND ( 'NONE', #24331, .T. ) ;
#42548=ADVANCED_FACE ( 'NONE', ( #8836, #49046 ), #50144, .F. ) ;
#42567=CARTESIAN_POINT ( 'NONE',  ( -3.000000000000000000, -20.55727247249726020, -16.78983467731313084 ) ) ;
#42572=FACE_OUTER_BOUND ( 'NONE', #13588, .T. ) ;
#42576=DIRECTION ( 'NONE',  ( -1.000000000000000000, -0.000000000000000000, 0.000000000000000000 ) ) ;
#42580=DIRECTION ( 'NONE',  ( 0.000000000000000000, 0.9510565162951523099, 0.3090169943749517811 ) ) ;
#42581=CARTESIAN_POINT ( 'NONE',  ( 10.00000000000000000, -0.8828120875903202602, 37.48860685352291000 ) ) ;
#42583=AXIS2_PLACEMENT_3D ( 'NONE', #16246, #72625, #61749 ) ;
#42589=DIRECTION ( 'NONE',  ( -1.000000000000000000, 0.000000000000000000, -0.000000000000000000 ) ) ;
#42600=AXIS2_PLACEMENT_3D ( 'NONE', #16481, #23242, #17590 ) ;
#42608=EDGE_CURVE ( 'NONE', #56328, #37934, #32493, .T. ) ;
#42616=EDGE_CURVE ( 'NONE', #35859, #23719, #14838, .T. ) ;
#42630=CIRCLE ( 'NONE', #26998, 16.00000000000000000 ) ;
#42631=LINE ( 'NONE', #66312, #34764 ) ;
#42636=ORIENTED_EDGE ( 'NONE', *, *, #51348, .F. ) ;
#42642=CARTESIAN_POINT ( 'NONE',  ( -3.000000000000000000, 0.000000000000000000, 0.000000000000000000 ) ) ;
#42646=CARTESIAN_POINT ( 'NONE',  ( -3.000000000000000000, -10.45096189432314837, -21.10159698893440350 ) ) ;
#42677=CARTESIAN_POINT ( 'NONE',  ( 10.00000000000000000, -15.48615015657555816, -39.04073710021360455 ) ) ;
#42683=FACE_OUTER_BOUND ( 'NONE', #16095, .T. ) ;
#42686=AXIS2_PLACEMENT_3D ( 'NONE', #52490, #50466, #50083 ) ;
#42687=CIRCLE ( 'NONE', #4274, 15.99999999999999822 ) ;
#42689=EDGE_CURVE ( 'NONE', #22980, #21912, #50903, .T. ) ;
#42693=CARTESIAN_POINT ( 'NONE',  ( 0.000000000000000000, 41.81611651403868990, -3.925862922255709542 ) ) ;
#42701=ORIENTED_EDGE ( 'NONE', *, *, #46282, .T. ) ;
#42702=VECTOR ( 'NONE', #48211, 1000.000000000000000 ) ;
#42711=ADVANCED_FACE ( 'NONE', ( #46020 ), #17438, .T. ) ;
#42714=CYLINDRICAL_SURFACE ( 'NONE', #16008, 42.00000000000000000 ) ;
#42722=ORIENTED_EDGE ( 'NONE', *, *, #36829, .F. ) ;
#42749=CIRCLE ( 'NONE', #48751, 37.49900000000000944 ) ;
#42759=ORIENTED_EDGE ( 'NONE', *, *, #17608, .T. ) ;
#42761=ORIENTED_EDGE ( 'NONE', *, *, #53289, .T. ) ;
#42778=EDGE_CURVE ( 'NONE', #11835, #35754, #32169, .T. ) ;
#42799=EDGE_CURVE ( 'NONE', #18231, #26331, #16700, .T. ) ;
#42831=ORIENTED_EDGE ( 'NONE', *, *, #26884, .T. ) ;
#42833=ORIENTED_EDGE ( 'NONE', *, *, #68193, .F. ) ;
#42845=ORIENTED_EDGE ( 'NONE', *, *, #30570, .F. ) ;
#42853=DIRECTION ( 'NONE',  ( 0.000000000000000000, 0.2079116908177664480, -0.9781476007338041345 ) ) ;
#42866=VECTOR ( 'NONE', #9756, 1000.000000000000114 ) ;
#42874=DIRECTION ( 'NONE',  ( -1.000000000000000000, 0.000000000000000000, 0.000000000000000000 ) ) ;
#42881=CIRCLE ( 'NONE', #40461, 37.49900000000000944 ) ;
#42889=PLANE ( 'NONE',  #40174 ) ;
#42895=ORIENTED_EDGE ( 'NONE', *, *, #71635, .F. ) ;
#42908=ORIENTED_EDGE ( 'NONE', *, *, #71898, .F. ) ;
#42918=VERTEX_POINT ( 'NONE', #2034 ) ;
#42926=FACE_OUTER_BOUND ( 'NONE', #66746, .T. ) ;
#42936=ORIENTED_EDGE ( 'NONE', *, *, #13987, .F. ) ;
#42939=DIRECTION ( 'NONE',  ( 0.000000000000000000, 0.000000000000000000, -1.000000000000000000 ) ) ;
#42941=DIRECTION ( 'NONE',  ( 0.000000000000000000, 0.3090169943749482839, -0.9510565162951533091 ) ) ;
#42943=CARTESIAN_POINT ( 'NONE',  ( 0.000000000000000000, 10.74501242461333028, -35.92658777277499382 ) ) ;
#42948=DIRECTION ( 'NONE',  ( -1.000000000000000000, -0.000000000000000000, 0.000000000000000000 ) ) ;
#42952=CARTESIAN_POINT ( 'NONE',  ( 10.00000000000000000, -30.80686688396994910, -21.53537804866113703 ) ) ;
#42969=DIRECTION ( 'NONE',  ( 1.000000000000000000, 0.000000000000000000, 0.000000000000000000 ) ) ;
#42973=EDGE_CURVE ( 'NONE', #29448, #4640, #74212, .T. ) ;
#42986=CARTESIAN_POINT ( 'NONE',  ( 10.00000000000000000, -35.92658777277502935, -10.74501242461320594 ) ) ;
#42995=CARTESIAN_POINT ( 'NONE',  ( 10.00000000000000000, -12.26510123303284594, 35.53030884539080603 ) ) ;
#43009=AXIS2_PLACEMENT_3D ( 'NONE', #4051, #3685, #25843 ) ;
#43018=CARTESIAN_POINT ( 'NONE',  ( 10.00000000000000000, -36.88895765772637247, 6.736453364083436313 ) ) ;
#43021=DIRECTION ( 'NONE',  ( -1.000000000000000000, -0.000000000000000000, 0.000000000000000000 ) ) ;
#43047=EDGE_CURVE ( 'NONE', #47629, #64038, #43350, .T. ) ;
#43054=AXIS2_PLACEMENT_3D ( 'NONE', #58690, #30103, #7190 ) ;
#43067=DIRECTION ( 'NONE',  ( 0.000000000000000000, -0.8660254037844363761, -0.5000000000000039968 ) ) ;
#43111=CARTESIAN_POINT ( 'NONE',  ( 0.000000000000000000, -3.925862922256468046, 41.81611651403860463 ) ) ;
#43114=ORIENTED_EDGE ( 'NONE', *, *, #41843, .T. ) ;
#43119=EDGE_CURVE ( 'NONE', #7439, #67004, #56084, .T. ) ;
#43125=CARTESIAN_POINT ( 'NONE',  ( 0.000000000000000000, 26.79245525562762253, -32.34446384429942611 ) ) ;
#43135=AXIS2_PLACEMENT_3D ( 'NONE', #60533, #9757, #67275 ) ;
#43139=LINE ( 'NONE', #19068, #10984 ) ;
#43149=DIRECTION ( 'NONE',  ( 0.000000000000000000, -0.1564344650402172410, -0.9876883405951399908 ) ) ;
#43162=CARTESIAN_POINT ( 'NONE',  ( 10.00000000000000000, 0.000000000000000000, 0.000000000000000000 ) ) ;
#43166=DIRECTION ( 'NONE',  ( 0.000000000000000000, -0.8090169943749531134, 0.5877852522924654766 ) ) ;
#43167=PRODUCT_DEFINITION_CONTEXT ( 'detailed design', #52245, 'design' ) ;
#43184=ORIENTED_EDGE ( 'NONE', *, *, #60968, .F. ) ;
#43194=ORIENTED_EDGE ( 'NONE', *, *, #24304, .F. ) ;
#43236=AXIS2_PLACEMENT_3D ( 'NONE', #64533, #42344, #18652 ) ;
#43249=DIRECTION ( 'NONE',  ( 0.000000000000000000, 0.000000000000000000, 1.000000000000000000 ) ) ;
#43254=CARTESIAN_POINT ( 'NONE',  ( 0.000000000000000000, -0.9646360437372163421, -23.52805723605591126 ) ) ;
#43267=AXIS2_PLACEMENT_3D ( 'NONE', #18108, #12453, #29731 ) ;
#43270=DIRECTION ( 'NONE',  ( -1.000000000000000000, 0.000000000000000000, 0.000000000000000000 ) ) ;
#43272=CARTESIAN_POINT ( 'NONE',  ( 10.00000000000000000, 5.202137450156907761, -37.22597642581151689 ) ) ;
#43284=VERTEX_POINT ( 'NONE', #28614 ) ;
#43292=VECTOR ( 'NONE', #4477, 1000.000000000000000 ) ;
#43305=ORIENTED_EDGE ( 'NONE', *, *, #35783, .T. ) ;
#43323=EDGE_LOOP ( 'NONE', ( #64923, #28767, #61993, #42831 ) ) ;
#43325=CYLINDRICAL_SURFACE ( 'NONE', #6004, 16.00000000000000000 ) ;
#43334=DIRECTION ( 'NONE',  ( -1.000000000000000000, -0.000000000000000000, -0.000000000000000000 ) ) ;
#43350=LINE ( 'NONE', #66986, #72947 ) ;
#43356=DIRECTION ( 'NONE',  ( -1.000000000000000000, 0.000000000000000000, -0.000000000000000000 ) ) ;
#43357=CARTESIAN_POINT ( 'NONE',  ( 10.00000000000000000, 0.000000000000000000, 0.000000000000000000 ) ) ;
#43369=ORIENTED_EDGE ( 'NONE', *, *, #66562, .F. ) ;
#43375=ADVANCED_FACE ( 'NONE', ( #1215 ), #24109, .T. ) ;
#43379=EDGE_CURVE ( 'NONE', #62067, #73125, #1578, .T. ) ;
#43384=ORIENTED_EDGE ( 'NONE', *, *, #26665, .F. ) ;
#43388=ORIENTED_EDGE ( 'NONE', *, *, #13670, .F. ) ;
#43393=ORIENTED_EDGE ( 'NONE', *, *, #53498, .T. ) ;
#43395=AXIS2_PLACEMENT_3D ( 'NONE', #48320, #71232, #19735 ) ;
#43412=VECTOR ( 'NONE', #24706, 1000.000000000000000 ) ;
#43422=LINE ( 'NONE', #49403, #59338 ) ;
#43426=ADVANCED_FACE ( 'NONE', ( #42500 ), #36112, .T. ) ;
#43467=ORIENTED_EDGE ( 'NONE', *, *, #21083, .T. ) ;
#43468=AXIS2_PLACEMENT_3D ( 'NONE', #44668, #32983, #49541 ) ;
#43476=CARTESIAN_POINT ( 'NONE',  ( 0.000000000000000000, 0.000000000000000000, 0.000000000000000000 ) ) ;
#43479=CARTESIAN_POINT ( 'NONE',  ( 0.000000000000000000, 9.615535125378773529, 24.73947219025917121 ) ) ;
#43485=ORIENTED_EDGE ( 'NONE', *, *, #32824, .T. ) ;
#43519=AXIS2_PLACEMENT_3D ( 'NONE', #42299, #37401, #59966 ) ;
#43524=VERTEX_POINT ( 'NONE', #60540 ) ;
#43529=FACE_BOUND ( 'NONE', #16272, .T. ) ;
#43534=CARTESIAN_POINT ( 'NONE',  ( 10.00000000000000000, 3.925862922256769583, -41.81611651403858332 ) ) ;
#43538=CARTESIAN_POINT ( 'NONE',  ( 0.000000000000000000, 12.42422080174688404, -35.38097989696498047 ) ) ;
#43543=CARTESIAN_POINT ( 'NONE',  ( -3.000000000000000000, -19.89357724624987256, -12.59942793731086041 ) ) ;
#43563=DIRECTION ( 'NONE',  ( 0.000000000000000000, -0.8910065241883721177, 0.4539904997395382003 ) ) ;
#43583=ORIENTED_EDGE ( 'NONE', *, *, #68418, .T. ) ;
#43598=CARTESIAN_POINT ( 'NONE',  ( 10.00000000000000000, -3.925862922256464493, 41.81611651403861174 ) ) ;
#43599=ORIENTED_EDGE ( 'NONE', *, *, #52782, .T. ) ;
#43612=CARTESIAN_POINT ( 'NONE',  ( 10.00000000000000000, 12.26510123303308752, -35.53030884539072787 ) ) ;
#43613=CARTESIAN_POINT ( 'NONE',  ( 0.000000000000000000, 40.98264845739763018, -9.188173127306864529 ) ) ;
#43681=ORIENTED_EDGE ( 'NONE', *, *, #70494, .F. ) ;
#43684=FACE_OUTER_BOUND ( 'NONE', #47367, .T. ) ;
#43686=CYLINDRICAL_SURFACE ( 'NONE', #62608, 16.00000000000000000 ) ;
#43687=FACE_OUTER_BOUND ( 'NONE', #25287, .T. ) ;
#43693=DIRECTION ( 'NONE',  ( -1.000000000000000000, 0.000000000000000000, -0.000000000000000000 ) ) ;
#43695=ORIENTED_EDGE ( 'NONE', *, *, #3578, .F. ) ;
#43711=CARTESIAN_POINT ( 'NONE',  ( 10.00000000000000000, -9.188173127307592836, 40.98264845739746676 ) ) ;
#43721=ORIENTED_EDGE ( 'NONE', *, *, #59921, .T. ) ;
#43727=CIRCLE ( 'NONE', #60525, 16.00000000000000355 ) ;
#43731=DIRECTION ( 'NONE',  ( 1.000000000000000000, -0.000000000000000000, -0.000000000000000000 ) ) ;
#43737=ORIENTED_EDGE ( 'NONE', *, *, #43997, .T. ) ;
#43746=EDGE_CURVE ( 'NONE', #32002, #1736, #45517, .T. ) ;
#43748=EDGE_CURVE ( 'NONE', #3791, #50602, #71888, .T. ) ;
#43749=AXIS2_PLACEMENT_3D ( 'NONE', #39722, #51351, #22045 ) ;
#43781=DIRECTION ( 'NONE',  ( 0.000000000000000000, -0.8090169943749403458, -0.5877852522924830181 ) ) ;
#43784=LINE ( 'NONE', #61811, #24195 ) ;
#43786=DIRECTION ( 'NONE',  ( 0.000000000000000000, 0.000000000000000000, -1.000000000000000000 ) ) ;
#43787=ORIENTED_EDGE ( 'NONE', *, *, #69841, .T. ) ;
#43791=DIRECTION ( 'NONE',  ( 1.000000000000000000, -0.000000000000000000, -0.000000000000000000 ) ) ;
#43807=CARTESIAN_POINT ( 'NONE',  ( -3.000000000000000000, -13.04903810567647682, -19.60159698893442481 ) ) ;
#43814=DIRECTION ( 'NONE',  ( 0.000000000000000000, -0.1045284632676429099, -0.9945218953682744001 ) ) ;
#43820=AXIS2_PLACEMENT_3D ( 'NONE', #68258, #61505, #16374 ) ;
#43825=EDGE_CURVE ( 'NONE', #68714, #13386, #15122, .T. ) ;
#43827=CARTESIAN_POINT ( 'NONE',  ( 5.000000000000000000, -31.52238457039619490, 27.75498641678731104 ) ) ;
#43828=EDGE_CURVE ( 'NONE', #14697, #1375, #20405, .T. ) ;
#43837=DIRECTION ( 'NONE',  ( -1.000000000000000000, -0.000000000000000000, -0.000000000000000000 ) ) ;
#43870=AXIS2_PLACEMENT_3D ( 'NONE', #70828, #42286, #14433 ) ;
#43891=AXIS2_PLACEMENT_3D ( 'NONE', #46842, #69759, #28800 ) ;
#43908=ORIENTED_EDGE ( 'NONE', *, *, #5539, .T. ) ;
#43917=EDGE_LOOP ( 'NONE', ( #36791, #30566, #10540, #5197 ) ) ;
#43923=SURFACE_STYLE_FILL_AREA ( #20609 ) ;
#43939=DIRECTION ( 'NONE',  ( 0.000000000000000000, -0.9510565162951502005, -0.3090169943749581094 ) ) ;
#43951=VERTEX_POINT ( 'NONE', #847 ) ;
#43966=ADVANCED_FACE ( 'NONE', ( #10978 ), #68499, .T. ) ;
#43967=DIRECTION ( 'NONE',  ( 0.000000000000000000, 0.4539904997395414754, 0.8910065241883706744 ) ) ;
#43995=DIRECTION ( 'NONE',  ( 1.000000000000000000, 0.000000000000000000, -0.000000000000000000 ) ) ;
#43997=EDGE_CURVE ( 'NONE', #16929, #63232, #47912, .T. ) ;
#44000=VERTEX_POINT ( 'NONE', #6455 ) ;
#44019=EDGE_LOOP ( 'NONE', ( #72059, #58627, #58624, #18423 ) ) ;
#44020=CARTESIAN_POINT ( 'NONE',  ( -3.000000000000000000, 8.688484142254221609, -21.88630264137359660 ) ) ;
#44021=ORIENTED_EDGE ( 'NONE', *, *, #32917, .T. ) ;
#44024=ORIENTED_EDGE ( 'NONE', *, *, #36563, .F. ) ;
#44028=VERTEX_POINT ( 'NONE', #16991 ) ;
#44033=AXIS2_PLACEMENT_3D ( 'NONE', #31276, #37310, #36178 ) ;
#44036=CIRCLE ( 'NONE', #2052, 16.00000000000000000 ) ;
#44039=EDGE_CURVE ( 'NONE', #19772, #64359, #67067, .T. ) ;
#44048=CARTESIAN_POINT ( 'NONE',  ( -3.000000000000000000, -25.60904388321916159, -6.976881207771517879 ) ) ;
#44066=CARTESIAN_POINT ( 'NONE',  ( -3.000000000000000000, 16.61724383029361718, 20.69703378468926402 ) ) ;
#44077=CARTESIAN_POINT ( 'NONE',  ( 10.00000000000000000, 12.42422080174688404, -35.38097989696498047 ) ) ;
#44078=CARTESIAN_POINT ( 'NONE',  ( 5.000000000000000000, -27.75498641678764855, 31.52238457039590358 ) ) ;
#44085=DIRECTION ( 'NONE',  ( -1.000000000000000000, -0.000000000000000000, 0.000000000000000000 ) ) ;
#44092=ORIENTED_EDGE ( 'NONE', *, *, #32602, .F. ) ;
#44098=ORIENTED_EDGE ( 'NONE', *, *, #70170, .T. ) ;
#44110=VERTEX_POINT ( 'NONE', #2325 ) ;
#44114=CARTESIAN_POINT ( 'NONE',  ( 10.00000000000000000, -12.42422080174614862, -35.38097989696524337 ) ) ;
#44134=CARTESIAN_POINT ( 'NONE',  ( 10.00000000000000000, 10.41901085202078114, 40.68715046381932865 ) ) ;
#44138=DIRECTION ( 'NONE',  ( 0.000000000000000000, -0.8090169943749508930, 0.5877852522924682521 ) ) ;
#44151=DIRECTION ( 'NONE',  ( -1.000000000000000000, -0.000000000000000000, -0.000000000000000000 ) ) ;
#44161=CARTESIAN_POINT ( 'NONE',  ( 10.00000000000000000, -30.84782396557233142, 21.32104025579104345 ) ) ;
#44162=PLANE ( 'NONE',  #26873 ) ;
#44181=AXIS2_PLACEMENT_3D ( 'NONE', #32248, #2985, #26243 ) ;
#44182=CARTESIAN_POINT ( 'NONE',  ( -3.000000000000000000, 22.07842321921492612, -8.187992925817130896 ) ) ;
#44193=LINE ( 'NONE', #67868, #40012 ) ;
#44206=AXIS2_PLACEMENT_3D ( 'NONE', #1794, #24679, #57795 ) ;
#44208=CARTESIAN_POINT ( 'NONE',  ( 10.00000000000000000, -22.64427369931148348, -30.00120703465229965 ) ) ;
#44210=DIRECTION ( 'NONE',  ( 0.000000000000000000, 0.000000000000000000, 1.000000000000000000 ) ) ;
#44222=CIRCLE ( 'NONE', #10609, 42.00000000000000000 ) ;
#44234=ORIENTED_EDGE ( 'NONE', *, *, #47032, .T. ) ;
#44238=LINE ( 'NONE', #32935, #47408 ) ;
#44239=DIRECTION ( 'NONE',  ( -1.000000000000000000, 0.000000000000000000, 0.000000000000000000 ) ) ;
#44268=VECTOR ( 'NONE', #49335, 1000.000000000000000 ) ;
#44278=ORIENTED_EDGE ( 'NONE', *, *, #54671, .T. ) ;
#44283=LINE ( 'NONE', #49907, #74141 ) ;
#44285=CIRCLE ( 'NONE', #8210, 16.00000000000000000 ) ;
#44289=ORIENTED_EDGE ( 'NONE', *, *, #36388, .F. ) ;
#44294=VECTOR ( 'NONE', #15400, 1000.000000000000000 ) ;
#44315=AXIS2_PLACEMENT_3D ( 'NONE', #72906, #26328, #38357 ) ;
#44325=AXIS2_PLACEMENT_3D ( 'NONE', #60379, #66020, #66389 ) ;
#44329=VERTEX_POINT ( 'NONE', #31952 ) ;
#44339=CARTESIAN_POINT ( 'NONE',  ( -3.000000000000000000, 0.000000000000000000, 0.000000000000000000 ) ) ;
#44340=CARTESIAN_POINT ( 'NONE',  ( 10.00000000000000000, -17.80606268964563554, 33.00180498840040855 ) ) ;
#44341=CARTESIAN_POINT ( 'NONE',  ( 0.000000000000000000, 16.61724383029361718, 20.69703378468926402 ) ) ;
#44348=CIRCLE ( 'NONE', #19106, 42.00000000000000000 ) ;
#44352=VECTOR ( 'NONE', #24529, 1000.000000000000000 ) ;
#44361=CARTESIAN_POINT ( 'NONE',  ( -3.000000000000000000, 5.835314593368772229, -22.81335362449846826 ) ) ;
#44365=VECTOR ( 'NONE', #35972, 1000.000000000000000 ) ;
#44371=DIRECTION ( 'NONE',  ( 0.000000000000000000, -0.9876883405951393247, 0.1564344650402207104 ) ) ;
#44382=FACE_OUTER_BOUND ( 'NONE', #45859, .T. ) ;
#44386=ORIENTED_EDGE ( 'NONE', *, *, #25235, .F. ) ;
#44389=EDGE_CURVE ( 'NONE', #41196, #53383, #47970, .T. ) ;
#44395=ADVANCED_FACE ( 'NONE', ( #54889 ), #74033, .T. ) ;
#44406=ORIENTED_EDGE ( 'NONE', *, *, #51004, .T. ) ;
#44407=ORIENTED_EDGE ( 'NONE', *, *, #51000, .F. ) ;
#44412=EDGE_CURVE ( 'NONE', #41638, #70257, #20317, .T. ) ;
#44432=ADVANCED_FACE ( 'NONE', ( #17268 ), #45861, .T. ) ;
#44436=CARTESIAN_POINT ( 'NONE',  ( 0.000000000000000000, 0.000000000000000000, 0.000000000000000000 ) ) ;
#44445=PLANE ( 'NONE',  #7595 ) ;
#44455=DIRECTION ( 'NONE',  ( -1.000000000000000000, -0.000000000000000000, -0.000000000000000000 ) ) ;
#44476=ORIENTED_EDGE ( 'NONE', *, *, #58219, .T. ) ;
#44496=ORIENTED_EDGE ( 'NONE', *, *, #55588, .F. ) ;
#44535=AXIS2_PLACEMENT_3D ( 'NONE', #73631, #40185, #33794 ) ;
#44542=CARTESIAN_POINT ( 'NONE',  ( -3.000000000000000000, 16.83928648764923253, 16.46020748918050458 ) ) ;
#44547=EDGE_CURVE ( 'NONE', #48910, #61428, #62413, .T. ) ;
#44567=DIRECTION ( 'NONE',  ( 1.000000000000000000, 0.000000000000000000, 0.000000000000000000 ) ) ;
#44585=CARTESIAN_POINT ( 'NONE',  ( 0.000000000000000000, 0.000000000000000000, 0.000000000000000000 ) ) ;
#44592=CARTESIAN_POINT ( 'NONE',  ( 10.00000000000000000, 0.000000000000000000, 0.000000000000000000 ) ) ;
#44597=EDGE_CURVE ( 'NONE', #40423, #46611, #18730, .T. ) ;
#44604=VERTEX_POINT ( 'NONE', #13825 ) ;
#44610=CARTESIAN_POINT ( 'NONE',  ( 4.999999999999999112, 16.65560815589411092, 38.55633173627015253 ) ) ;
#44616=ORIENTED_EDGE ( 'NONE', *, *, #48876, .F. ) ;
#44626=AXIS2_PLACEMENT_3D ( 'NONE', #8352, #19986, #42941 ) ;
#44633=CYLINDRICAL_SURFACE ( 'NONE', #35289, 37.49900000000000233 ) ;
#44637=CARTESIAN_POINT ( 'NONE',  ( 0.000000000000000000, 17.80606268964585226, -33.00180498840028775 ) ) ;
#44646=EDGE_CURVE ( 'NONE', #31921, #18187, #70975, .T. ) ;
#44650=VECTOR ( 'NONE', #14524, 999.9999999999998863 ) ;
#44651=AXIS2_PLACEMENT_3D ( 'NONE', #20858, #2870, #43814 ) ;
#44658=CARTESIAN_POINT ( 'NONE',  ( 10.00000000000000000, 16.45098606841126454, 33.79645857604518966 ) ) ;
#44668=CARTESIAN_POINT ( 'NONE',  ( 10.00000000000000000, 0.000000000000000000, 0.000000000000000000 ) ) ;
#44669=EDGE_CURVE ( 'NONE', #4640, #17707, #68427, .T. ) ;
#44691=AXIS2_PLACEMENT_3D ( 'NONE', #13322, #58826, #6225 ) ;
#44719=CARTESIAN_POINT ( 'NONE',  ( 10.00000000000000000, -37.48860685352291711, 0.8828120875899322373 ) ) ;
#44723=CARTESIAN_POINT ( 'NONE',  ( 10.00000000000000000, -36.88895765772628010, -6.736453364083947015 ) ) ;
#44740=EDGE_CURVE ( 'NONE', #27990, #62190, #26597, .T. ) ;
#44744=ADVANCED_FACE ( 'NONE', ( #54076 ), #26961, .T. ) ;
#44746=VECTOR ( 'NONE', #70293, 1000.000000000000000 ) ;
#44758=DIRECTION ( 'NONE',  ( 0.000000000000000000, -0.5877852522924689183, -0.8090169943749504489 ) ) ;
#44765=ORIENTED_EDGE ( 'NONE', *, *, #4695, .F. ) ;
#44769=CARTESIAN_POINT ( 'NONE',  ( 10.00000000000000178, 0.000000000000000000, 0.000000000000000000 ) ) ;
#44789=VECTOR ( 'NONE', #13394, 1000.000000000000000 ) ;
#44791=CARTESIAN_POINT ( 'NONE',  ( 0.000000000000000000, 22.07842321921492612, -8.187992925817130896 ) ) ;
#44805=LINE ( 'NONE', #39160, #35558 ) ;
#44807=DIRECTION ( 'NONE',  ( 0.000000000000000000, 0.000000000000000000, 1.000000000000000000 ) ) ;
#44810=LINE ( 'NONE', #21867, #56982 ) ;
#44814=CARTESIAN_POINT ( 'NONE',  ( 0.000000000000000000, -23.29833615347109443, 3.418703333116492438 ) ) ;
#44833=ADVANCED_FACE ( 'NONE', ( #9304 ), #32225, .T. ) ;
#44843=DIRECTION ( 'NONE',  ( -1.000000000000000000, 0.000000000000000000, 0.000000000000000000 ) ) ;
#44853=ORIENTED_EDGE ( 'NONE', *, *, #153, .F. ) ;
#44857=EDGE_LOOP ( 'NONE', ( #15631, #60136, #10167, #44289 ) ) ;
#44861=DIRECTION ( 'NONE',  ( -1.000000000000000000, 0.000000000000000000, 0.000000000000000000 ) ) ;
#44870=CYLINDRICAL_SURFACE ( 'NONE', #45020, 37.49900000000000233 ) ;
#44890=FACE_OUTER_BOUND ( 'NONE', #45074, .T. ) ;
#44909=CARTESIAN_POINT ( 'NONE',  ( 0.000000000000000000, -3.948201729842037544, -23.21447184625298021 ) ) ;
#44925=DIRECTION ( 'NONE',  ( -0.000000000000000000, -0.2079116908177653378, 0.9781476007338044676 ) ) ;
#44926=DIRECTION ( 'NONE',  ( 0.000000000000000000, 0.9876883405951382144, -0.1564344650402276493 ) ) ;
#44936=ORIENTED_EDGE ( 'NONE', *, *, #26910, .T. ) ;
#44938=ADVANCED_FACE ( 'NONE', ( #51381 ), #67947, .F. ) ;
#44944=ORIENTED_EDGE ( 'NONE', *, *, #31422, .T. ) ;
#44946=DIRECTION ( 'NONE',  ( 0.000000000000000000, -0.3090169943749548342, 0.9510565162951511997 ) ) ;
#44952=ORIENTED_EDGE ( 'NONE', *, *, #20207, .T. ) ;
#44960=DIRECTION ( 'NONE',  ( -1.000000000000000000, 0.000000000000000000, 0.000000000000000000 ) ) ;
#44964=CARTESIAN_POINT ( 'NONE',  ( 10.00000000000000000, -37.16516213103273714, -4.992566952385376844 ) ) ;
#44969=ORIENTED_EDGE ( 'NONE', *, *, #38907, .T. ) ;
#44976=DIRECTION ( 'NONE',  ( 1.000000000000000000, -0.000000000000000000, -0.000000000000000000 ) ) ;
#44983=VERTEX_POINT ( 'NONE', #21698 ) ;
#44985=EDGE_CURVE ( 'NONE', #67887, #11862, #39005, .T. ) ;
#45008=CARTESIAN_POINT ( 'NONE',  ( 0.000000000000000000, -21.40280677340345505, -36.13751322684441192 ) ) ;
#45020=AXIS2_PLACEMENT_3D ( 'NONE', #73787, #50493, #32082 ) ;
#45031=VECTOR ( 'NONE', #37891, 1000.000000000000000 ) ;
#45045=FACE_OUTER_BOUND ( 'NONE', #49123, .T. ) ;
#45055=AXIS2_PLACEMENT_3D ( 'NONE', #64491, #11858, #17881 ) ;
#45074=EDGE_LOOP ( 'NONE', ( #14806, #41787, #35225, #52612 ) ) ;
#45075=LINE ( 'NONE', #67997, #54029 ) ;
#45076=CYLINDRICAL_SURFACE ( 'NONE', #5283, 16.00000000000000000 ) ;
#45089=DIRECTION ( 'NONE',  ( -0.000000000000000000, 0.4067366430758000417, -0.9135454576426009776 ) ) ;
#45101=LINE ( 'NONE', #20400, #7291 ) ;
#45103=CIRCLE ( 'NONE', #69081, 42.00000000000000000 ) ;
#45126=ORIENTED_EDGE ( 'NONE', *, *, #22921, .F. ) ;
#45144=ORIENTED_EDGE ( 'NONE', *, *, #52444, .F. ) ;
#45165=DIRECTION ( 'NONE',  ( -1.000000000000000000, -0.000000000000000000, -0.000000000000000000 ) ) ;
#45174=CARTESIAN_POINT ( 'NONE',  ( 10.00000000000000000, 31.52238457039599595, 27.75498641678753842 ) ) ;
#45185=EDGE_CURVE ( 'NONE', #39781, #68825, #4626, .T. ) ;
#45205=CARTESIAN_POINT ( 'NONE',  ( 0.000000000000000000, -22.32062822937469804, -14.36278369418829826 ) ) ;
#45208=CARTESIAN_POINT ( 'NONE',  ( 0.000000000000000000, 0.000000000000000000, 0.000000000000000000 ) ) ;
#45216=CARTESIAN_POINT ( 'NONE',  ( 0.000000000000000000, -11.95096189432345390, 23.69967320028757385 ) ) ;
#45221=ORIENTED_EDGE ( 'NONE', *, *, #66629, .F. ) ;
#45225=ORIENTED_EDGE ( 'NONE', *, *, #31409, .F. ) ;
#45228=EDGE_LOOP ( 'NONE', ( #58912, #46315, #21628, #46182 ) ) ;
#45241=EDGE_CURVE ( 'NONE', #54986, #55937, #12060, .T. ) ;
#45245=CYLINDRICAL_SURFACE ( 'NONE', #15142, 16.00000000000000000 ) ;
#45246=CYLINDRICAL_SURFACE ( 'NONE', #31205, 37.49900000000000233 ) ;
#45256=CARTESIAN_POINT ( 'NONE',  ( 10.00000000000000000, 0.6853352020795618893, -37.58145647212453611 ) ) ;
#45266=VECTOR ( 'NONE', #27364, 1000.000000000000000 ) ;
#45273=CARTESIAN_POINT ( 'NONE',  ( 0.000000000000000000, 4.992566952384984269, 37.16516213103279398 ) ) ;
#45276=CARTESIAN_POINT ( 'NONE',  ( 10.00000000000000000, 3.925862922256160736, 41.81611651403863306 ) ) ;
#45299=ORIENTED_EDGE ( 'NONE', *, *, #3082, .T. ) ;
#45313=EDGE_LOOP ( 'NONE', ( #31677, #31160, #63077, #1363 ) ) ;
#45337=CARTESIAN_POINT ( 'NONE',  ( 0.000000000000000000, 35.92658777277525672, -10.74501242461245809 ) ) ;
#45352=CYLINDRICAL_SURFACE ( 'NONE', #16241, 37.49900000000000233 ) ;
#45354=DIRECTION ( 'NONE',  ( 0.000000000000000000, 0.000000000000000000, 1.000000000000000000 ) ) ;
#45355=EDGE_CURVE ( 'NONE', #59768, #59223, #7239, .T. ) ;
#45361=EDGE_CURVE ( 'NONE', #26842, #22221, #5733, .T. ) ;
#45364=ADVANCED_FACE ( 'NONE', ( #52312 ), #69607, .T. ) ;
#45384=LINE ( 'NONE', #22441, #46843 ) ;
#45386=CIRCLE ( 'NONE', #12929, 21.00000000000000000 ) ;
#45389=EDGE_LOOP ( 'NONE', ( #58991, #5391, #48668, #64482 ) ) ;
#45399=CIRCLE ( 'NONE', #53757, 37.49900000000000944 ) ;
#45405=AXIS2_PLACEMENT_3D ( 'NONE', #31295, #25661, #54249 ) ;
#45408=CARTESIAN_POINT ( 'NONE',  ( 10.00000000000000000, -17.67226234102849958, 33.17418723428301774 ) ) ;
#45409=EDGE_CURVE ( 'NONE', #9559, #37478, #29008, .T. ) ;
#45419=EDGE_LOOP ( 'NONE', ( #13298, #19488, #69630, #62830 ) ) ;
#45437=ORIENTED_EDGE ( 'NONE', *, *, #42616, .T. ) ;
#45442=VERTEX_POINT ( 'NONE', #13561 ) ;
#45448=AXIS2_PLACEMENT_3D ( 'NONE', #16054, #25214, #47759 ) ;
#45459=CARTESIAN_POINT ( 'NONE',  ( 10.00000000000000000, -26.08949754953044220, 27.05870788708222818 ) ) ;
#45484=DIRECTION ( 'NONE',  ( -1.000000000000000000, 0.000000000000000000, 0.000000000000000000 ) ) ;
#45487=DIRECTION ( 'NONE',  ( -1.000000000000000000, -0.000000000000000000, -0.000000000000000000 ) ) ;
#45490=AXIS2_PLACEMENT_3D ( 'NONE', #41120, #70776, #70035 ) ;
#45491=DIRECTION ( 'NONE',  ( -1.000000000000000000, -0.000000000000000000, -0.000000000000000000 ) ) ;
#45517=CIRCLE ( 'NONE', #17857, 42.00000000000000000 ) ;
#45518=ORIENTED_EDGE ( 'NONE', *, *, #36133, .F. ) ;
#45545=AXIS2_PLACEMENT_3D ( 'NONE', #38769, #55316, #14719 ) ;
#45551=CIRCLE ( 'NONE', #2362, 37.49900000000000233 ) ;
#45552=VECTOR ( 'NONE', #6719, 1000.000000000000000 ) ;
#45556=DIRECTION ( 'NONE',  ( 0.000000000000000000, 0.000000000000000000, 1.000000000000000000 ) ) ;
#45568=CARTESIAN_POINT ( 'NONE',  ( 5.000000000000000000, 21.40280677340421889, -36.13751322684397138 ) ) ;
#45585=FACE_OUTER_BOUND ( 'NONE', #52518, .T. ) ;
#45606=VERTEX_POINT ( 'NONE', #1960 ) ;
#45614=AXIS2_PLACEMENT_3D ( 'NONE', #53662, #12326, #53292 ) ;
#45618=EDGE_CURVE ( 'NONE', #54954, #56201, #15043, .T. ) ;
#45622=AXIS2_PLACEMENT_3D ( 'NONE', #33685, #56639, #5138 ) ;
#45634=EDGE_CURVE ( 'NONE', #52314, #32720, #62368, .T. ) ;
#45640=PLANE ( 'NONE',  #70945 ) ;
#45661=CARTESIAN_POINT ( 'NONE',  ( 4.999999999999999112, -40.98264845739743123, -9.188173127307734944 ) ) ;
#45662=PLANE ( 'NONE',  #46597 ) ;
#45665=CYLINDRICAL_SURFACE ( 'NONE', #13703, 42.00000000000000000 ) ;
#45674=CYLINDRICAL_SURFACE ( 'NONE', #23320, 37.49900000000000233 ) ;
#45677=CIRCLE ( 'NONE', #27620, 37.49900000000000233 ) ;
#45704=ORIENTED_EDGE ( 'NONE', *, *, #68681, .F. ) ;
#45728=DIRECTION ( 'NONE',  ( -0.000000000000000000, -0.2079116908177653378, 0.9781476007338044676 ) ) ;
#45731=DIRECTION ( 'NONE',  ( 0.000000000000000000, 0.000000000000000000, 1.000000000000000000 ) ) ;
#45733=ORIENTED_EDGE ( 'NONE', *, *, #44646, .T. ) ;
#45743=CARTESIAN_POINT ( 'NONE',  ( 0.000000000000000000, 0.000000000000000000, 0.000000000000000000 ) ) ;
#45764=CARTESIAN_POINT ( 'NONE',  ( -3.000000000000000000, -26.23277895567245821, -4.042438405570103477 ) ) ;
#45767=AXIS2_PLACEMENT_3D ( 'NONE', #30630, #46461, #69386 ) ;
#45768=EDGE_CURVE ( 'NONE', #8213, #21151, #11888, .T. ) ;
#45820=VECTOR ( 'NONE', #72880, 1000.000000000000227 ) ;
#45826=AXIS2_PLACEMENT_3D ( 'NONE', #27283, #27669, #50595 ) ;
#45839=DIRECTION ( 'NONE',  ( -1.000000000000000000, 0.000000000000000000, 0.000000000000000000 ) ) ;
#45851=EDGE_CURVE ( 'NONE', #22210, #20975, #52745, .T. ) ;
#45854=CARTESIAN_POINT ( 'NONE',  ( 10.00000000000000000, 0.000000000000000000, 0.000000000000000000 ) ) ;
#45859=EDGE_LOOP ( 'NONE', ( #18405, #4172, #57074, #220 ) ) ;
#45860=EDGE_CURVE ( 'NONE', #19435, #13671, #60436, .T. ) ;
#45861=CYLINDRICAL_SURFACE ( 'NONE', #62374, 42.00000000000000000 ) ;
#45888=EDGE_LOOP ( 'NONE', ( #28117, #41160, #20703, #71461 ) ) ;
#45898=CARTESIAN_POINT ( 'NONE',  ( -3.000000000000000000, 16.83928648764923253, 16.46020748918050458 ) ) ;
#45900=ORIENTED_EDGE ( 'NONE', *, *, #24012, .F. ) ;
#45936=VECTOR ( 'NONE', #13166, 1000.000000000000000 ) ;
#45941=LINE ( 'NONE', #68866, #53690 ) ;
#45968=ORIENTED_EDGE ( 'NONE', *, *, #31414, .T. ) ;
#45972=ORIENTED_EDGE ( 'NONE', *, *, #21305, .F. ) ;
#45990=ORIENTED_EDGE ( 'NONE', *, *, #9485, .T. ) ;
#46012=CARTESIAN_POINT ( 'NONE',  ( -10.00000000000000000, 0.000000000000000000, 0.000000000000000000 ) ) ;
#46020=FACE_OUTER_BOUND ( 'NONE', #45389, .T. ) ;
#46022=CARTESIAN_POINT ( 'NONE',  ( 0.000000000000000000, 9.188173127307898369, -40.98264845739739570 ) ) ;
#46023=DIRECTION ( 'NONE',  ( -1.000000000000000000, 0.000000000000000000, 0.000000000000000000 ) ) ;
#46024=PLANE ( 'NONE',  #20891 ) ;
#46025=LINE ( 'NONE', #44542, #14242 ) ;
#46055=CARTESIAN_POINT ( 'NONE',  ( 10.00000000000000000, 27.75498641678742473, 31.52238457039609898 ) ) ;
#46064=DIRECTION ( 'NONE',  ( 0.000000000000000000, 0.000000000000000000, 1.000000000000000000 ) ) ;
#46073=ORIENTED_EDGE ( 'NONE', *, *, #70656, .T. ) ;
#46089=AXIS2_PLACEMENT_3D ( 'NONE', #34630, #6086, #46291 ) ;
#46093=ORIENTED_EDGE ( 'NONE', *, *, #68504, .F. ) ;
#46097=DIRECTION ( 'NONE',  ( -1.000000000000000000, 0.000000000000000000, 0.000000000000000000 ) ) ;
#46100=AXIS2_PLACEMENT_3D ( 'NONE', #30149, #53458, #24884 ) ;
#46102=DIRECTION ( 'NONE',  ( -1.000000000000000000, -0.000000000000000000, -0.000000000000000000 ) ) ;
#46121=EDGE_CURVE ( 'NONE', #71727, #15277, #34401, .T. ) ;
#46128=DIRECTION ( 'NONE',  ( 0.000000000000000000, -0.9135454576426056406, 0.4067366430757897722 ) ) ;
#46157=ORIENTED_EDGE ( 'NONE', *, *, #34921, .F. ) ;
#46167=ORIENTED_EDGE ( 'NONE', *, *, #41177, .T. ) ;
#46168=DIRECTION ( 'NONE',  ( 0.000000000000000000, -0.7431448254773954654, 0.6691306063588569053 ) ) ;
#46181=EDGE_CURVE ( 'NONE', #66145, #36593, #29974, .T. ) ;
#46182=ORIENTED_EDGE ( 'NONE', *, *, #60467, .T. ) ;
#46204=LINE ( 'NONE', #40934, #72823 ) ;
#46215=ORIENTED_EDGE ( 'NONE', *, *, #65602, .T. ) ;
#46222=ORIENTED_EDGE ( 'NONE', *, *, #45241, .F. ) ;
#46230=VECTOR ( 'NONE', #41353, 1000.000000000000000 ) ;
#46245=ORIENTED_EDGE ( 'NONE', *, *, #30198, .F. ) ;
#46248=VECTOR ( 'NONE', #49486, 1000.000000000000000 ) ;
#46257=EDGE_CURVE ( 'NONE', #22414, #3329, #51704, .T. ) ;
#46258=AXIS2_PLACEMENT_3D ( 'NONE', #47210, #30636, #2502 ) ;
#46259=EDGE_LOOP ( 'NONE', ( #66948, #20140, #28049, #51209 ) ) ;
#46265=CARTESIAN_POINT ( 'NONE',  ( 0.000000000000000000, 0.000000000000000000, 0.000000000000000000 ) ) ;
#46273=DIRECTION ( 'NONE',  ( -1.000000000000000000, 0.000000000000000000, 0.000000000000000000 ) ) ;
#46277=CIRCLE ( 'NONE', #13828, 37.49900000000000233 ) ;
#46282=EDGE_CURVE ( 'NONE', #1736, #30220, #34760, .T. ) ;
#46286=AXIS2_PLACEMENT_3D ( 'NONE', #6253, #47237, #47598 ) ;
#46291=DIRECTION ( 'NONE',  ( 0.000000000000000000, 0.000000000000000000, 1.000000000000000000 ) ) ;
#46296=DIRECTION ( 'NONE',  ( -1.000000000000000000, 0.000000000000000000, 0.000000000000000000 ) ) ;
#46301=VECTOR ( 'NONE', #47833, 1000.000000000000000 ) ;
#46315=ORIENTED_EDGE ( 'NONE', *, *, #55067, .F. ) ;
#46322=ORIENTED_EDGE ( 'NONE', *, *, #61640, .F. ) ;
#46326=ORIENTED_EDGE ( 'NONE', *, *, #35733, .T. ) ;
#46334=ORIENTED_EDGE ( 'NONE', *, *, #56396, .F. ) ;
#46365=DIRECTION ( 'NONE',  ( 1.000000000000000000, -0.000000000000000000, -0.000000000000000000 ) ) ;
#46369=ORIENTED_EDGE ( 'NONE', *, *, #45409, .T. ) ;
#46371=EDGE_CURVE ( 'NONE', #35258, #10635, #18956, .T. ) ;
#46374=CARTESIAN_POINT ( 'NONE',  ( -10.00000000000000000, 0.000000000000000000, 0.000000000000000000 ) ) ;
#46375=CARTESIAN_POINT ( 'NONE',  ( 10.00000000000000000, -16.23288003029473359, -33.80338159004301701 ) ) ;
#46380=CARTESIAN_POINT ( 'NONE',  ( 0.000000000000000000, -41.81611651403859042, -3.925862922256606602 ) ) ;
#46400=ORIENTED_EDGE ( 'NONE', *, *, #47523, .T. ) ;
#46413=ORIENTED_EDGE ( 'NONE', *, *, #1254, .T. ) ;
#46417=VERTEX_POINT ( 'NONE', #33570 ) ;
#46429=FACE_OUTER_BOUND ( 'NONE', #61599, .T. ) ;
#46438=ORIENTED_EDGE ( 'NONE', *, *, #62895, .T. ) ;
#46448=AXIS2_PLACEMENT_3D ( 'NONE', #36149, #47798, #8319 ) ;
#46449=DIRECTION ( 'NONE',  ( -1.000000000000000000, 0.000000000000000000, 0.000000000000000000 ) ) ;
#46454=ORIENTED_EDGE ( 'NONE', *, *, #11523, .F. ) ;
#46461=DIRECTION ( 'NONE',  ( 1.000000000000000000, 0.000000000000000000, 0.000000000000000000 ) ) ;
#46463=ADVANCED_FACE ( 'NONE', ( #73421 ), #45246, .T. ) ;
#46467=AXIS2_PLACEMENT_3D ( 'NONE', #8503, #65646, #49083 ) ;
#46471=DIRECTION ( 'NONE',  ( -1.000000000000000000, -0.000000000000000000, -0.000000000000000000 ) ) ;
#46473=DIRECTION ( 'NONE',  ( 0.000000000000000000, 0.8090169943749445647, 0.5877852522924770229 ) ) ;
#46489=ORIENTED_EDGE ( 'NONE', *, *, #40070, .T. ) ;
#46492=CARTESIAN_POINT ( 'NONE',  ( -3.000000000000000000, -3.948201729842038432, -23.21447184625298021 ) ) ;
#46494=ORIENTED_EDGE ( 'NONE', *, *, #31579, .T. ) ;
#46523=PLANE ( 'NONE',  #72195 ) ;
#46530=VERTEX_POINT ( 'NONE', #55773 ) ;
#46536=LINE ( 'NONE', #11943, #36297 ) ;
#46546=ORIENTED_EDGE ( 'NONE', *, *, #41073, .F. ) ;
#46552=CARTESIAN_POINT ( 'NONE',  ( -3.000000000000000000, 23.50000000000000000, 1.499999999999997780 ) ) ;
#46556=LINE ( 'NONE', #58201, #70249 ) ;
#46568=DIRECTION ( 'NONE',  ( -1.000000000000000000, 0.000000000000000000, 0.000000000000000000 ) ) ;
#46579=FACE_OUTER_BOUND ( 'NONE', #8614, .T. ) ;
#46589=EDGE_LOOP ( 'NONE', ( #57287, #52626, #17667, #24359 ) ) ;
#46597=AXIS2_PLACEMENT_3D ( 'NONE', #40007, #5438, #28335 ) ;
#46603=AXIS2_PLACEMENT_3D ( 'NONE', #31653, #48222, #53122 ) ;
#46611=VERTEX_POINT ( 'NONE', #894 ) ;
#46613=VERTEX_POINT ( 'NONE', #63280 ) ;
#46642=CARTESIAN_POINT ( 'NONE',  ( 10.00000000000000000, 33.80338159004307386, -16.23288003029461279 ) ) ;
#46665=ORIENTED_EDGE ( 'NONE', *, *, #59076, .F. ) ;
#46670=AXIS2_PLACEMENT_3D ( 'NONE', #16338, #52024, #34365 ) ;
#46675=CARTESIAN_POINT ( 'NONE',  ( 50.00005079999999680, 0.000000000000000000, 0.000000000000000000 ) ) ;
#46687=DIRECTION ( 'NONE',  ( -1.000000000000000000, 0.000000000000000000, 0.000000000000000000 ) ) ;
#46698=EDGE_CURVE ( 'NONE', #26852, #62900, #45677, .T. ) ;
#46701=ORIENTED_EDGE ( 'NONE', *, *, #54809, .F. ) ;
#46718=DIRECTION ( 'NONE',  ( 0.000000000000000000, -0.9510565162951500895, -0.3090169943749583314 ) ) ;
#46720=DIRECTION ( 'NONE',  ( -1.000000000000000000, 0.000000000000000000, 0.000000000000000000 ) ) ;
#46730=DIRECTION ( 'NONE',  ( -1.000000000000000000, -0.000000000000000000, -0.000000000000000000 ) ) ;
#46735=CIRCLE ( 'NONE', #14301, 42.00000000000000000 ) ;
#46741=VECTOR ( 'NONE', #48020, 1000.000000000000000 ) ;
#46746=LINE ( 'NONE', #17786, #12689 ) ;
#46759=CARTESIAN_POINT ( 'NONE',  ( 10.00000000000000000, -26.08949754953044220, 27.05870788708222818 ) ) ;
#46767=VECTOR ( 'NONE', #62528, 1000.000000000000000 ) ;
#46776=EDGE_CURVE ( 'NONE', #64038, #22283, #70738, .T. ) ;
#46781=ORIENTED_EDGE ( 'NONE', *, *, #60968, .T. ) ;
#46784=ORIENTED_EDGE ( 'NONE', *, *, #52948, .F. ) ;
#46798=ORIENTED_EDGE ( 'NONE', *, *, #52362, .F. ) ;
#46801=CARTESIAN_POINT ( 'NONE',  ( 10.00000000000000000, 0.000000000000000000, 0.000000000000000000 ) ) ;
#46807=ORIENTED_EDGE ( 'NONE', *, *, #73894, .F. ) ;
#46810=DIRECTION ( 'NONE',  ( -1.000000000000000000, 0.000000000000000000, 0.000000000000000000 ) ) ;
#46814=CARTESIAN_POINT ( 'NONE',  ( 10.00000000000000000, 37.58145647212453611, 0.6853352020791767529 ) ) ;
#46830=CIRCLE ( 'NONE', #52835, 16.00000000000000000 ) ;
#46832=CARTESIAN_POINT ( 'NONE',  ( 10.00000000000000000, -30.80686688397025108, 21.53537804866070715 ) ) ;
#46842=CARTESIAN_POINT ( 'NONE',  ( 10.00000000000000000, -37.22597642581153821, -5.202137450156795850 ) ) ;
#46843=VECTOR ( 'NONE', #6540, 1000.000000000000000 ) ;
#46848=CARTESIAN_POINT ( 'NONE',  ( 0.000000000000000000, -19.89357724624986901, -12.59942793731086041 ) ) ;
#46856=DIRECTION ( 'NONE',  ( -1.000000000000000000, -0.000000000000000000, -0.000000000000000000 ) ) ;
#46858=DIRECTION ( 'NONE',  ( 0.000000000000000000, 0.4067366430758009854, -0.9135454576426004225 ) ) ;
#46860=EDGE_CURVE ( 'NONE', #58339, #22472, #59113, .T. ) ;
#46922=ORIENTED_EDGE ( 'NONE', *, *, #60105, .F. ) ;
#46924=VERTEX_POINT ( 'NONE', #66951 ) ;
#46940=FACE_OUTER_BOUND ( 'NONE', #53000, .T. ) ;
#46960=ORIENTED_EDGE ( 'NONE', *, *, #50391, .T. ) ;
#46979=DIRECTION ( 'NONE',  ( -1.000000000000000000, -0.000000000000000000, 0.000000000000000000 ) ) ;
#46995=CARTESIAN_POINT ( 'NONE',  ( 10.00000000000000000, 0.000000000000000000, 0.000000000000000000 ) ) ;
#47006=VERTEX_POINT ( 'NONE', #50402 ) ;
#47011=FACE_OUTER_BOUND ( 'NONE', #65657, .T. ) ;
#47013=ORIENTED_EDGE ( 'NONE', *, *, #3448, .F. ) ;
#47019=DIRECTION ( 'NONE',  ( 0.000000000000000000, 0.000000000000000000, 1.000000000000000000 ) ) ;
#47024=EDGE_CURVE ( 'NONE', #70934, #64038, #51145, .T. ) ;
#47029=DIRECTION ( 'NONE',  ( 0.000000000000000000, 0.000000000000000000, 1.000000000000000000 ) ) ;
#47032=EDGE_CURVE ( 'NONE', #23374, #32002, #1324, .T. ) ;
#47098=CIRCLE ( 'NONE', #54281, 16.00000000000000355 ) ;
#47101=ORIENTED_EDGE ( 'NONE', *, *, #48547, .F. ) ;
#47105=CYLINDRICAL_SURFACE ( 'NONE', #758, 16.00000000000000000 ) ;
#47110=CARTESIAN_POINT ( 'NONE',  ( 10.00000000000000000, -5.202137450156655518, 37.22597642581156663 ) ) ;
#47122=LINE ( 'NONE', #548, #34575 ) ;
#47132=DIRECTION ( 'NONE',  ( -1.000000000000000000, 0.000000000000000000, 0.000000000000000000 ) ) ;
#47135=LINE ( 'NONE', #64424, #38917 ) ;
#47136=DIRECTION ( 'NONE',  ( 0.000000000000000000, 0.000000000000000000, 1.000000000000000000 ) ) ;
#47144=ADVANCED_FACE ( 'NONE', ( #64656 ), #14251, .F. ) ;
#47149=DIRECTION ( 'NONE',  ( -1.000000000000000000, 0.000000000000000000, 0.000000000000000000 ) ) ;
#47156=AXIS2_PLACEMENT_3D ( 'NONE', #56074, #61354, #21104 ) ;
#47172=CARTESIAN_POINT ( 'NONE',  ( 0.000000000000000000, -33.80338159004273280, -16.23288003029533044 ) ) ;
#47175=DIRECTION ( 'NONE',  ( -1.000000000000000000, -0.000000000000000000, -0.000000000000000000 ) ) ;
#47180=VERTEX_POINT ( 'NONE', #69913 ) ;
#47185=DIRECTION ( 'NONE',  ( 0.000000000000000000, -6.938893903907228378E-15, 1.000000000000000000 ) ) ;
#47186=DIRECTION ( 'NONE',  ( 0.000000000000000000, -0.9510565162951565288, 0.3090169943749384029 ) ) ;
#47195=CIRCLE ( 'NONE', #14762, 37.49900000000000944 ) ;
#47200=DIRECTION ( 'NONE',  ( -1.000000000000000000, -0.000000000000000000, -0.000000000000000000 ) ) ;
#47210=CARTESIAN_POINT ( 'NONE',  ( 0.000000000000000000, 37.22597642581158084, -5.202137450156524068 ) ) ;
#47212=CARTESIAN_POINT ( 'NONE',  ( 0.000000000000000000, -27.75498641678720446, -31.52238457039628727 ) ) ;
#47213=CARTESIAN_POINT ( 'NONE',  ( 10.00000000000000000, 0.000000000000000000, 0.000000000000000000 ) ) ;
#47215=CARTESIAN_POINT ( 'NONE',  ( 0.000000000000000000, 33.00180498840072829, -17.80606268964504935 ) ) ;
#47234=ORIENTED_EDGE ( 'NONE', *, *, #66727, .F. ) ;
#47235=VERTEX_POINT ( 'NONE', #44161 ) ;
#47237=DIRECTION ( 'NONE',  ( -1.000000000000000000, 0.000000000000000000, 0.000000000000000000 ) ) ;
#47243=CARTESIAN_POINT ( 'NONE',  ( 4.999999999999999112, -9.188173127307004862, -40.98264845739759465 ) ) ;
#47244=CIRCLE ( 'NONE', #42416, 42.00000000000000000 ) ;
#47252=ORIENTED_EDGE ( 'NONE', *, *, #2176, .T. ) ;
#47259=CIRCLE ( 'NONE', #61646, 16.00000000000000000 ) ;
#47279=DIRECTION ( 'NONE',  ( -1.000000000000000000, 0.000000000000000000, 0.000000000000000000 ) ) ;
#47289=AXIS2_PLACEMENT_3D ( 'NONE', #33392, #61996, #11221 ) ;
#47300=DIRECTION ( 'NONE',  ( -1.000000000000000000, -0.000000000000000000, -0.000000000000000000 ) ) ;
#47308=EDGE_CURVE ( 'NONE', #8777, #67030, #19295, .T. ) ;
#47313=ADVANCED_FACE ( 'NONE', ( #71753 ), #10010, .T. ) ;
#47320=DIRECTION ( 'NONE',  ( 0.000000000000000000, 7.228014483236689653E-16, -1.000000000000000000 ) ) ;
#47364=AXIS2_PLACEMENT_3D ( 'NONE', #72528, #49236, #37963 ) ;
#47367=EDGE_LOOP ( 'NONE', ( #37112, #43467, #45990, #39396 ) ) ;
#47375=CARTESIAN_POINT ( 'NONE',  ( -3.000000000000000000, 14.60985201121704513, 18.46759930825707841 ) ) ;
#47386=CYLINDRICAL_SURFACE ( 'NONE', #24764, 16.00000000000000000 ) ;
#47390=DIRECTION ( 'NONE',  ( 0.000000000000000000, 0.3090169943749411230, 0.9510565162951555296 ) ) ;
#47392=EDGE_CURVE ( 'NONE', #54476, #59274, #61327, .T. ) ;
#47408=VECTOR ( 'NONE', #61534, 1000.000000000000000 ) ;
#47415=VERTEX_POINT ( 'NONE', #62656 ) ;
#47422=ORIENTED_EDGE ( 'NONE', *, *, #10166, .T. ) ;
#47441=ORIENTED_EDGE ( 'NONE', *, *, #22071, .F. ) ;
#47452=DIRECTION ( 'NONE',  ( -1.000000000000000000, -0.000000000000000000, 0.000000000000000000 ) ) ;
#47471=CYLINDRICAL_SURFACE ( 'NONE', #55466, 37.49900000000000233 ) ;
#47477=VERTEX_POINT ( 'NONE', #29146 ) ;
#47480=EDGE_CURVE ( 'NONE', #17553, #42918, #69745, .T. ) ;
#47482=CARTESIAN_POINT ( 'NONE',  ( 10.00000000000000000, 40.98264845739749518, 9.188173127307441845 ) ) ;
#47487=ORIENTED_EDGE ( 'NONE', *, *, #13167, .T. ) ;
#47489=VECTOR ( 'NONE', #58755, 1000.000000000000000 ) ;
#47504=LINE ( 'NONE', #30933, #27438 ) ;
#47516=FACE_OUTER_BOUND ( 'NONE', #70076, .T. ) ;
#47517=EDGE_CURVE ( 'NONE', #49481, #55130, #40436, .T. ) ;
#47521=EDGE_CURVE ( 'NONE', #53901, #4438, #73321, .T. ) ;
#47523=EDGE_CURVE ( 'NONE', #21232, #74280, #64483, .T. ) ;
#47536=ORIENTED_EDGE ( 'NONE', *, *, #27639, .T. ) ;
#47541=EDGE_CURVE ( 'NONE', #45606, #31921, #57363, .T. ) ;
#47553=CARTESIAN_POINT ( 'NONE',  ( 0.000000000000000000, -33.79645857604525361, 16.45098606841114730 ) ) ;
#47561=ADVANCED_FACE ( 'NONE', ( #6246 ), #28787, .F. ) ;
#47566=CARTESIAN_POINT ( 'NONE',  ( -3.000000000000000000, -22.67460108101783334, 6.353146135317912169 ) ) ;
#47575=DIRECTION ( 'NONE',  ( 1.000000000000000000, -0.000000000000000000, 0.000000000000000000 ) ) ;
#47598=DIRECTION ( 'NONE',  ( 0.000000000000000000, -0.3090169943749548342, 0.9510565162951511997 ) ) ;
#47628=LINE ( 'NONE', #30693, #44365 ) ;
#47629=VERTEX_POINT ( 'NONE', #18970 ) ;
#47630=EDGE_CURVE ( 'NONE', #29668, #67669, #37345, .T. ) ;
#47632=VECTOR ( 'NONE', #25927, 1000.000000000000000 ) ;
#47633=EDGE_LOOP ( 'NONE', ( #23339, #54738, #10757, #43393 ) ) ;
#47637=CARTESIAN_POINT ( 'NONE',  ( 0.000000000000000000, -12.26510123303284594, 35.53030884539080603 ) ) ;
#47643=EDGE_CURVE ( 'NONE', #51502, #41287, #4937, .T. ) ;
#47648=EDGE_LOOP ( 'NONE', ( #69230, #56597, #30074, #5689 ) ) ;
#47683=CARTESIAN_POINT ( 'NONE',  ( 50.00005079999999680, 0.000000000000000000, 21.00000000000000000 ) ) ;
#47688=AXIS2_PLACEMENT_3D ( 'NONE', #43476, #54363, #31421 ) ;
#47691=ORIENTED_EDGE ( 'NONE', *, *, #35296, .T. ) ;
#47694=DIRECTION ( 'NONE',  ( 0.000000000000000000, 0.000000000000000000, 1.000000000000000000 ) ) ;
#47742=CARTESIAN_POINT ( 'NONE',  ( 0.000000000000000000, 0.000000000000000000, 0.000000000000000000 ) ) ;
#47759=DIRECTION ( 'NONE',  ( 0.000000000000000000, 0.000000000000000000, 1.000000000000000000 ) ) ;
#47772=DIRECTION ( 'NONE',  ( 0.000000000000000000, 0.000000000000000000, 1.000000000000000000 ) ) ;
#47780=ORIENTED_EDGE ( 'NONE', *, *, #58055, .T. ) ;
#47783=ADVANCED_FACE ( 'NONE', ( #44890 ), #4676, .F. ) ;
#47798=DIRECTION ( 'NONE',  ( -1.000000000000000000, -0.000000000000000000, 0.000000000000000000 ) ) ;
#47813=ORIENTED_EDGE ( 'NONE', *, *, #42799, .T. ) ;
#47827=DIRECTION ( 'NONE',  ( 0.000000000000000000, -0.3090169943749460635, -0.9510565162951539753 ) ) ;
#47832=CARTESIAN_POINT ( 'NONE',  ( 10.00000000000000000, 0.000000000000000000, 0.000000000000000000 ) ) ;
#47833=DIRECTION ( 'NONE',  ( -1.000000000000000000, 0.000000000000000000, -0.000000000000000000 ) ) ;
#47855=EDGE_CURVE ( 'NONE', #15277, #48910, #43784, .T. ) ;
#47858=EDGE_CURVE ( 'NONE', #12105, #31980, #69785, .T. ) ;
#47864=ORIENTED_EDGE ( 'NONE', *, *, #35733, .F. ) ;
#47871=EDGE_LOOP ( 'NONE', ( #6328, #42936, #39513, #59167 ) ) ;
#47879=ORIENTED_EDGE ( 'NONE', *, *, #3675, .F. ) ;
#47890=EDGE_CURVE ( 'NONE', #66514, #19617, #55415, .T. ) ;
#47909=DIRECTION ( 'NONE',  ( 0.000000000000000000, -0.4999999999999913403, -0.8660254037844435926 ) ) ;
#47912=CIRCLE ( 'NONE', #40672, 42.00000000000000000 ) ;
#47914=DIRECTION ( 'NONE',  ( 0.000000000000000000, 0.000000000000000000, 1.000000000000000000 ) ) ;
#47917=AXIS2_PLACEMENT_3D ( 'NONE', #29458, #22362, #68225 ) ;
#47923=CYLINDRICAL_SURFACE ( 'NONE', #41986, 37.49900000000000233 ) ;
#47934=CARTESIAN_POINT ( 'NONE',  ( -3.000000000000000000, -26.23277895567251505, 4.042438405569750870 ) ) ;
#47970=CIRCLE ( 'NONE', #15551, 37.49900000000000233 ) ;
#47976=ORIENTED_EDGE ( 'NONE', *, *, #10303, .T. ) ;
#47979=EDGE_CURVE ( 'NONE', #70065, #53287, #9793, .T. ) ;
#47992=VECTOR ( 'NONE', #67760, 1000.000000000000000 ) ;
#48014=DIRECTION ( 'NONE',  ( 0.000000000000000000, 0.9876883405951382144, -0.1564344650402276493 ) ) ;
#48017=AXIS2_PLACEMENT_3D ( 'NONE', #49878, #14563, #60812 ) ;
#48019=CIRCLE ( 'NONE', #71996, 37.49900000000000944 ) ;
#48020=DIRECTION ( 'NONE',  ( -1.000000000000000000, 0.000000000000000000, -0.000000000000000000 ) ) ;
#48033=EDGE_CURVE ( 'NONE', #72759, #63788, #51989, .T. ) ;
#48041=FACE_OUTER_BOUND ( 'NONE', #14602, .T. ) ;
#48042=EDGE_CURVE ( 'NONE', #21068, #45442, #51826, .T. ) ;
#48055=DIRECTION ( 'NONE',  ( -1.000000000000000000, 0.000000000000000000, 0.000000000000000000 ) ) ;
#48091=ORIENTED_EDGE ( 'NONE', *, *, #65602, .F. ) ;
#48107=ORIENTED_EDGE ( 'NONE', *, *, #57574, .F. ) ;
#48109=FACE_OUTER_BOUND ( 'NONE', #65861, .T. ) ;
#48110=ORIENTED_EDGE ( 'NONE', *, *, #38553, .F. ) ;
#48115=CARTESIAN_POINT ( 'NONE',  ( 0.000000000000000000, 35.47612816024523852, 22.48208911017513145 ) ) ;
#48119=EDGE_CURVE ( 'NONE', #11255, #12875, #30530, .T. ) ;
#48143=CARTESIAN_POINT ( 'NONE',  ( 10.00000000000000000, -27.13269053701078448, -25.88420570971428702 ) ) ;
#48153=VECTOR ( 'NONE', #8925, 1000.000000000000000 ) ;
#48155=VECTOR ( 'NONE', #73071, 1000.000000000000000 ) ;
#48164=VECTOR ( 'NONE', #45089, 999.9999999999998863 ) ;
#48165=ORIENTED_EDGE ( 'NONE', *, *, #18160, .T. ) ;
#48170=ORIENTED_EDGE ( 'NONE', *, *, #16066, .F. ) ;
#48174=DIRECTION ( 'NONE',  ( -0.000000000000000000, -0.6691306063588569053, -0.7431448254773954654 ) ) ;
#48180=VERTEX_POINT ( 'NONE', #71859 ) ;
#48181=ADVANCED_FACE ( 'NONE', ( #24902 ), #47471, .T. ) ;
#48211=DIRECTION ( 'NONE',  ( 1.000000000000000000, 0.000000000000000000, -0.000000000000000000 ) ) ;
#48222=DIRECTION ( 'NONE',  ( -1.000000000000000000, 0.000000000000000000, 0.000000000000000000 ) ) ;
#48226=EDGE_LOOP ( 'NONE', ( #64920, #33150, #28660, #69363 ) ) ;
#48232=DIRECTION ( 'NONE',  ( 1.000000000000000000, -0.000000000000000000, -0.000000000000000000 ) ) ;
#48233=DIRECTION ( 'NONE',  ( 0.000000000000000000, 0.000000000000000000, -1.000000000000000000 ) ) ;
#48264=VECTOR ( 'NONE', #14891, 1000.000000000000000 ) ;
#48267=CARTESIAN_POINT ( 'NONE',  ( 0.000000000000000000, 37.22597642581158084, 10.79786254984347593 ) ) ;
#48270=ORIENTED_EDGE ( 'NONE', *, *, #55183, .F. ) ;
#48279=FACE_OUTER_BOUND ( 'NONE', #54184, .T. ) ;
#48320=CARTESIAN_POINT ( 'NONE',  ( 0.000000000000000000, 0.000000000000000000, 0.000000000000000000 ) ) ;
#48325=VECTOR ( 'NONE', #13049, 1000.000000000000114 ) ;
#48346=EDGE_CURVE ( 'NONE', #13386, #31034, #25417, .T. ) ;
#48353=ORIENTED_EDGE ( 'NONE', *, *, #63526, .T. ) ;
#48354=ORIENTED_EDGE ( 'NONE', *, *, #14767, .T. ) ;
#48379=ORIENTED_EDGE ( 'NONE', *, *, #29121, .F. ) ;
#48386=CARTESIAN_POINT ( 'NONE',  ( 0.000000000000000000, 20.85821328998756385, -10.92862929874494959 ) ) ;
#48416=DIRECTION ( 'NONE',  ( -1.000000000000000000, -0.000000000000000000, -0.000000000000000000 ) ) ;
#48423=CARTESIAN_POINT ( 'NONE',  ( -3.000000000000000000, -0.9646360437375307573, 23.52805723605590060 ) ) ;
#48443=EDGE_CURVE ( 'NONE', #28069, #11579, #57847, .T. ) ;
#48444=CARTESIAN_POINT ( 'NONE',  ( -3.000000000000000000, -23.29833615347109443, 3.418703333116492438 ) ) ;
#48456=ORIENTED_EDGE ( 'NONE', *, *, #55243, .T. ) ;
#48459=VERTEX_POINT ( 'NONE', #46642 ) ;
#48466=ORIENTED_EDGE ( 'NONE', *, *, #1133, .T. ) ;
#48472=CARTESIAN_POINT ( 'NONE',  ( 0.000000000000000000, 0.000000000000000000, 0.000000000000000000 ) ) ;
#48473=EDGE_CURVE ( 'NONE', #63672, #37478, #38677, .T. ) ;
#48487=DIRECTION ( 'NONE',  ( 0.000000000000000000, 0.000000000000000000, 1.000000000000000000 ) ) ;
#48494=CARTESIAN_POINT ( 'NONE',  ( 0.000000000000000000, -26.23277895567251505, 4.042438405569750870 ) ) ;
#48500=FACE_OUTER_BOUND ( 'NONE', #5686, .T. ) ;
#48523=AXIS2_PLACEMENT_3D ( 'NONE', #27136, #21500, #67374 ) ;
#48529=VECTOR ( 'NONE', #1757, 1000.000000000000000 ) ;
#48531=ORIENTED_EDGE ( 'NONE', *, *, #1588, .T. ) ;
#48538=ORIENTED_EDGE ( 'NONE', *, *, #32016, .T. ) ;
#48544=CIRCLE ( 'NONE', #58212, 16.00000000000000000 ) ;
#48547=EDGE_CURVE ( 'NONE', #68891, #19238, #1475, .T. ) ;
#48553=DIRECTION ( 'NONE',  ( -1.000000000000000000, 0.000000000000000000, 0.000000000000000000 ) ) ;
#48554=CARTESIAN_POINT ( 'NONE',  ( 0.000000000000000000, -37.58145647212455032, 0.6853352020789044152 ) ) ;
#48572=DIRECTION ( 'NONE',  ( 1.000000000000000000, 0.000000000000000000, 0.000000000000000000 ) ) ;
#48579=CARTESIAN_POINT ( 'NONE',  ( -3.000000000000000000, -20.55727247249726020, -16.78983467731313084 ) ) ;
#48591=DIRECTION ( 'NONE',  ( 0.000000000000000000, 0.000000000000000000, 1.000000000000000000 ) ) ;
#48601=DIRECTION ( 'NONE',  ( -1.000000000000000000, -0.000000000000000000, -0.000000000000000000 ) ) ;
#48611=CARTESIAN_POINT ( 'NONE',  ( -3.000000000000000000, -4.261787119644969479, -26.19803753235780519 ) ) ;
#48625=DIRECTION ( 'NONE',  ( 1.000000000000000000, -0.000000000000000000, -0.000000000000000000 ) ) ;
#48629=ORIENTED_EDGE ( 'NONE', *, *, #59921, .F. ) ;
#48632=CARTESIAN_POINT ( 'NONE',  ( -3.000000000000000000, 6.762365576493643893, -25.66652317338391853 ) ) ;
#48633=ORIENTED_EDGE ( 'NONE', *, *, #34559, .F. ) ;
#48636=VECTOR ( 'NONE', #44843, 1000.000000000000000 ) ;
#48637=DIRECTION ( 'NONE',  ( -1.000000000000000000, 0.000000000000000000, 0.000000000000000000 ) ) ;
#48665=DIRECTION ( 'NONE',  ( -1.000000000000000000, 0.000000000000000000, -0.000000000000000000 ) ) ;
#48668=ORIENTED_EDGE ( 'NONE', *, *, #2446, .T. ) ;
#48676=LINE ( 'NONE', #60711, #41103 ) ;
#48692=CARTESIAN_POINT ( 'NONE',  ( 0.000000000000000000, -18.13022148937243472, -15.02647892043568767 ) ) ;
#48707=EDGE_CURVE ( 'NONE', #50093, #53901, #40875, .T. ) ;
#48710=VECTOR ( 'NONE', #30943, 1000.000000000000000 ) ;
#48747=ORIENTED_EDGE ( 'NONE', *, *, #58584, .T. ) ;
#48751=AXIS2_PLACEMENT_3D ( 'NONE', #28260, #11341, #22636 ) ;
#48771=DIRECTION ( 'NONE',  ( 0.000000000000000000, 0.8910065241883688980, -0.4539904997395447506 ) ) ;
#48778=ORIENTED_EDGE ( 'NONE', *, *, #28357, .F. ) ;
#48787=DIRECTION ( 'NONE',  ( 0.000000000000000000, 0.000000000000000000, 1.000000000000000000 ) ) ;
#48788=VECTOR ( 'NONE', #10948, 1000.000000000000000 ) ;
#48813=VERTEX_POINT ( 'NONE', #43479 ) ;
#48833=ORIENTED_EDGE ( 'NONE', *, *, #28573, .F. ) ;
#48837=ORIENTED_EDGE ( 'NONE', *, *, #70496, .T. ) ;
#48850=CARTESIAN_POINT ( 'NONE',  ( -3.000000000000000000, -23.29833615347104825, -3.418703333116803744 ) ) ;
#48876=EDGE_CURVE ( 'NONE', #47477, #19038, #70901, .T. ) ;
#48893=EDGE_CURVE ( 'NONE', #73125, #30694, #66319, .T. ) ;
#48904=DIRECTION ( 'NONE',  ( 0.000000000000000000, 0.000000000000000000, 1.000000000000000000 ) ) ;
#48910=VERTEX_POINT ( 'NONE', #64914 ) ;
#48936=ORIENTED_EDGE ( 'NONE', *, *, #72184, .F. ) ;
#48939=CARTESIAN_POINT ( 'NONE',  ( 10.00000000000000000, 37.22597642581158084, 10.79786254984347593 ) ) ;
#48973=EDGE_CURVE ( 'NONE', #72829, #71534, #48676, .T. ) ;
#48985=ORIENTED_EDGE ( 'NONE', *, *, #7997, .T. ) ;
#48989=VERTEX_POINT ( 'NONE', #3214 ) ;
#48990=ORIENTED_EDGE ( 'NONE', *, *, #63152, .T. ) ;
#48995=ORIENTED_EDGE ( 'NONE', *, *, #29176, .T. ) ;
#49021=DIRECTION ( 'NONE',  ( -1.000000000000000000, 0.000000000000000000, 0.000000000000000000 ) ) ;
#49026=DIRECTION ( 'NONE',  ( 0.000000000000000000, 0.000000000000000000, 1.000000000000000000 ) ) ;
#49040=AXIS2_PLACEMENT_3D ( 'NONE', #44361, #74035, #22546 ) ;
#49046=FACE_OUTER_BOUND ( 'NONE', #54045, .T. ) ;
#49053=CARTESIAN_POINT ( 'NONE',  ( -3.000000000000000000, 6.762365576493310826, 25.66652317338401090 ) ) ;
#49069=EDGE_CURVE ( 'NONE', #20728, #49481, #31744, .T. ) ;
#49083=DIRECTION ( 'NONE',  ( 0.000000000000000000, 0.000000000000000000, 1.000000000000000000 ) ) ;
#49111=CARTESIAN_POINT ( 'NONE',  ( 10.00000000000000000, 4.992566952385523393, -37.16516213103272293 ) ) ;
#49122=VECTOR ( 'NONE', #69493, 1000.000000000000000 ) ;
#49123=EDGE_LOOP ( 'NONE', ( #18707, #69347, #31132, #50474 ) ) ;
#49127=CARTESIAN_POINT ( 'NONE',  ( 0.000000000000000000, 16.83928648764923253, 16.46020748918050458 ) ) ;
#49135=AXIS2_PLACEMENT_3D ( 'NONE', #15748, #26272, #4118 ) ;
#49159=ORIENTED_EDGE ( 'NONE', *, *, #50, .T. ) ;
#49160=CIRCLE ( 'NONE', #7156, 16.00000000000000000 ) ;
#49172=DIRECTION ( 'NONE',  ( -1.000000000000000000, -0.000000000000000000, -0.000000000000000000 ) ) ;
#49181=CARTESIAN_POINT ( 'NONE',  ( 10.00000000000000000, -27.75498641678720446, -31.52238457039628727 ) ) ;
#49185=AXIS2_PLACEMENT_3D ( 'NONE', #59184, #41886, #58431 ) ;
#49191=DIRECTION ( 'NONE',  ( -0.000000000000000000, 0.8090169943749504489, -0.5877852522924689183 ) ) ;
#49196=ORIENTED_EDGE ( 'NONE', *, *, #26415, .F. ) ;
#49215=CARTESIAN_POINT ( 'NONE',  ( 0.000000000000000000, 0.000000000000000000, 0.000000000000000000 ) ) ;
#49218=CARTESIAN_POINT ( 'NONE',  ( 10.00000000000000000, 37.22597642581158084, -5.202137450156524068 ) ) ;
#49229=FACE_OUTER_BOUND ( 'NONE', #39285, .T. ) ;
#49232=LINE ( 'NONE', #26298, #10327 ) ;
#49236=DIRECTION ( 'NONE',  ( -1.000000000000000000, -0.000000000000000000, -0.000000000000000000 ) ) ;
#49241=LINE ( 'NONE', #5544, #64061 ) ;
#49250=CARTESIAN_POINT ( 'NONE',  ( 10.00000000000000000, 0.000000000000000000, 0.000000000000000000 ) ) ;
#49254=ORIENTED_EDGE ( 'NONE', *, *, #56650, .F. ) ;
#49255=ORIENTED_EDGE ( 'NONE', *, *, #47643, .T. ) ;
#49265=ORIENTED_EDGE ( 'NONE', *, *, #45634, .F. ) ;
#49267=EDGE_LOOP ( 'NONE', ( #24351, #44406, #28892, #62109 ) ) ;
#49278=CARTESIAN_POINT ( 'NONE',  ( -3.000000000000000000, -13.04903810567647682, -19.60159698893442481 ) ) ;
#49282=ADVANCED_FACE ( 'NONE', ( #56168 ), #73450, .T. ) ;
#49308=DIRECTION ( 'NONE',  ( 0.000000000000000000, 0.5877852522924742473, -0.8090169943749465631 ) ) ;
#49335=DIRECTION ( 'NONE',  ( 1.000000000000000000, -0.000000000000000000, -0.000000000000000000 ) ) ;
#49339=VERTEX_POINT ( 'NONE', #19541 ) ;
#49348=DIRECTION ( 'NONE',  ( 1.000000000000000000, -0.000000000000000000, -0.000000000000000000 ) ) ;
#49350=DIRECTION ( 'NONE',  ( 0.000000000000000000, -0.1564344650402380854, 0.9876883405951365491 ) ) ;
#49374=ORIENTED_EDGE ( 'NONE', *, *, #70041, .F. ) ;
#49377=ORIENTED_EDGE ( 'NONE', *, *, #37367, .T. ) ;
#49401=DIRECTION ( 'NONE',  ( 0.000000000000000000, 0.3090169943749580539, -0.9510565162951500895 ) ) ;
#49403=CARTESIAN_POINT ( 'NONE',  ( 10.00000000000000000, 36.88895765772642932, -6.736453364083163642 ) ) ;
#49420=FACE_OUTER_BOUND ( 'NONE', #16913, .T. ) ;
#49421=ADVANCED_FACE ( 'NONE', ( #11766 ), #5797, .T. ) ;
#49425=CARTESIAN_POINT ( 'NONE',  ( 4.999999999999999112, -41.91543099594816368, -2.663952781846588014 ) ) ;
#49432=DIRECTION ( 'NONE',  ( 1.000000000000000000, -0.000000000000000000, -0.000000000000000000 ) ) ;
#49433=ORIENTED_EDGE ( 'NONE', *, *, #59076, .T. ) ;
#49447=CARTESIAN_POINT ( 'NONE',  ( -3.000000000000000000, 20.85821328998741109, 10.92862929874522315 ) ) ;
#49451=AXIS2_PLACEMENT_3D ( 'NONE', #17493, #40421, #16004 ) ;
#49455=FACE_OUTER_BOUND ( 'NONE', #23255, .T. ) ;
#49465=EDGE_LOOP ( 'NONE', ( #37194, #35577, #58476, #48629 ) ) ;
#49473=ADVANCED_FACE ( 'NONE', ( #27026 ), #3391, .T. ) ;
#49480=ADVANCED_FACE ( 'NONE', ( #37953 ), #60166, .T. ) ;
#49481=VERTEX_POINT ( 'NONE', #48494 ) ;
#49486=DIRECTION ( 'NONE',  ( -0.000000000000000000, 0.8090169943749504489, -0.5877852522924689183 ) ) ;
#49487=AXIS2_PLACEMENT_3D ( 'NONE', #39436, #23998, #51821 ) ;
#49508=FACE_BOUND ( 'NONE', #57986, .T. ) ;
#49524=DIRECTION ( 'NONE',  ( 0.000000000000000000, 0.000000000000000000, -1.000000000000000000 ) ) ;
#49536=AXIS2_PLACEMENT_3D ( 'NONE', #72974, #21480, #38791 ) ;
#49541=DIRECTION ( 'NONE',  ( 0.000000000000000000, -0.3090169943749349057, -0.9510565162951576390 ) ) ;
#49581=DIRECTION ( 'NONE',  ( -1.000000000000000000, -0.000000000000000000, 0.000000000000000000 ) ) ;
#49587=AXIS2_PLACEMENT_3D ( 'NONE', #3343, #31505, #53706 ) ;
#49594=CARTESIAN_POINT ( 'NONE',  ( 0.000000000000000000, 0.000000000000000000, 0.000000000000000000 ) ) ;
#49595=CARTESIAN_POINT ( 'NONE',  ( -10.00000000000000000, 0.000000000000000000, 0.000000000000000000 ) ) ;
#49608=DIRECTION ( 'NONE',  ( 1.000000000000000000, -0.000000000000000000, 0.000000000000000000 ) ) ;
#49609=CARTESIAN_POINT ( 'NONE',  ( 10.00000000000000000, -21.32104025579091910, -30.84782396557241313 ) ) ;
#49610=ORIENTED_EDGE ( 'NONE', *, *, #39404, .T. ) ;
#49614=ADVANCED_FACE ( 'NONE', ( #51829 ), #55981, .T. ) ;
#49616=ORIENTED_EDGE ( 'NONE', *, *, #59501, .F. ) ;
#49620=VERTEX_POINT ( 'NONE', #22525 ) ;
#49635=ORIENTED_EDGE ( 'NONE', *, *, #5700, .T. ) ;
#49637=CIRCLE ( 'NONE', #40062, 16.00000000000000355 ) ;
#49646=ORIENTED_EDGE ( 'NONE', *, *, #9693, .F. ) ;
#49657=ADVANCED_FACE ( 'NONE', ( #56369 ), #11234, .F. ) ;
#49666=CARTESIAN_POINT ( 'NONE',  ( 0.000000000000000000, -40.68715046381921496, -10.41901085202121280 ) ) ;
#49712=DIRECTION ( 'NONE',  ( -1.000000000000000000, -0.000000000000000000, 0.000000000000000000 ) ) ;
#49717=ORIENTED_EDGE ( 'NONE', *, *, #27544, .F. ) ;
#49718=DIRECTION ( 'NONE',  ( -1.000000000000000000, -0.000000000000000000, -0.000000000000000000 ) ) ;
#49738=VECTOR ( 'NONE', #18669, 1000.000000000000000 ) ;
#49754=CARTESIAN_POINT ( 'NONE',  ( 0.000000000000000000, 0.000000000000000000, 0.000000000000000000 ) ) ;
#49776=DIRECTION ( 'NONE',  ( 0.000000000000000000, 0.000000000000000000, 1.000000000000000000 ) ) ;
#49779=AXIS2_PLACEMENT_3D ( 'NONE', #31625, #50306, #13602 ) ;
#49780=CYLINDRICAL_SURFACE ( 'NONE', #61964, 37.49900000000000233 ) ;
#49783=PLANE ( 'NONE',  #70510 ) ;
#49788=CARTESIAN_POINT ( 'NONE',  ( -3.000000000000000000, -14.54903810567645195, -22.19967320028775504 ) ) ;
#49793=FACE_OUTER_BOUND ( 'NONE', #14624, .T. ) ;
#49834=FACE_OUTER_BOUND ( 'NONE', #37828, .T. ) ;
#49836=DIRECTION ( 'NONE',  ( 0.000000000000000000, -0.2079116908177532363, -0.9781476007338069101 ) ) ;
#49853=DIRECTION ( 'NONE',  ( -1.000000000000000000, -0.000000000000000000, -0.000000000000000000 ) ) ;
#49872=CIRCLE ( 'NONE', #43891, 15.99999999999999822 ) ;
#49878=CARTESIAN_POINT ( 'NONE',  ( 0.000000000000000000, 12.26510123303308752, -35.53030884539072787 ) ) ;
#49903=CARTESIAN_POINT ( 'NONE',  ( 10.00000000000000000, -37.01155633439053361, -6.555932627142825986 ) ) ;
#49907=CARTESIAN_POINT ( 'NONE',  ( 5.000000000000000000, 38.55633173627010279, 16.65560815589424593 ) ) ;
#49915=EDGE_CURVE ( 'NONE', #23048, #36276, #3309, .T. ) ;
#49935=DIRECTION ( 'NONE',  ( 0.000000000000000000, 0.7431448254773862505, 0.6691306063588671194 ) ) ;
#49947=ORIENTED_EDGE ( 'NONE', *, *, #1563, .F. ) ;
#49950=DIRECTION ( 'NONE',  ( -1.000000000000000000, 0.000000000000000000, -0.000000000000000000 ) ) ;
#49961=DIRECTION ( 'NONE',  ( 0.000000000000000000, 0.6691306063588563502, 0.7431448254773960205 ) ) ;
#49974=AXIS2_PLACEMENT_3D ( 'NONE', #27270, #60042, #14894 ) ;
#49981=DIRECTION ( 'NONE',  ( 0.000000000000000000, 0.000000000000000000, 1.000000000000000000 ) ) ;
#49986=VERTEX_POINT ( 'NONE', #25102 ) ;
#49990=CARTESIAN_POINT ( 'NONE',  ( 0.000000000000000000, 14.60985201121729737, -18.46759930825688301 ) ) ;
#49996=ORIENTED_EDGE ( 'NONE', *, *, #26207, .F. ) ;
#49999=DIRECTION ( 'NONE',  ( 0.000000000000000000, 0.000000000000000000, 1.000000000000000000 ) ) ;
#50010=ORIENTED_EDGE ( 'NONE', *, *, #41524, .T. ) ;
#50027=ORIENTED_EDGE ( 'NONE', *, *, #32153, .F. ) ;
#50040=ORIENTED_EDGE ( 'NONE', *, *, #60185, .T. ) ;
#50045=EDGE_CURVE ( 'NONE', #61428, #11862, #8558, .T. ) ;
#50049=CARTESIAN_POINT ( 'NONE',  ( 0.000000000000000000, 20.85821328998741109, 10.92862929874522315 ) ) ;
#50056=CYLINDRICAL_SURFACE ( 'NONE', #69356, 37.49900000000000233 ) ;
#50060=ORIENTED_EDGE ( 'NONE', *, *, #36829, .T. ) ;
#50068=FACE_OUTER_BOUND ( 'NONE', #65656, .T. ) ;
#50073=ORIENTED_EDGE ( 'NONE', *, *, #1398, .T. ) ;
#50083=DIRECTION ( 'NONE',  ( 0.000000000000000000, 0.000000000000000000, -1.000000000000000000 ) ) ;
#50093=VERTEX_POINT ( 'NONE', #55898 ) ;
#50099=ORIENTED_EDGE ( 'NONE', *, *, #66656, .T. ) ;
#50108=CARTESIAN_POINT ( 'NONE',  ( 0.000000000000000000, 5.835314593368477354, 22.81335362449854642 ) ) ;
#50111=EDGE_LOOP ( 'NONE', ( #71011, #9515, #28077, #15862 ) ) ;
#50139=LINE ( 'NONE', #33978, #14395 ) ;
#50142=ADVANCED_FACE ( 'NONE', ( #56276 ), #44633, .T. ) ;
#50144=PLANE ( 'NONE',  #17441 ) ;
#50151=AXIS2_PLACEMENT_3D ( 'NONE', #50556, #44567, #27242 ) ;
#50152=CARTESIAN_POINT ( 'NONE',  ( 0.000000000000000000, -6.555932627142676772, 37.01155633439056203 ) ) ;
#50155=AXIS2_PLACEMENT_3D ( 'NONE', #39180, #62113, #29725 ) ;
#50171=CARTESIAN_POINT ( 'NONE',  ( 10.00000000000000000, 39.04073710021366139, -15.48615015657542848 ) ) ;
#50179=AXIS2_PLACEMENT_3D ( 'NONE', #11882, #52114, #657 ) ;
#50180=ORIENTED_EDGE ( 'NONE', *, *, #14757, .T. ) ;
#50199=VECTOR ( 'NONE', #48625, 1000.000000000000000 ) ;
#50204=ORIENTED_EDGE ( 'NONE', *, *, #8419, .T. ) ;
#50242=VECTOR ( 'NONE', #15876, 1000.000000000000000 ) ;
#50250=ADVANCED_FACE ( 'NONE', ( #285 ), #6977, .T. ) ;
#50267=DIRECTION ( 'NONE',  ( 0.000000000000000000, 0.9945218953682742891, -0.1045284632676436315 ) ) ;
#50285=ORIENTED_EDGE ( 'NONE', *, *, #38260, .F. ) ;
#50288=AXIS2_PLACEMENT_3D ( 'NONE', #26666, #33045, #72884 ) ;
#50296=CYLINDRICAL_SURFACE ( 'NONE', #39543, 16.00000000000000000 ) ;
#50306=DIRECTION ( 'NONE',  ( 1.000000000000000000, 0.000000000000000000, 0.000000000000000000 ) ) ;
#50307=EDGE_CURVE ( 'NONE', #25402, #17509, #31617, .T. ) ;
#50309=VERTEX_POINT ( 'NONE', #58119 ) ;
#50316=ORIENTED_EDGE ( 'NONE', *, *, #3578, .T. ) ;
#50323=VECTOR ( 'NONE', #16071, 999.9999999999998863 ) ;
#50338=CARTESIAN_POINT ( 'NONE',  ( 4.999999999999999112, -16.65560815589383381, -38.55633173627028754 ) ) ;
#50340=CYLINDRICAL_SURFACE ( 'NONE', #39274, 37.49900000000000233 ) ;
#50346=AXIS2_PLACEMENT_3D ( 'NONE', #15898, #16638, #56509 ) ;
#50358=CARTESIAN_POINT ( 'NONE',  ( 10.00000000000000000, -25.88420570971419821, 27.13269053701087330 ) ) ;
#50368=VECTOR ( 'NONE', #42420, 1000.000000000000000 ) ;
#50391=EDGE_CURVE ( 'NONE', #21912, #58096, #64503, .T. ) ;
#50402=CARTESIAN_POINT ( 'NONE',  ( 10.00000000000000000, 32.34446384429971744, 26.79245525562727082 ) ) ;
#50403=DIRECTION ( 'NONE',  ( 0.000000000000000000, 0.000000000000000000, 1.000000000000000000 ) ) ;
#50406=ORIENTED_EDGE ( 'NONE', *, *, #70682, .F. ) ;
#50424=CIRCLE ( 'NONE', #56457, 16.00000000000000355 ) ;
#50448=DIRECTION ( 'NONE',  ( 1.000000000000000000, 0.000000000000000000, -0.000000000000000000 ) ) ;
#50449=DIRECTION ( 'NONE',  ( -1.000000000000000000, -0.000000000000000000, -0.000000000000000000 ) ) ;
#50450=VERTEX_POINT ( 'NONE', #2861 ) ;
#50466=DIRECTION ( 'NONE',  ( 1.000000000000000000, 0.000000000000000000, 0.000000000000000000 ) ) ;
#50474=ORIENTED_EDGE ( 'NONE', *, *, #44597, .F. ) ;
#50493=DIRECTION ( 'NONE',  ( -1.000000000000000000, -0.000000000000000000, 0.000000000000000000 ) ) ;
#50503=ORIENTED_EDGE ( 'NONE', *, *, #3448, .T. ) ;
#50504=CARTESIAN_POINT ( 'NONE',  ( 0.000000000000000000, -10.41901085202050581, -40.68715046381939970 ) ) ;
#50521=CARTESIAN_POINT ( 'NONE',  ( 10.00000000000000000, 30.00120703465236716, -22.64427369931138756 ) ) ;
#50554=EDGE_CURVE ( 'NONE', #74050, #47235, #40117, .T. ) ;
#50556=CARTESIAN_POINT ( 'NONE',  ( 0.000000000000000000, -33.79645857604501913, -16.45098606841161626 ) ) ;
#50573=VERTEX_POINT ( 'NONE', #27217 ) ;
#50575=VECTOR ( 'NONE', #20374, 1000.000000000000114 ) ;
#50576=CIRCLE ( 'NONE', #198, 15.99999999999999467 ) ;
#50595=DIRECTION ( 'NONE',  ( 0.000000000000000000, 0.000000000000000000, 1.000000000000000000 ) ) ;
#50602=VERTEX_POINT ( 'NONE', #39269 ) ;
#50606=CARTESIAN_POINT ( 'NONE',  ( 0.000000000000000000, -33.17418723428294669, -17.67226234102862747 ) ) ;
#50615=VECTOR ( 'NONE', #14184, 1000.000000000000000 ) ;
#50616=PLANE ( 'NONE',  #57515 ) ;
#50620=DIRECTION ( 'NONE',  ( 0.000000000000000000, 0.000000000000000000, 1.000000000000000000 ) ) ;
#50635=VECTOR ( 'NONE', #42241, 999.9999999999998863 ) ;
#50637=EDGE_CURVE ( 'NONE', #39991, #35258, #62198, .T. ) ;
#50654=CARTESIAN_POINT ( 'NONE',  ( -10.00000000000000000, 0.000000000000000000, 0.000000000000000000 ) ) ;
#50660=ORIENTED_EDGE ( 'NONE', *, *, #25289, .F. ) ;
#50671=AXIS2_PLACEMENT_3D ( 'NONE', #7891, #31186, #60159 ) ;
#50701=ORIENTED_EDGE ( 'NONE', *, *, #27780, .F. ) ;
#50714=DIRECTION ( 'NONE',  ( -1.000000000000000000, -0.000000000000000000, -0.000000000000000000 ) ) ;
#50716=DIRECTION ( 'NONE',  ( -1.000000000000000000, -0.000000000000000000, -0.000000000000000000 ) ) ;
#50718=LINE ( 'NONE', #39832, #33626 ) ;
#50737=EDGE_CURVE ( 'NONE', #11359, #24241, #5308, .T. ) ;
#50739=EDGE_CURVE ( 'NONE', #5518, #33832, #22725, .T. ) ;
#50751=EDGE_CURVE ( 'NONE', #67112, #22210, #56932, .T. ) ;
#50767=ADVANCED_FACE ( 'NONE', ( #18541 ), #46024, .F. ) ;
#50768=ADVANCED_FACE ( 'NONE', ( #6181 ), #45665, .T. ) ;
#50784=DIRECTION ( 'NONE',  ( 0.000000000000000000, 0.000000000000000000, 1.000000000000000000 ) ) ;
#50840=LINE ( 'NONE', #57614, #70836 ) ;
#50845=EDGE_CURVE ( 'NONE', #70056, #66947, #34729, .T. ) ;
#50896=VECTOR ( 'NONE', #15426, 1000.000000000000000 ) ;
#50901=AXIS2_PLACEMENT_3D ( 'NONE', #59232, #7726, #19368 ) ;
#50902=CIRCLE ( 'NONE', #73696, 16.00000000000000000 ) ;
#50903=LINE ( 'NONE', #11062, #59455 ) ;
#50908=EDGE_CURVE ( 'NONE', #41967, #10069, #11180, .T. ) ;
#50912=AXIS2_PLACEMENT_3D ( 'NONE', #71937, #30973, #32455 ) ;
#50928=DIRECTION ( 'NONE',  ( 1.000000000000000000, -0.000000000000000000, 0.000000000000000000 ) ) ;
#50935=ORIENTED_EDGE ( 'NONE', *, *, #69497, .F. ) ;
#50996=CARTESIAN_POINT ( 'NONE',  ( 10.00000000000000000, -30.00120703465189465, -22.64427369931201639 ) ) ;
#51000=EDGE_CURVE ( 'NONE', #36560, #8213, #5193, .T. ) ;
#51004=EDGE_CURVE ( 'NONE', #32855, #24127, #64164, .T. ) ;
#51016=AXIS2_PLACEMENT_3D ( 'NONE', #38809, #32780, #10982 ) ;
#51018=ORIENTED_EDGE ( 'NONE', *, *, #15969, .T. ) ;
#51023=AXIS2_PLACEMENT_3D ( 'NONE', #52834, #69375, #997 ) ;
#51031=CARTESIAN_POINT ( 'NONE',  ( 10.00000000000000000, -33.00180498840035170, -17.80606268964575278 ) ) ;
#51040=ORIENTED_EDGE ( 'NONE', *, *, #3860, .T. ) ;
#51043=ORIENTED_EDGE ( 'NONE', *, *, #50739, .F. ) ;
#51051=ORIENTED_EDGE ( 'NONE', *, *, #14364, .T. ) ;
#51066=ORIENTED_EDGE ( 'NONE', *, *, #24554, .T. ) ;
#51067=AXIS2_PLACEMENT_3D ( 'NONE', #23262, #63861, #18342 ) ;
#51072=DIRECTION ( 'NONE',  ( 0.000000000000000000, 0.000000000000000000, 1.000000000000000000 ) ) ;
#51084=LINE ( 'NONE', #57474, #37340 ) ;
#51095=DIRECTION ( 'NONE',  ( 0.000000000000000000, 0.000000000000000000, 1.000000000000000000 ) ) ;
#51107=DIRECTION ( 'NONE',  ( 0.000000000000000000, 0.000000000000000000, 1.000000000000000000 ) ) ;
#51110=CIRCLE ( 'NONE', #52292, 16.00000000000000000 ) ;
#51138=ORIENTED_EDGE ( 'NONE', *, *, #6450, .T. ) ;
#51139=EDGE_LOOP ( 'NONE', ( #70632, #52700, #48633, #55820 ) ) ;
#51144=VERTEX_POINT ( 'NONE', #15869 ) ;
#51145=LINE ( 'NONE', #29318, #7288 ) ;
#51148=ORIENTED_EDGE ( 'NONE', *, *, #52963, .F. ) ;
#51150=ORIENTED_EDGE ( 'NONE', *, *, #61640, .T. ) ;
#51151=CARTESIAN_POINT ( 'NONE',  ( 10.00000000000000000, 0.000000000000000000, 37.49900000000000233 ) ) ;
#51153=VERTEX_POINT ( 'NONE', #12075 ) ;
#51163=VECTOR ( 'NONE', #1503, 1000.000000000000000 ) ;
#51180=CARTESIAN_POINT ( 'NONE',  ( 0.000000000000000000, -1.278221433540145613, -26.51162292216073979 ) ) ;
#51189=CYLINDRICAL_SURFACE ( 'NONE', #50155, 42.00000000000000000 ) ;
#51205=ORIENTED_EDGE ( 'NONE', *, *, #45355, .F. ) ;
#51209=ORIENTED_EDGE ( 'NONE', *, *, #19286, .T. ) ;
#51211=ORIENTED_EDGE ( 'NONE', *, *, #31409, .T. ) ;
#51217=CARTESIAN_POINT ( 'NONE',  ( 10.00000000000000000, -4.992566952385247170, 37.16516213103275845 ) ) ;
#51229=VERTEX_POINT ( 'NONE', #40281 ) ;
#51236=DIRECTION ( 'NONE',  ( -1.000000000000000000, -0.000000000000000000, 0.000000000000000000 ) ) ;
#51237=CYLINDRICAL_SURFACE ( 'NONE', #17878, 37.49900000000000233 ) ;
#51252=ORIENTED_EDGE ( 'NONE', *, *, #8909, .T. ) ;
#51259=DIRECTION ( 'NONE',  ( 0.000000000000000000, 0.000000000000000000, -1.000000000000000000 ) ) ;
#51268=VECTOR ( 'NONE', #57243, 1000.000000000000000 ) ;
#51277=ADVANCED_FACE ( 'NONE', ( #471 ), #11330, .F. ) ;
#51282=DIRECTION ( 'NONE',  ( -1.000000000000000000, 0.000000000000000000, 0.000000000000000000 ) ) ;
#51294=DIRECTION ( 'NONE',  ( 0.000000000000000000, 0.000000000000000000, -1.000000000000000000 ) ) ;
#51296=DIRECTION ( 'NONE',  ( 0.000000000000000000, -0.5000000000000039968, 0.8660254037844363761 ) ) ;
#51302=DIRECTION ( 'NONE',  ( -1.000000000000000000, 0.000000000000000000, 0.000000000000000000 ) ) ;
#51304=LINE ( 'NONE', #34017, #4013 ) ;
#51317=CARTESIAN_POINT ( 'NONE',  ( 10.00000000000000000, 22.64427369931169309, 30.00120703465213623 ) ) ;
#51333=CARTESIAN_POINT ( 'NONE',  ( 0.000000000000000000, -26.23277895567245821, -4.042438405570103477 ) ) ;
#51339=EDGE_LOOP ( 'NONE', ( #69349, #7934, #32750, #48538 ) ) ;
#51340=DIRECTION ( 'NONE',  ( -1.000000000000000000, -0.000000000000000000, -0.000000000000000000 ) ) ;
#51344=ADVANCED_FACE ( 'NONE', ( #25216 ), #14291, .F. ) ;
#51348=EDGE_CURVE ( 'NONE', #65222, #70426, #37241, .T. ) ;
#51351=DIRECTION ( 'NONE',  ( -1.000000000000000000, -0.000000000000000000, -0.000000000000000000 ) ) ;
#51366=DIRECTION ( 'NONE',  ( 0.000000000000000000, 0.9876883405951372152, 0.1564344650402346160 ) ) ;
#51377=CIRCLE ( 'NONE', #56162, 37.49900000000000944 ) ;
#51381=FACE_OUTER_BOUND ( 'NONE', #15632, .T. ) ;
#51382=FACE_OUTER_BOUND ( 'NONE', #23991, .T. ) ;
#51386=ORIENTED_EDGE ( 'NONE', *, *, #9695, .F. ) ;
#51396=CYLINDRICAL_SURFACE ( 'NONE', #26112, 42.00000000000000000 ) ;
#51398=EDGE_CURVE ( 'NONE', #26897, #33925, #53045, .T. ) ;
#51402=EDGE_LOOP ( 'NONE', ( #23034, #26279, #53276, #67413 ) ) ;
#51415=EDGE_LOOP ( 'NONE', ( #33174, #40811, #23861, #46167 ) ) ;
#51422=VECTOR ( 'NONE', #30275, 1000.000000000000000 ) ;
#51432=AXIS2_PLACEMENT_3D ( 'NONE', #19635, #31287, #42580 ) ;
#51437=DIRECTION ( 'NONE',  ( 0.000000000000000000, 0.000000000000000000, -1.000000000000000000 ) ) ;
#51441=CARTESIAN_POINT ( 'NONE',  ( 10.00000000000000000, 35.92658777277511462, 10.74501242461295014 ) ) ;
#51449=CYLINDRICAL_SURFACE ( 'NONE', #44535, 42.00000000000000000 ) ;
#51462=AXIS2_PLACEMENT_3D ( 'NONE', #4151, #27047, #49981 ) ;
#51474=CARTESIAN_POINT ( 'NONE',  ( 0.000000000000000000, 24.81905959214261514, 9.408202855044827118 ) ) ;
#51477=CARTESIAN_POINT ( 'NONE',  ( 0.000000000000000000, 8.688484142253939169, 21.88630264137371029 ) ) ;
#51481=VERTEX_POINT ( 'NONE', #74312 ) ;
#51482=ORIENTED_EDGE ( 'NONE', *, *, #30855, .T. ) ;
#51489=CIRCLE ( 'NONE', #32435, 15.99999999999999645 ) ;
#51502=VERTEX_POINT ( 'NONE', #57395 ) ;
#51515=ORIENTED_EDGE ( 'NONE', *, *, #34472, .T. ) ;
#51533=EDGE_CURVE ( 'NONE', #14021, #58339, #49241, .T. ) ;
#51535=CARTESIAN_POINT ( 'NONE',  ( 10.00000000000000000, -37.22597642581153821, -5.202137450156795850 ) ) ;
#51538=VECTOR ( 'NONE', #48665, 1000.000000000000000 ) ;
#51544=LINE ( 'NONE', #99, #69947 ) ;
#51546=EDGE_CURVE ( 'NONE', #28466, #54954, #68688, .T. ) ;
#51554=DIRECTION ( 'NONE',  ( 0.000000000000000000, -0.1564344650402170189, -0.9876883405951399908 ) ) ;
#51559=CARTESIAN_POINT ( 'NONE',  ( -3.000000000000000000, 6.762365576493643893, -25.66652317338391853 ) ) ;
#51566=CARTESIAN_POINT ( 'NONE',  ( 10.00000000000000000, 0.000000000000000000, 0.000000000000000000 ) ) ;
#51572=DIRECTION ( 'NONE',  ( 1.000000000000000000, -0.000000000000000000, -0.000000000000000000 ) ) ;
#51573=DIRECTION ( 'NONE',  ( 0.000000000000000000, 0.000000000000000000, -1.000000000000000000 ) ) ;
#51578=VECTOR ( 'NONE', #49401, 1000.000000000000227 ) ;
#51587=CARTESIAN_POINT ( 'NONE',  ( 0.000000000000000000, -16.23288003029473359, -33.80338159004301701 ) ) ;
#51594=ORIENTED_EDGE ( 'NONE', *, *, #38720, .F. ) ;
#51609=FACE_OUTER_BOUND ( 'NONE', #16215, .T. ) ;
#51634=ORIENTED_EDGE ( 'NONE', *, *, #41177, .F. ) ;
#51648=EDGE_CURVE ( 'NONE', #40343, #32004, #23277, .T. ) ;
#51672=CARTESIAN_POINT ( 'NONE',  ( 10.00000000000000000, 0.000000000000000000, 0.000000000000000000 ) ) ;
#51677=CIRCLE ( 'NONE', #61289, 16.00000000000000000 ) ;
#51680=ORIENTED_EDGE ( 'NONE', *, *, #73675, .T. ) ;
#51686=ORIENTED_EDGE ( 'NONE', *, *, #15375, .F. ) ;
#51690=VERTEX_POINT ( 'NONE', #64152 ) ;
#51692=AXIS2_PLACEMENT_3D ( 'NONE', #54055, #19087, #58207 ) ;
#51693=ORIENTED_EDGE ( 'NONE', *, *, #31196, .F. ) ;
#51704=LINE ( 'NONE', #252, #32323 ) ;
#51707=VERTEX_POINT ( 'NONE', #58880 ) ;
#51709=VERTEX_POINT ( 'NONE', #70492 ) ;
#51717=DIRECTION ( 'NONE',  ( 1.000000000000000000, 0.000000000000000000, 0.000000000000000000 ) ) ;
#51722=CARTESIAN_POINT ( 'NONE',  ( -3.000000000000000000, 23.50000000000000000, -1.500000000000001332 ) ) ;
#51726=EDGE_CURVE ( 'NONE', #61246, #56682, #19006, .T. ) ;
#51731=DIRECTION ( 'NONE',  ( -1.000000000000000000, 0.000000000000000000, 0.000000000000000000 ) ) ;
#51737=DIRECTION ( 'NONE',  ( 1.000000000000000000, 0.000000000000000000, -0.000000000000000000 ) ) ;
#51752=CIRCLE ( 'NONE', #1406, 16.00000000000000000 ) ;
#51762=ADVANCED_FACE ( 'NONE', ( #11886 ), #15223, .T. ) ;
#51785=DIRECTION ( 'NONE',  ( 0.000000000000000000, 0.000000000000000000, 1.000000000000000000 ) ) ;
#51789=EDGE_CURVE ( 'NONE', #24685, #67688, #37801, .T. ) ;
#51805=VERTEX_POINT ( 'NONE', #42693 ) ;
#51816=FACE_OUTER_BOUND ( 'NONE', #7938, .T. ) ;
#51817=DIRECTION ( 'NONE',  ( 1.000000000000000000, 0.000000000000000000, 0.000000000000000000 ) ) ;
#51821=DIRECTION ( 'NONE',  ( 0.000000000000000000, 0.000000000000000000, 1.000000000000000000 ) ) ;
#51824=ORIENTED_EDGE ( 'NONE', *, *, #68495, .F. ) ;
#51826=CIRCLE ( 'NONE', #72192, 16.00000000000000355 ) ;
#51829=FACE_OUTER_BOUND ( 'NONE', #8979, .T. ) ;
#51835=CARTESIAN_POINT ( 'NONE',  ( 10.00000000000000000, -22.74946021919153694, 29.81001611431000597 ) ) ;
#51836=DIRECTION ( 'NONE',  ( -1.000000000000000000, -0.000000000000000000, -0.000000000000000000 ) ) ;
#51844=CARTESIAN_POINT ( 'NONE',  ( 0.000000000000000000, -22.74946021919153694, 29.81001611431000597 ) ) ;
#51858=CARTESIAN_POINT ( 'NONE',  ( 10.00000000000000000, 0.000000000000000000, 0.000000000000000000 ) ) ;
#51860=DIRECTION ( 'NONE',  ( -1.000000000000000000, -0.000000000000000000, 0.000000000000000000 ) ) ;
#51869=DIRECTION ( 'NONE',  ( 0.000000000000000000, -0.4539904997395351471, -0.8910065241883737830 ) ) ;
#51871=AXIS2_PLACEMENT_3D ( 'NONE', #63946, #52277, #34994 ) ;
#51875=AXIS2_PLACEMENT_3D ( 'NONE', #24978, #19334, #47914 ) ;
#51883=EDGE_CURVE ( 'NONE', #23196, #28466, #67845, .T. ) ;
#51887=ORIENTED_EDGE ( 'NONE', *, *, #16210, .F. ) ;
#51888=ORIENTED_EDGE ( 'NONE', *, *, #14767, .F. ) ;
#51893=ORIENTED_EDGE ( 'NONE', *, *, #68155, .T. ) ;
#51899=DIRECTION ( 'NONE',  ( -1.000000000000000000, -0.000000000000000000, -0.000000000000000000 ) ) ;
#51931=ORIENTED_EDGE ( 'NONE', *, *, #57044, .T. ) ;
#51938=CARTESIAN_POINT ( 'NONE',  ( 0.000000000000000000, -27.05870788708250885, 26.08949754953014022 ) ) ;
#51950=EDGE_LOOP ( 'NONE', ( #51594, #24235, #17784, #67961 ) ) ;
#51958=ADVANCED_FACE ( 'NONE', ( #49793 ), #45674, .T. ) ;
#51961=AXIS2_PLACEMENT_3D ( 'NONE', #45408, #56308, #63080 ) ;
#51963=CARTESIAN_POINT ( 'NONE',  ( 10.00000000000000000, -32.34446384429989507, 26.79245525562703278 ) ) ;
#51969=ORIENTED_EDGE ( 'NONE', *, *, #71868, .F. ) ;
#51976=CARTESIAN_POINT ( 'NONE',  ( 10.00000000000000000, -40.98264845739743834, -9.188173127307738497 ) ) ;
#51989=LINE ( 'NONE', #41101, #66211 ) ;
#52007=DIRECTION ( 'NONE',  ( -1.000000000000000000, 0.000000000000000000, 0.000000000000000000 ) ) ;
#52024=DIRECTION ( 'NONE',  ( -1.000000000000000000, 0.000000000000000000, 0.000000000000000000 ) ) ;
#52032=DIRECTION ( 'NONE',  ( -1.000000000000000000, -0.000000000000000000, -0.000000000000000000 ) ) ;
#52051=ORIENTED_EDGE ( 'NONE', *, *, #13235, .T. ) ;
#52066=CARTESIAN_POINT ( 'NONE',  ( 10.00000000000000000, 0.000000000000000000, 0.000000000000000000 ) ) ;
#52069=ORIENTED_EDGE ( 'NONE', *, *, #46257, .F. ) ;
#52079=LINE ( 'NONE', #5868, #10965 ) ;
#52081=LINE ( 'NONE', #69374, #57834 ) ;
#52093=DIRECTION ( 'NONE',  ( 1.000000000000000000, 0.000000000000000000, -0.000000000000000000 ) ) ;
#52102=CYLINDRICAL_SURFACE ( 'NONE', #18942, 16.00000000000000000 ) ;
#52114=DIRECTION ( 'NONE',  ( -1.000000000000000000, 0.000000000000000000, -0.000000000000000000 ) ) ;
#52121=VERTEX_POINT ( 'NONE', #1321 ) ;
#52130=ADVANCED_FACE ( 'NONE', ( #13648 ), #36957, .F. ) ;
#52157=CIRCLE ( 'NONE', #45767, 16.00000000000000000 ) ;
#52165=FACE_OUTER_BOUND ( 'NONE', #51415, .T. ) ;
#52171=ORIENTED_EDGE ( 'NONE', *, *, #72449, .T. ) ;
#52173=DIRECTION ( 'NONE',  ( 0.000000000000000000, 0.000000000000000000, 1.000000000000000000 ) ) ;
#52175=CARTESIAN_POINT ( 'NONE',  ( 10.00000000000000000, 30.80686688397010542, 21.53537804866092387 ) ) ;
#52176=DIRECTION ( 'NONE',  ( -1.000000000000000000, 0.000000000000000000, 0.000000000000000000 ) ) ;
#52182=CARTESIAN_POINT ( 'NONE',  ( -3.000000000000000000, -22.32062822937469804, -14.36278369418829826 ) ) ;
#52211=ORIENTED_EDGE ( 'NONE', *, *, #59179, .F. ) ;
#52212=CARTESIAN_POINT ( 'NONE',  ( -3.000000000000000000, 26.50000000000000000, -1.500000000000001332 ) ) ;
#52213=DIRECTION ( 'NONE',  ( 0.000000000000000000, 0.000000000000000000, 1.000000000000000000 ) ) ;
#52225=DIRECTION ( 'NONE',  ( -1.000000000000000000, 0.000000000000000000, -0.000000000000000000 ) ) ;
#52235=ORIENTED_EDGE ( 'NONE', *, *, #7951, .F. ) ;
#52245=APPLICATION_CONTEXT ( 'automotive_design' ) ;
#52252=( LENGTH_UNIT ( ) NAMED_UNIT ( * ) SI_UNIT ( .MILLI., .METRE. ) );
#52267=VECTOR ( 'NONE', #71329, 999.9999999999998863 ) ;
#52274=DIRECTION ( 'NONE',  ( 0.000000000000000000, 0.000000000000000000, 1.000000000000000000 ) ) ;
#52276=ADVANCED_FACE ( 'NONE', ( #50068 ), #22632, .F. ) ;
#52277=DIRECTION ( 'NONE',  ( -1.000000000000000000, -0.000000000000000000, -0.000000000000000000 ) ) ;
#52279=CIRCLE ( 'NONE', #43870, 37.49900000000000233 ) ;
#52288=EDGE_CURVE ( 'NONE', #13480, #779, #26949, .T. ) ;
#52292=AXIS2_PLACEMENT_3D ( 'NONE', #23495, #18585, #64099 ) ;
#52306=VECTOR ( 'NONE', #2483, 1000.000000000000114 ) ;
#52309=DIRECTION ( 'NONE',  ( 0.000000000000000000, 0.000000000000000000, 1.000000000000000000 ) ) ;
#52312=FACE_OUTER_BOUND ( 'NONE', #4189, .T. ) ;
#52314=VERTEX_POINT ( 'NONE', #9489 ) ;
#52319=ORIENTED_EDGE ( 'NONE', *, *, #69679, .F. ) ;
#52330=EDGE_LOOP ( 'NONE', ( #51893, #72250, #59838, #18034 ) ) ;
#52362=EDGE_CURVE ( 'NONE', #1695, #53734, #29304, .T. ) ;
#52373=CARTESIAN_POINT ( 'NONE',  ( 0.000000000000000000, -35.53030884539077050, -12.26510123303296851 ) ) ;
#52385=ADVANCED_FACE ( 'NONE', ( #55726 ), #73746, .T. ) ;
#52387=EDGE_CURVE ( 'NONE', #17536, #51707, #19754, .T. ) ;
#52391=ORIENTED_EDGE ( 'NONE', *, *, #26706, .F. ) ;
#52408=EDGE_LOOP ( 'NONE', ( #27999, #53597, #41506, #28575 ) ) ;
#52410=ORIENTED_EDGE ( 'NONE', *, *, #3675, .T. ) ;
#52419=ORIENTED_EDGE ( 'NONE', *, *, #21793, .F. ) ;
#52421=CIRCLE ( 'NONE', #20007, 16.00000000000000000 ) ;
#52444=EDGE_CURVE ( 'NONE', #69078, #35859, #53055, .T. ) ;
#52451=CIRCLE ( 'NONE', #59652, 16.00000000000000000 ) ;
#52456=LINE ( 'NONE', #29517, #38971 ) ;
#52461=EDGE_CURVE ( 'NONE', #23684, #23048, #16124, .T. ) ;
#52471=DIRECTION ( 'NONE',  ( 0.000000000000000000, 0.7431448254773862505, 0.6691306063588672304 ) ) ;
#52474=EDGE_CURVE ( 'NONE', #66826, #21068, #12522, .T. ) ;
#52490=CARTESIAN_POINT ( 'NONE',  ( 0.000000000000000000, 12.26510123303259725, 35.53030884539089840 ) ) ;
#52491=VECTOR ( 'NONE', #32377, 1000.000000000000000 ) ;
#52495=LINE ( 'NONE', #6293, #65684 ) ;
#52509=CIRCLE ( 'NONE', #8090, 42.00000000000000000 ) ;
#52513=CARTESIAN_POINT ( 'NONE',  ( -3.000000000000000000, 16.83928648764945279, -16.46020748918028076 ) ) ;
#52518=EDGE_LOOP ( 'NONE', ( #46157, #46489, #67143, #20822 ) ) ;
#52540=FACE_OUTER_BOUND ( 'NONE', #43917, .T. ) ;
#52541=CARTESIAN_POINT ( 'NONE',  ( 10.00000000000000000, 16.23288003029543347, -33.80338159004267595 ) ) ;
#52547=DIRECTION ( 'NONE',  ( 0.000000000000000000, 0.000000000000000000, 1.000000000000000000 ) ) ;
#52559=VECTOR ( 'NONE', #110, 1000.000000000000000 ) ;
#52562=FACE_OUTER_BOUND ( 'NONE', #41969, .T. ) ;
#52576=CARTESIAN_POINT ( 'NONE',  ( 0.000000000000000000, 0.000000000000000000, 0.000000000000000000 ) ) ;
#52577=ORIENTED_EDGE ( 'NONE', *, *, #73086, .F. ) ;
#52578=CIRCLE ( 'NONE', #23766, 42.00000000000000000 ) ;
#52587=ORIENTED_EDGE ( 'NONE', *, *, #11205, .T. ) ;
#52596=ADVANCED_FACE ( 'NONE', ( #70687 ), #42889, .F. ) ;
#52612=ORIENTED_EDGE ( 'NONE', *, *, #42342, .T. ) ;
#52614=ORIENTED_EDGE ( 'NONE', *, *, #67019, .T. ) ;
#52619=VECTOR ( 'NONE', #61081, 1000.000000000000000 ) ;
#52620=ORIENTED_EDGE ( 'NONE', *, *, #56292, .F. ) ;
#52625=CIRCLE ( 'NONE', #11775, 16.00000000000000355 ) ;
#52626=ORIENTED_EDGE ( 'NONE', *, *, #12659, .F. ) ;
#52638=CARTESIAN_POINT ( 'NONE',  ( 10.00000000000000000, 21.53537804866081373, 30.80686688397018358 ) ) ;
#52639=VERTEX_POINT ( 'NONE', #30839 ) ;
#52649=ADVANCED_FACE ( 'NONE', ( #31955 ), #54170, .T. ) ;
#52660=CIRCLE ( 'NONE', #45490, 16.00000000000000355 ) ;
#52676=DIRECTION ( 'NONE',  ( 0.000000000000000000, 0.5877852522924797984, -0.8090169943749426773 ) ) ;
#52680=DIRECTION ( 'NONE',  ( 0.000000000000000000, -0.4539904997395541320, 0.8910065241883640130 ) ) ;
#52685=VERTEX_POINT ( 'NONE', #1958 ) ;
#52689=DIRECTION ( 'NONE',  ( 1.000000000000000000, 0.000000000000000000, 0.000000000000000000 ) ) ;
#52700=ORIENTED_EDGE ( 'NONE', *, *, #55586, .F. ) ;
#52745=CIRCLE ( 'NONE', #16733, 42.00000000000000000 ) ;
#52747=AXIS2_PLACEMENT_3D ( 'NONE', #38663, #43939, #10080 ) ;
#52753=CYLINDRICAL_SURFACE ( 'NONE', #68117, 16.00000000000000000 ) ;
#52765=FACE_OUTER_BOUND ( 'NONE', #52958, .T. ) ;
#52776=ORIENTED_EDGE ( 'NONE', *, *, #64982, .T. ) ;
#52778=CARTESIAN_POINT ( 'NONE',  ( 10.00000000000000000, -35.95386929396264009, 10.96151621346475658 ) ) ;
#52781=AXIS2_PLACEMENT_3D ( 'NONE', #50521, #73068, #34997 ) ;
#52782=EDGE_CURVE ( 'NONE', #62190, #70424, #72539, .T. ) ;
#52817=CARTESIAN_POINT ( 'NONE',  ( 0.000000000000000000, 0.8828120875900632436, 37.48860685352291000 ) ) ;
#52830=DIRECTION ( 'NONE',  ( -1.000000000000000000, -0.000000000000000000, 0.000000000000000000 ) ) ;
#52834=CARTESIAN_POINT ( 'NONE',  ( -10.00000000000000000, 0.000000000000000000, 0.000000000000000000 ) ) ;
#52835=AXIS2_PLACEMENT_3D ( 'NONE', #21957, #62576, #32854 ) ;
#52838=CARTESIAN_POINT ( 'NONE',  ( 10.00000000000000000, -37.58145647212455032, 16.68533520207890319 ) ) ;
#52848=DIRECTION ( 'NONE',  ( 0.000000000000000000, 0.000000000000000000, 1.000000000000000000 ) ) ;
#52858=DIRECTION ( 'NONE',  ( -1.000000000000000000, 0.000000000000000000, 0.000000000000000000 ) ) ;
#52861=DIRECTION ( 'NONE',  ( 1.000000000000000000, 0.000000000000000000, 0.000000000000000000 ) ) ;
#52873=ADVANCED_FACE ( 'NONE', ( #61655 ), #56007, .F. ) ;
#52874=VERTEX_POINT ( 'NONE', #49609 ) ;
#52884=DIRECTION ( 'NONE',  ( 0.000000000000000000, 0.000000000000000000, 1.000000000000000000 ) ) ;
#52905=ORIENTED_EDGE ( 'NONE', *, *, #73163, .F. ) ;
#52940=LINE ( 'NONE', #1481, #63844 ) ;
#52948=EDGE_CURVE ( 'NONE', #17753, #68977, #42630, .T. ) ;
#52958=EDGE_LOOP ( 'NONE', ( #39948, #70640, #4467, #21728 ) ) ;
#52962=DIRECTION ( 'NONE',  ( 0.000000000000000000, 0.000000000000000000, 1.000000000000000000 ) ) ;
#52963=EDGE_CURVE ( 'NONE', #43951, #9784, #29408, .T. ) ;
#52967=ORIENTED_EDGE ( 'NONE', *, *, #14373, .T. ) ;
#52983=ORIENTED_EDGE ( 'NONE', *, *, #55762, .F. ) ;
#52987=LINE ( 'NONE', #69535, #72503 ) ;
#53000=EDGE_LOOP ( 'NONE', ( #20420, #9155, #35688, #9216 ) ) ;
#53004=FILL_AREA_STYLE ('',( #58267 ) ) ;
#53009=VERTEX_POINT ( 'NONE', #51477 ) ;
#53028=DIRECTION ( 'NONE',  ( -0.000000000000000000, -0.3090169943749573878, 0.9510565162951503115 ) ) ;
#53043=EDGE_CURVE ( 'NONE', #21151, #61705, #61804, .T. ) ;
#53045=LINE ( 'NONE', #35731, #6427 ) ;
#53047=ADVANCED_FACE ( 'NONE', ( #62278 ), #67913, .T. ) ;
#53055=LINE ( 'NONE', #1591, #71321 ) ;
#53069=ORIENTED_EDGE ( 'NONE', *, *, #30696, .T. ) ;
#53085=CIRCLE ( 'NONE', #62719, 37.49900000000001654 ) ;
#53087=ORIENTED_EDGE ( 'NONE', *, *, #5057, .F. ) ;
#53093=CYLINDRICAL_SURFACE ( 'NONE', #46100, 16.00000000000000000 ) ;
#53117=CIRCLE ( 'NONE', #14672, 15.99999999999999822 ) ;
#53118=ORIENTED_EDGE ( 'NONE', *, *, #43828, .T. ) ;
#53122=DIRECTION ( 'NONE',  ( 0.000000000000000000, 0.000000000000000000, 1.000000000000000000 ) ) ;
#53123=LINE ( 'NONE', #17788, #15792 ) ;
#53125=CARTESIAN_POINT ( 'NONE',  ( 0.000000000000000000, 0.000000000000000000, 0.000000000000000000 ) ) ;
#53128=EDGE_CURVE ( 'NONE', #14021, #11081, #16030, .T. ) ;
#53131=EDGE_CURVE ( 'NONE', #24073, #18738, #44238, .T. ) ;
#53155=CARTESIAN_POINT ( 'NONE',  ( 10.00000000000000000, -33.17418723428319538, 17.67226234102814431 ) ) ;
#53162=AXIS2_PLACEMENT_3D ( 'NONE', #34249, #57194, #63951 ) ;
#53175=EDGE_LOOP ( 'NONE', ( #43305, #20905, #12471, #28957 ) ) ;
#53177=VERTEX_POINT ( 'NONE', #18251 ) ;
#53181=FACE_OUTER_BOUND ( 'NONE', #68741, .T. ) ;
#53183=DIRECTION ( 'NONE',  ( 0.000000000000000000, -0.8910065241883627918, -0.4539904997395569630 ) ) ;
#53193=DIRECTION ( 'NONE',  ( 0.000000000000000000, 0.3090169943749442316, 0.9510565162951545304 ) ) ;
#53195=DIRECTION ( 'NONE',  ( 0.000000000000000000, -0.9510565162951565288, 0.3090169943749384029 ) ) ;
#53196=CARTESIAN_POINT ( 'NONE',  ( 10.00000000000000000, -38.55633173626998911, -16.65560815589452304 ) ) ;
#53202=ORIENTED_EDGE ( 'NONE', *, *, #20818, .T. ) ;
#53208=EDGE_CURVE ( 'NONE', #17471, #48180, #69098, .T. ) ;
#53214=ORIENTED_EDGE ( 'NONE', *, *, #26743, .T. ) ;
#53218=AXIS2_PLACEMENT_3D ( 'NONE', #33043, #67273, #43249 ) ;
#53223=CARTESIAN_POINT ( 'NONE',  ( 0.000000000000000000, 23.50000000000000000, -1.500000000000001332 ) ) ;
#53228=DIRECTION ( 'NONE',  ( -1.000000000000000000, -0.000000000000000000, 0.000000000000000000 ) ) ;
#53229=ADVANCED_FACE ( 'NONE', ( #22804 ), #69385, .T. ) ;
#53244=ORIENTED_EDGE ( 'NONE', *, *, #10264, .T. ) ;
#53263=EDGE_LOOP ( 'NONE', ( #39367, #26461, #16433, #33248 ) ) ;
#53273=ADVANCED_FACE ( 'NONE', ( #5884 ), #28795, .F. ) ;
#53276=ORIENTED_EDGE ( 'NONE', *, *, #45860, .F. ) ;
#53287=VERTEX_POINT ( 'NONE', #57749 ) ;
#53289=EDGE_CURVE ( 'NONE', #39053, #54369, #21037, .T. ) ;
#53292=DIRECTION ( 'NONE',  ( 0.000000000000000000, 0.000000000000000000, 1.000000000000000000 ) ) ;
#53296=EDGE_LOOP ( 'NONE', ( #4395, #35736, #29606, #34565 ) ) ;
#53301=ORIENTED_EDGE ( 'NONE', *, *, #7634, .T. ) ;
#53311=DIRECTION ( 'NONE',  ( -1.000000000000000000, -0.000000000000000000, -0.000000000000000000 ) ) ;
#53323=CARTESIAN_POINT ( 'NONE',  ( -3.000000000000000000, 23.50000000000000000, 1.499999999999997780 ) ) ;
#53324=EDGE_CURVE ( 'NONE', #61596, #68440, #13385, .T. ) ;
#53331=LINE ( 'NONE', #32139, #10425 ) ;
#53347=AXIS2_PLACEMENT_3D ( 'NONE', #29297, #24777, #784 ) ;
#53354=CARTESIAN_POINT ( 'NONE',  ( 0.000000000000000000, 27.13269053701132094, -25.88420570971372570 ) ) ;
#53362=ORIENTED_EDGE ( 'NONE', *, *, #33916, .T. ) ;
#53383=VERTEX_POINT ( 'NONE', #34846 ) ;
#53390=FACE_OUTER_BOUND ( 'NONE', #45419, .T. ) ;
#53393=DIRECTION ( 'NONE',  ( -1.000000000000000000, -0.000000000000000000, -0.000000000000000000 ) ) ;
#53398=LINE ( 'NONE', #60169, #47632 ) ;
#53410=DIRECTION ( 'NONE',  ( 0.000000000000000000, -0.9135454576426059736, 0.4067366430757887730 ) ) ;
#53411=DIRECTION ( 'NONE',  ( 0.000000000000000000, 0.1045284632676436315, 0.9945218953682742891 ) ) ;
#53414=ADVANCED_FACE ( 'NONE', ( #7002 ), #23561, .F. ) ;
#53415=ORIENTED_EDGE ( 'NONE', *, *, #60997, .T. ) ;
#53418=CIRCLE ( 'NONE', #25775, 42.00000000000000000 ) ;
#53424=EDGE_LOOP ( 'NONE', ( #50503, #72405, #22127, #46781 ) ) ;
#53434=DIRECTION ( 'NONE',  ( -1.000000000000000000, 0.000000000000000000, -0.000000000000000000 ) ) ;
#53449=EDGE_CURVE ( 'NONE', #5103, #50093, #65505, .T. ) ;
#53450=ORIENTED_EDGE ( 'NONE', *, *, #48893, .T. ) ;
#53457=ADVANCED_FACE ( 'NONE', ( #42341 ), #70893, .F. ) ;
#53458=DIRECTION ( 'NONE',  ( -1.000000000000000000, 0.000000000000000000, 0.000000000000000000 ) ) ;
#53470=EDGE_LOOP ( 'NONE', ( #42759, #31344, #8695, #68250 ) ) ;
#53494=ORIENTED_EDGE ( 'NONE', *, *, #50045, .T. ) ;
#53498=EDGE_CURVE ( 'NONE', #913, #49620, #27043, .T. ) ;
#53504=DIRECTION ( 'NONE',  ( -1.000000000000000000, 0.000000000000000000, 0.000000000000000000 ) ) ;
#53506=FACE_OUTER_BOUND ( 'NONE', #31877, .T. ) ;
#53510=CARTESIAN_POINT ( 'NONE',  ( 0.000000000000000000, 33.00180498840046539, 17.80606268964551120 ) ) ;
#53518=DIRECTION ( 'NONE',  ( 0.000000000000000000, -0.3090169943749563330, 0.9510565162951507556 ) ) ;
#53520=VERTEX_POINT ( 'NONE', #10241 ) ;
#53532=ORIENTED_EDGE ( 'NONE', *, *, #44985, .T. ) ;
#53540=ORIENTED_EDGE ( 'NONE', *, *, #6363, .T. ) ;
#53550=DIRECTION ( 'NONE',  ( -1.000000000000000000, -0.000000000000000000, -0.000000000000000000 ) ) ;
#53552=CARTESIAN_POINT ( 'NONE',  ( 10.00000000000000000, 4.992566952385523393, -37.16516213103272293 ) ) ;
#53564=FACE_OUTER_BOUND ( 'NONE', #7412, .T. ) ;
#53567=DIRECTION ( 'NONE',  ( -1.000000000000000000, -0.000000000000000000, 0.000000000000000000 ) ) ;
#53570=EDGE_CURVE ( 'NONE', #17509, #64359, #15516, .T. ) ;
#53572=CARTESIAN_POINT ( 'NONE',  ( 10.00000000000000000, 40.98264845739763018, -9.188173127306866306 ) ) ;
#53577=CIRCLE ( 'NONE', #16332, 16.00000000000000000 ) ;
#53587=VECTOR ( 'NONE', #61136, 1000.000000000000000 ) ;
#53597=ORIENTED_EDGE ( 'NONE', *, *, #8419, .F. ) ;
#53625=ORIENTED_EDGE ( 'NONE', *, *, #26665, .T. ) ;
#53638=EDGE_CURVE ( 'NONE', #52121, #70257, #16468, .T. ) ;
#53646=EDGE_CURVE ( 'NONE', #8512, #27109, #23655, .T. ) ;
#53658=DIRECTION ( 'NONE',  ( 0.000000000000000000, 0.9135454576426003115, 0.4067366430758017071 ) ) ;
#53662=CARTESIAN_POINT ( 'NONE',  ( 0.000000000000000000, 0.000000000000000000, 0.000000000000000000 ) ) ;
#53668=EDGE_LOOP ( 'NONE', ( #68443, #14317, #31910, #48990 ) ) ;
#53677=DIRECTION ( 'NONE',  ( 1.000000000000000000, -0.000000000000000000, -0.000000000000000000 ) ) ;
#53690=VECTOR ( 'NONE', #12441, 1000.000000000000000 ) ;
#53705=DIRECTION ( 'NONE',  ( 0.000000000000000000, 0.000000000000000000, 1.000000000000000000 ) ) ;
#53706=DIRECTION ( 'NONE',  ( 0.000000000000000000, 0.000000000000000000, 1.000000000000000000 ) ) ;
#53713=EDGE_LOOP ( 'NONE', ( #42003, #6879, #66483, #7936 ) ) ;
#53734=VERTEX_POINT ( 'NONE', #40681 ) ;
#53737=EDGE_LOOP ( 'NONE', ( #25055, #29649, #66571, #68898 ) ) ;
#53738=AXIS2_PLACEMENT_3D ( 'NONE', #40749, #12160, #59145 ) ;
#53756=DIRECTION ( 'NONE',  ( 0.000000000000000000, 0.4539904997395414754, 0.8910065241883706744 ) ) ;
#53757=AXIS2_PLACEMENT_3D ( 'NONE', #30676, #6298, #1434 ) ;
#53766=LINE ( 'NONE', #43254, #20618 ) ;
#53768=DIRECTION ( 'NONE',  ( -1.000000000000000000, 0.000000000000000000, 0.000000000000000000 ) ) ;
#53780=CIRCLE ( 'NONE', #67029, 42.00000000000000000 ) ;
#53784=CIRCLE ( 'NONE', #30971, 16.00000000000000000 ) ;
#53785=CIRCLE ( 'NONE', #8114, 37.49900000000000944 ) ;
#53798=CARTESIAN_POINT ( 'NONE',  ( 10.00000000000000000, 10.74501242461333028, -35.92658777277499382 ) ) ;
#53805=CIRCLE ( 'NONE', #33408, 15.99999999999999822 ) ;
#53838=DIRECTION ( 'NONE',  ( 0.000000000000000000, 0.5877852522924696954, 0.8090169943749498938 ) ) ;
#53847=DIRECTION ( 'NONE',  ( 0.000000000000000000, 0.000000000000000000, 1.000000000000000000 ) ) ;
#53850=ORIENTED_EDGE ( 'NONE', *, *, #73086, .T. ) ;
#53857=DIRECTION ( 'NONE',  ( -1.000000000000000000, 0.000000000000000000, 0.000000000000000000 ) ) ;
#53870=AXIS2_PLACEMENT_3D ( 'NONE', #41416, #499, #57970 ) ;
#53876=EDGE_CURVE ( 'NONE', #46530, #3129, #42881, .T. ) ;
#53881=DIRECTION ( 'NONE',  ( 1.000000000000000000, 0.000000000000000000, -0.000000000000000000 ) ) ;
#53888=AXIS2_PLACEMENT_3D ( 'NONE', #26819, #54302, #33572 ) ;
#53896=CIRCLE ( 'NONE', #62335, 16.00000000000000000 ) ;
#53901=VERTEX_POINT ( 'NONE', #46055 ) ;
#53939=EDGE_LOOP ( 'NONE', ( #60312, #18320, #20159, #18125 ) ) ;
#53947=ORIENTED_EDGE ( 'NONE', *, *, #8909, .F. ) ;
#53959=CIRCLE ( 'NONE', #3518, 16.00000000000000000 ) ;
#53964=DIRECTION ( 'NONE',  ( 1.000000000000000000, 0.000000000000000000, -0.000000000000000000 ) ) ;
#53970=FACE_OUTER_BOUND ( 'NONE', #21345, .T. ) ;
#53972=DIRECTION ( 'NONE',  ( -1.000000000000000000, -0.000000000000000000, 0.000000000000000000 ) ) ;
#53983=CIRCLE ( 'NONE', #5970, 37.49900000000000233 ) ;
#53998=CYLINDRICAL_SURFACE ( 'NONE', #43236, 16.00000000000000000 ) ;
#54000=FACE_OUTER_BOUND ( 'NONE', #21062, .T. ) ;
#54002=DIRECTION ( 'NONE',  ( -1.000000000000000000, 0.000000000000000000, -0.000000000000000000 ) ) ;
#54006=VECTOR ( 'NONE', #49348, 1000.000000000000000 ) ;
#54008=ORIENTED_EDGE ( 'NONE', *, *, #28445, .F. ) ;
#54011=ORIENTED_EDGE ( 'NONE', *, *, #31422, .F. ) ;
#54029=VECTOR ( 'NONE', #73995, 1000.000000000000000 ) ;
#54045=EDGE_LOOP ( 'NONE', ( #55942, #18912, #33957, #30865, #24403, #67249, #68540, #21537, #57912, #57908, #59017, #62919, #12836, #70141, #36311, #63463, #59103, #38583, #49254, #46798, #22286, #22800, #63254, #62136, #28677, #10707, #13301, #1403, #48270, #47234, #58174, #20431, #34788, #70625, #13051, #4265, #22867, #61052, #48091, #54425, #68059, #35789, #19491, #24104, #60233, #9792, #60671, #46222, #18371, #57733, #63546, #56049, #74317, #40391, #41218, #72605, #32733, #20700, #54190, #24746, #3485, #42469, #30587, #3560, #54752, #73934, #57323, #51386, #15740, #28410, #15139, #21270, #45900, #48107, #42895, #59439, #51205, #9795, #13022, #17056, #13566, #49265, #48833, #43369, #58651, #40909, #65380, #14405, #33836, #70905, #31817, #72134, #54011, #23250, #42722, #45704, #48110, #23164, #64772, #56490, #14070, #62612, #9819, #6193, #32335, #19066, #71910, #34654, #52319, #34505, #17841, #68872, #9126, #39805, #40434, #11620, #47101, #71161, #37082, #65035, #26541, #40417, #46665, #65665, #12041, #72595, #55481, #50285, #47879, #9599, #1898, #45972, #22285, #4693, #65611, #19719, #10568, #27349, #9836, #1527, #12243, #30201, #10718, #27476, #3452, #15534, #505, #2666, #44024, #72623, #38474, #60029, #23853, #55005, #46807, #7103, #66315, #54848, #5484, #25157, #31395, #66937, #16932, #13750, #44407 ) ) ;
#54046=DIRECTION ( 'NONE',  ( -1.000000000000000000, -0.000000000000000000, 0.000000000000000000 ) ) ;
#54055=CARTESIAN_POINT ( 'NONE',  ( 10.00000000000000000, 0.000000000000000000, 0.000000000000000000 ) ) ;
#54062=CARTESIAN_POINT ( 'NONE',  ( 10.00000000000000000, 0.000000000000000000, 0.000000000000000000 ) ) ;
#54063=ORIENTED_EDGE ( 'NONE', *, *, #7147, .F. ) ;
#54068=CARTESIAN_POINT ( 'NONE',  ( 0.000000000000000000, -16.45098606841102651, -33.79645857604531045 ) ) ;
#54076=FACE_OUTER_BOUND ( 'NONE', #12924, .T. ) ;
#54090=CARTESIAN_POINT ( 'NONE',  ( 10.00000000000000000, 37.48860685352291000, -0.8828120875901940279 ) ) ;
#54093=CARTESIAN_POINT ( 'NONE',  ( 4.999999999999999112, 40.98264845739749518, 9.188173127307448951 ) ) ;
#54098=ORIENTED_EDGE ( 'NONE', *, *, #19018, .F. ) ;
#54104=DIRECTION ( 'NONE',  ( -1.000000000000000000, 0.000000000000000000, 0.000000000000000000 ) ) ;
#54120=VECTOR ( 'NONE', #30267, 1000.000000000000000 ) ;
#54160=ADVANCED_FACE ( 'NONE', ( #16646 ), #33936, .T. ) ;
#54170=CYLINDRICAL_SURFACE ( 'NONE', #4224, 16.00000000000000000 ) ;
#54179=ORIENTED_EDGE ( 'NONE', *, *, #23800, .F. ) ;
#54182=ORIENTED_EDGE ( 'NONE', *, *, #37621, .T. ) ;
#54184=EDGE_LOOP ( 'NONE', ( #29025, #58822, #47487, #59258 ) ) ;
#54186=VERTEX_POINT ( 'NONE', #27166 ) ;
#54190=ORIENTED_EDGE ( 'NONE', *, *, #19683, .F. ) ;
#54205=CARTESIAN_POINT ( 'NONE',  ( 10.00000000000000000, 35.53030884539084866, 12.26510123303271982 ) ) ;
#54224=DIRECTION ( 'NONE',  ( 1.000000000000000000, -0.000000000000000000, 0.000000000000000000 ) ) ;
#54232=PLANE ( 'NONE',  #17901 ) ;
#54234=ORIENTED_EDGE ( 'NONE', *, *, #8498, .F. ) ;
#54238=ADVANCED_FACE ( 'NONE', ( #59744 ), #7501, .T. ) ;
#54249=DIRECTION ( 'NONE',  ( 0.000000000000000000, -1.000000000000000000, -1.040834085586084257E-14 ) ) ;
#54281=AXIS2_PLACEMENT_3D ( 'NONE', #49218, #61625, #38319 ) ;
#54297=LINE ( 'NONE', #60678, #72717 ) ;
#54300=DIRECTION ( 'NONE',  ( 0.000000000000000000, -0.8090169943749426773, -0.5877852522924797984 ) ) ;
#54302=DIRECTION ( 'NONE',  ( -1.000000000000000000, -0.000000000000000000, -0.000000000000000000 ) ) ;
#54310=CARTESIAN_POINT ( 'NONE',  ( 10.00000000000000000, 32.34446384430010113, -26.79245525562679831 ) ) ;
#54331=AXIS2_PLACEMENT_3D ( 'NONE', #34920, #5623, #29620 ) ;
#54342=VECTOR ( 'NONE', #28126, 1000.000000000000114 ) ;
#54352=CIRCLE ( 'NONE', #5156, 42.00000000000000000 ) ;
#54361=FACE_OUTER_BOUND ( 'NONE', #35683, .T. ) ;
#54363=DIRECTION ( 'NONE',  ( -1.000000000000000000, 0.000000000000000000, 0.000000000000000000 ) ) ;
#54364=CARTESIAN_POINT ( 'NONE',  ( -3.000000000000000000, 23.50000000000000000, -1.500000000000001332 ) ) ;
#54369=VERTEX_POINT ( 'NONE', #71737 ) ;
#54370=ORIENTED_EDGE ( 'NONE', *, *, #12537, .T. ) ;
#54389=CARTESIAN_POINT ( 'NONE',  ( 0.000000000000000000, 8.688484142254221609, -21.88630264137359660 ) ) ;
#54396=AXIS2_PLACEMENT_3D ( 'NONE', #29616, #12341, #42038 ) ;
#54397=CARTESIAN_POINT ( 'NONE',  ( 0.000000000000000000, 0.000000000000000000, 0.000000000000000000 ) ) ;
#54410=CARTESIAN_POINT ( 'NONE',  ( 10.00000000000000000, 0.000000000000000000, 0.000000000000000000 ) ) ;
#54414=CARTESIAN_POINT ( 'NONE',  ( 10.00000000000000000, 33.00180498840046539, 17.80606268964551120 ) ) ;
#54417=CARTESIAN_POINT ( 'NONE',  ( -3.000000000000000000, 14.60985201121729737, -18.46759930825687945 ) ) ;
#54420=AXIS2_PLACEMENT_3D ( 'NONE', #17897, #5533, #5901 ) ;
#54425=ORIENTED_EDGE ( 'NONE', *, *, #47480, .F. ) ;
#54475=CIRCLE ( 'NONE', #73679, 16.00000000000000000 ) ;
#54476=VERTEX_POINT ( 'NONE', #60131 ) ;
#54479=CARTESIAN_POINT ( 'NONE',  ( 0.000000000000000000, 0.000000000000000000, 0.000000000000000000 ) ) ;
#54487=DIRECTION ( 'NONE',  ( 1.000000000000000000, -0.000000000000000000, 0.000000000000000000 ) ) ;
#54493=VECTOR ( 'NONE', #44925, 999.9999999999998863 ) ;
#54494=DIRECTION ( 'NONE',  ( 1.000000000000000000, 0.000000000000000000, 0.000000000000000000 ) ) ;
#54516=CARTESIAN_POINT ( 'NONE',  ( 0.000000000000000000, 40.68715046381943523, -10.41901085202036370 ) ) ;
#54518=EDGE_CURVE ( 'NONE', #13842, #68033, #62354, .T. ) ;
#54523=LINE ( 'NONE', #25941, #56627 ) ;
#54526=FACE_OUTER_BOUND ( 'NONE', #583, .T. ) ;
#54532=DIRECTION ( 'NONE',  ( 1.000000000000000000, 0.000000000000000000, 0.000000000000000000 ) ) ;
#54544=AXIS2_PLACEMENT_3D ( 'NONE', #11077, #57688, #68965 ) ;
#54565=DIRECTION ( 'NONE',  ( -1.000000000000000000, 0.000000000000000000, 0.000000000000000000 ) ) ;
#54591=ORIENTED_EDGE ( 'NONE', *, *, #28612, .T. ) ;
#54600=CARTESIAN_POINT ( 'NONE',  ( 10.00000000000000000, 0.000000000000000000, 0.000000000000000000 ) ) ;
#54632=DIRECTION ( 'NONE',  ( -1.000000000000000000, 0.000000000000000000, -0.000000000000000000 ) ) ;
#54639=CARTESIAN_POINT ( 'NONE',  ( 10.00000000000000000, -16.65560815589383381, -38.55633173627028754 ) ) ;
#54642=ORIENTED_EDGE ( 'NONE', *, *, #10933, .T. ) ;
#54656=DIRECTION ( 'NONE',  ( -0.000000000000000000, -0.3090169943749448977, -0.9510565162951543083 ) ) ;
#54661=CARTESIAN_POINT ( 'NONE',  ( 10.00000000000000000, 30.00120703465236716, -22.64427369931138756 ) ) ;
#54664=DIRECTION ( 'NONE',  ( 0.000000000000000000, 0.8090169943749486725, -0.5877852522924713607 ) ) ;
#54671=EDGE_CURVE ( 'NONE', #8248, #53177, #63863, .T. ) ;
#54674=DIRECTION ( 'NONE',  ( 0.000000000000000000, 0.000000000000000000, 1.000000000000000000 ) ) ;
#54681=VECTOR ( 'NONE', #66359, 1000.000000000000000 ) ;
#54689=LINE ( 'NONE', #26105, #56548 ) ;
#54691=ADVANCED_FACE ( 'NONE', ( #70920 ), #46523, .F. ) ;
#54692=ORIENTED_EDGE ( 'NONE', *, *, #1973, .T. ) ;
#54722=EDGE_CURVE ( 'NONE', #71560, #10365, #37450, .T. ) ;
#54729=DIRECTION ( 'NONE',  ( -1.000000000000000000, -0.000000000000000000, 0.000000000000000000 ) ) ;
#54736=EDGE_CURVE ( 'NONE', #18846, #23196, #63830, .T. ) ;
#54738=ORIENTED_EDGE ( 'NONE', *, *, #24554, .F. ) ;
#54752=ORIENTED_EDGE ( 'NONE', *, *, #39423, .F. ) ;
#54758=DIRECTION ( 'NONE',  ( -1.000000000000000000, -0.000000000000000000, -0.000000000000000000 ) ) ;
#54766=AXIS2_PLACEMENT_3D ( 'NONE', #14956, #65087, #26227 ) ;
#54773=EDGE_CURVE ( 'NONE', #21073, #27990, #20906, .T. ) ;
#54782=CARTESIAN_POINT ( 'NONE',  ( 0.000000000000000000, 0.000000000000000000, 0.000000000000000000 ) ) ;
#54788=DIRECTION ( 'NONE',  ( -1.000000000000000000, 0.000000000000000000, -0.000000000000000000 ) ) ;
#54800=CARTESIAN_POINT ( 'NONE',  ( 0.000000000000000000, 17.67226234102826510, 33.17418723428314564 ) ) ;
#54809=EDGE_CURVE ( 'NONE', #2347, #57306, #29003, .T. ) ;
#54810=ORIENTED_EDGE ( 'NONE', *, *, #47308, .F. ) ;
#54827=CIRCLE ( 'NONE', #24774, 37.49900000000000944 ) ;
#54828=PLANE ( 'NONE',  #28134 ) ;
#54834=LINE ( 'NONE', #4096, #63491 ) ;
#54842=ORIENTED_EDGE ( 'NONE', *, *, #632, .T. ) ;
#54848=ORIENTED_EDGE ( 'NONE', *, *, #52288, .F. ) ;
#54851=DIRECTION ( 'NONE',  ( 0.000000000000000000, -0.8090169943749402348, -0.5877852522924830181 ) ) ;
#54852=EDGE_LOOP ( 'NONE', ( #27992, #22215, #41178, #71957 ) ) ;
#54877=CARTESIAN_POINT ( 'NONE',  ( 0.000000000000000000, 0.000000000000000000, 0.000000000000000000 ) ) ;
#54883=CIRCLE ( 'NONE', #34436, 37.49900000000000233 ) ;
#54889=FACE_OUTER_BOUND ( 'NONE', #51139, .T. ) ;
#54892=DIRECTION ( 'NONE',  ( -1.000000000000000000, -0.000000000000000000, 0.000000000000000000 ) ) ;
#54905=VERTEX_POINT ( 'NONE', #66772 ) ;
#54946=DIRECTION ( 'NONE',  ( 0.000000000000000000, 0.000000000000000000, 1.000000000000000000 ) ) ;
#54954=VERTEX_POINT ( 'NONE', #74263 ) ;
#54958=DIRECTION ( 'NONE',  ( -1.000000000000000000, -0.000000000000000000, -0.000000000000000000 ) ) ;
#54960=DIRECTION ( 'NONE',  ( -1.000000000000000000, -0.000000000000000000, -0.000000000000000000 ) ) ;
#54961=DIRECTION ( 'NONE',  ( 0.000000000000000000, -0.4539904997395352027, -0.8910065241883737830 ) ) ;
#54976=DIRECTION ( 'NONE',  ( -1.000000000000000000, 0.000000000000000000, 0.000000000000000000 ) ) ;
#54986=VERTEX_POINT ( 'NONE', #44964 ) ;
#54988=DIRECTION ( 'NONE',  ( -1.000000000000000000, 0.000000000000000000, 0.000000000000000000 ) ) ;
#54991=CIRCLE ( 'NONE', #56187, 42.00000000000000000 ) ;
#54994=CARTESIAN_POINT ( 'NONE',  ( 5.000000000000000000, -15.48615015657555993, -39.04073710021360455 ) ) ;
#55005=ORIENTED_EDGE ( 'NONE', *, *, #16455, .F. ) ;
#55018=EDGE_CURVE ( 'NONE', #66019, #18578, #39867, .T. ) ;
#55030=ORIENTED_EDGE ( 'NONE', *, *, #67118, .T. ) ;
#55034=VERTEX_POINT ( 'NONE', #61886 ) ;
#55038=CARTESIAN_POINT ( 'NONE',  ( 0.000000000000000000, 21.40280677340371795, 36.13751322684426270 ) ) ;
#55046=AXIS2_PLACEMENT_3D ( 'NONE', #36874, #31235, #14316 ) ;
#55059=FACE_OUTER_BOUND ( 'NONE', #30131, .T. ) ;
#55060=DIRECTION ( 'NONE',  ( 0.000000000000000000, 0.1564344650402242354, 0.9876883405951387696 ) ) ;
#55067=EDGE_CURVE ( 'NONE', #23136, #33855, #53117, .T. ) ;
#55100=CARTESIAN_POINT ( 'NONE',  ( 0.000000000000000000, 0.000000000000000000, 0.000000000000000000 ) ) ;
#55110=DIRECTION ( 'NONE',  ( 1.000000000000000000, 0.000000000000000000, 0.000000000000000000 ) ) ;
#55112=CARTESIAN_POINT ( 'NONE',  ( 10.00000000000000000, 0.8828120875905820508, -37.48860685352290290 ) ) ;
#55118=ORIENTED_EDGE ( 'NONE', *, *, #45618, .T. ) ;
#55130=VERTEX_POINT ( 'NONE', #2092 ) ;
#55133=ORIENTED_EDGE ( 'NONE', *, *, #58401, .F. ) ;
#55142=CARTESIAN_POINT ( 'NONE',  ( 0.000000000000000000, 0.000000000000000000, 0.000000000000000000 ) ) ;
#55145=FACE_OUTER_BOUND ( 'NONE', #73398, .T. ) ;
#55146=VECTOR ( 'NONE', #37504, 1000.000000000000227 ) ;
#55154=CARTESIAN_POINT ( 'NONE',  ( 10.00000000000000000, 0.000000000000000000, 0.000000000000000000 ) ) ;
#55170=EDGE_LOOP ( 'NONE', ( #10665, #65328, #64739, #50040 ) ) ;
#55176=AXIS2_PLACEMENT_3D ( 'NONE', #45854, #48416, #59708 ) ;
#55178=DIRECTION ( 'NONE',  ( 1.000000000000000000, 0.000000000000000000, 0.000000000000000000 ) ) ;
#55183=EDGE_CURVE ( 'NONE', #27537, #74050, #61488, .T. ) ;
#55195=ORIENTED_EDGE ( 'NONE', *, *, #32216, .T. ) ;
#55200=CIRCLE ( 'NONE', #17969, 16.00000000000000000 ) ;
#55207=CYLINDRICAL_SURFACE ( 'NONE', #71879, 37.49900000000000233 ) ;
#55234=AXIS2_PLACEMENT_3D ( 'NONE', #39260, #33601, #3949 ) ;
#55243=EDGE_CURVE ( 'NONE', #3072, #68962, #18281, .T. ) ;
#55249=DIRECTION ( 'NONE',  ( -1.000000000000000000, 0.000000000000000000, 0.000000000000000000 ) ) ;
#55250=CIRCLE ( 'NONE', #4895, 16.00000000000000000 ) ;
#55287=ORIENTED_EDGE ( 'NONE', *, *, #38007, .T. ) ;
#55298=EDGE_LOOP ( 'NONE', ( #54234, #51888, #880, #2699 ) ) ;
#55307=CIRCLE ( 'NONE', #22920, 37.49900000000000233 ) ;
#55313=VERTEX_POINT ( 'NONE', #2023 ) ;
#55315=EDGE_LOOP ( 'NONE', ( #10997, #8700, #52776, #7206 ) ) ;
#55316=DIRECTION ( 'NONE',  ( -1.000000000000000000, 0.000000000000000000, -0.000000000000000000 ) ) ;
#55334=DIRECTION ( 'NONE',  ( -1.000000000000000000, -0.000000000000000000, -0.000000000000000000 ) ) ;
#55360=AXIS2_PLACEMENT_3D ( 'NONE', #37116, #19436, #19804 ) ;
#55362=DIRECTION ( 'NONE',  ( 1.000000000000000000, 0.000000000000000000, 0.000000000000000000 ) ) ;
#55363=ORIENTED_EDGE ( 'NONE', *, *, #55018, .F. ) ;
#55367=ORIENTED_EDGE ( 'NONE', *, *, #24044, .T. ) ;
#55374=CARTESIAN_POINT ( 'NONE',  ( 0.000000000000000000, 0.000000000000000000, 0.000000000000000000 ) ) ;
#55375=VERTEX_POINT ( 'NONE', #36928 ) ;
#55404=ORIENTED_EDGE ( 'NONE', *, *, #65130, .T. ) ;
#55415=LINE ( 'NONE', #35802, #1418 ) ;
#55417=DIRECTION ( 'NONE',  ( -1.000000000000000000, 0.000000000000000000, 0.000000000000000000 ) ) ;
#55423=EDGE_CURVE ( 'NONE', #26982, #61409, #54352, .T. ) ;
#55425=CARTESIAN_POINT ( 'NONE',  ( 0.000000000000000000, 25.88420570971400991, 27.13269053701105449 ) ) ;
#55428=CARTESIAN_POINT ( 'NONE',  ( 10.00000000000000000, -6.555932627142676772, 37.01155633439056203 ) ) ;
#55444=EDGE_CURVE ( 'NONE', #59943, #63855, #6332, .T. ) ;
#55451=CIRCLE ( 'NONE', #56692, 16.00000000000000000 ) ;
#55454=EDGE_CURVE ( 'NONE', #44110, #62228, #27931, .T. ) ;
#55463=AXIS2_PLACEMENT_3D ( 'NONE', #44208, #60764, #37470 ) ;
#55466=AXIS2_PLACEMENT_3D ( 'NONE', #47832, #70377, #36544 ) ;
#55472=CARTESIAN_POINT ( 'NONE',  ( 10.00000000000000000, -30.80686688396994910, -21.53537804866113703 ) ) ;
#55481=ORIENTED_EDGE ( 'NONE', *, *, #63694, .F. ) ;
#55495=DIRECTION ( 'NONE',  ( 1.000000000000000000, 0.000000000000000000, 0.000000000000000000 ) ) ;
#55513=ADVANCED_FACE ( 'NONE', ( #62094 ), #66973, .F. ) ;
#55523=CARTESIAN_POINT ( 'NONE',  ( 10.00000000000000000, -21.53537804866103045, 30.80686688397002371 ) ) ;
#55528=FACE_BOUND ( 'NONE', #46589, .T. ) ;
#55537=CYLINDRICAL_SURFACE ( 'NONE', #43009, 16.00000000000000000 ) ;
#55561=FILL_AREA_STYLE_COLOUR ( '', #27291 ) ;
#55566=AXIS2_PLACEMENT_3D ( 'NONE', #55428, #5061, #67823 ) ;
#55582=DIRECTION ( 'NONE',  ( 0.000000000000000000, 0.7071067811865487940, -0.7071067811865462405 ) ) ;
#55586=EDGE_CURVE ( 'NONE', #1365, #41638, #67547, .T. ) ;
#55588=EDGE_CURVE ( 'NONE', #70424, #21232, #51544, .T. ) ;
#55615=DIRECTION ( 'NONE',  ( 1.000000000000000000, 0.000000000000000000, -0.000000000000000000 ) ) ;
#55619=DIRECTION ( 'NONE',  ( 0.000000000000000000, 0.000000000000000000, 1.000000000000000000 ) ) ;
#55658=EDGE_CURVE ( 'NONE', #66947, #60556, #61545, .T. ) ;
#55687=ORIENTED_EDGE ( 'NONE', *, *, #23458, .T. ) ;
#55690=EDGE_LOOP ( 'NONE', ( #43485, #12685, #57229, #13290 ) ) ;
#55694=CARTESIAN_POINT ( 'NONE',  ( 0.000000000000000000, -10.45096189432314837, -21.10159698893440350 ) ) ;
#55721=AXIS2_PLACEMENT_3D ( 'NONE', #48611, #66644, #36214 ) ;
#55723=DIRECTION ( 'NONE',  ( 0.000000000000000000, -0.8910065241883626808, -0.4539904997395570740 ) ) ;
#55724=DIRECTION ( 'NONE',  ( -1.000000000000000000, -0.000000000000000000, -0.000000000000000000 ) ) ;
#55726=FACE_OUTER_BOUND ( 'NONE', #67, .T. ) ;
#55729=CIRCLE ( 'NONE', #54544, 16.00000000000000000 ) ;
#55731=CARTESIAN_POINT ( 'NONE',  ( 5.000000000000000000, 32.34446384429971744, 26.79245525562726016 ) ) ;
#55740=AXIS2_PLACEMENT_3D ( 'NONE', #23778, #64748, #46718 ) ;
#55743=VERTEX_POINT ( 'NONE', #13895 ) ;
#55748=VERTEX_POINT ( 'NONE', #36836 ) ;
#55749=EDGE_CURVE ( 'NONE', #62067, #57334, #18329, .T. ) ;
#55750=EDGE_CURVE ( 'NONE', #19617, #67442, #24454, .T. ) ;
#55758=DIRECTION ( 'NONE',  ( -1.000000000000000000, 0.000000000000000000, 0.000000000000000000 ) ) ;
#55762=EDGE_CURVE ( 'NONE', #61705, #20201, #6792, .T. ) ;
#55765=EDGE_LOOP ( 'NONE', ( #68189, #30269, #34068, #28051 ) ) ;
#55767=AXIS2_PLACEMENT_3D ( 'NONE', #9328, #38282, #25515 ) ;
#55772=DIRECTION ( 'NONE',  ( 0.000000000000000000, -0.3090169943749549453, 0.9510565162951511997 ) ) ;
#55773=CARTESIAN_POINT ( 'NONE',  ( 10.00000000000000000, 37.16516213103285082, -4.992566952384588141 ) ) ;
#55781=AXIS2_PLACEMENT_3D ( 'NONE', #33906, #56849, #38808 ) ;
#55782=DIRECTION ( 'NONE',  ( -1.000000000000000000, -0.000000000000000000, -0.000000000000000000 ) ) ;
#55786=LINE ( 'NONE', #9553, #4818 ) ;
#55808=CARTESIAN_POINT ( 'NONE',  ( 10.00000000000000000, -37.48860685352290290, -0.8828120875904512665 ) ) ;
#55819=CARTESIAN_POINT ( 'NONE',  ( 5.000000000000000000, 36.13751322684419165, 21.40280677340384585 ) ) ;
#55820=ORIENTED_EDGE ( 'NONE', *, *, #15452, .T. ) ;
#55830=DIRECTION ( 'NONE',  ( 1.000000000000000000, -0.000000000000000000, -0.000000000000000000 ) ) ;
#55841=EDGE_CURVE ( 'NONE', #7754, #56288, #68792, .T. ) ;
#55843=CYLINDRICAL_SURFACE ( 'NONE', #72891, 16.00000000000000000 ) ;
#55849=VECTOR ( 'NONE', #44976, 1000.000000000000000 ) ;
#55864=EDGE_LOOP ( 'NONE', ( #69339, #4040, #25347, #47013 ) ) ;
#55877=CARTESIAN_POINT ( 'NONE',  ( -3.000000000000000000, -1.278221433540502217, 26.51162292216071847 ) ) ;
#55886=DIRECTION ( 'NONE',  ( 1.000000000000000000, -0.000000000000000000, -0.000000000000000000 ) ) ;
#55889=VERTEX_POINT ( 'NONE', #44341 ) ;
#55892=CIRCLE ( 'NONE', #7845, 15.99999999999999822 ) ;
#55898=CARTESIAN_POINT ( 'NONE',  ( 0.000000000000000000, 27.75498641678742473, 31.52238457039609187 ) ) ;
#55922=ADVANCED_FACE ( 'NONE', ( #31933 ), #32670, .T. ) ;
#55923=ORIENTED_EDGE ( 'NONE', *, *, #31391, .F. ) ;
#55930=EDGE_CURVE ( 'NONE', #48180, #13600, #4136, .T. ) ;
#55937=VERTEX_POINT ( 'NONE', #21774 ) ;
#55942=ORIENTED_EDGE ( 'NONE', *, *, #64245, .F. ) ;
#55948=ORIENTED_EDGE ( 'NONE', *, *, #73085, .T. ) ;
#55949=EDGE_CURVE ( 'NONE', #36342, #58159, #55984, .T. ) ;
#55958=CYLINDRICAL_SURFACE ( 'NONE', #36470, 42.00000000000000000 ) ;
#55965=CIRCLE ( 'NONE', #59565, 16.00000000000000000 ) ;
#55968=EDGE_LOOP ( 'NONE', ( #55118, #62035, #45518, #20986 ) ) ;
#55970=CARTESIAN_POINT ( 'NONE',  ( 10.00000000000000000, -35.95386929396248377, -10.96151621346525751 ) ) ;
#55976=DIRECTION ( 'NONE',  ( -0.000000000000000000, -0.3090169943749448977, -0.9510565162951543083 ) ) ;
#55981=CYLINDRICAL_SURFACE ( 'NONE', #7592, 16.00000000000000000 ) ;
#55984=LINE ( 'NONE', #44723, #72417 ) ;
#55985=LINE ( 'NONE', #16508, #21211 ) ;
#55990=FACE_OUTER_BOUND ( 'NONE', #16351, .T. ) ;
#56002=AXIS2_PLACEMENT_3D ( 'NONE', #57846, #3676, #59687 ) ;
#56007=PLANE ( 'NONE',  #25774 ) ;
#56014=ORIENTED_EDGE ( 'NONE', *, *, #57295, .F. ) ;
#56023=CYLINDRICAL_SURFACE ( 'NONE', #70503, 16.00000000000000000 ) ;
#56040=AXIS2_PLACEMENT_3D ( 'NONE', #22196, #31976, #27448 ) ;
#56045=PLANE ( 'NONE',  #72606 ) ;
#56049=ORIENTED_EDGE ( 'NONE', *, *, #53498, .F. ) ;
#56059=LINE ( 'NONE', #44791, #5932 ) ;
#56074=CARTESIAN_POINT ( 'NONE',  ( 10.00000000000000000, 0.000000000000000000, 0.000000000000000000 ) ) ;
#56084=LINE ( 'NONE', #9475, #10553 ) ;
#56090=EDGE_CURVE ( 'NONE', #11281, #64952, #11192, .T. ) ;
#56091=CYLINDRICAL_SURFACE ( 'NONE', #66505, 42.00000000000000000 ) ;
#56096=CARTESIAN_POINT ( 'NONE',  ( -3.000000000000000000, -22.32062822937489344, 14.36278369418800160 ) ) ;
#56103=AXIS2_PLACEMENT_3D ( 'NONE', #57187, #35364, #69203 ) ;
#56118=CARTESIAN_POINT ( 'NONE',  ( 0.000000000000000000, 30.84782396557217865, 21.32104025579125306 ) ) ;
#56121=ORIENTED_EDGE ( 'NONE', *, *, #68432, .F. ) ;
#56135=ORIENTED_EDGE ( 'NONE', *, *, #9693, .T. ) ;
#56143=LINE ( 'NONE', #67797, #19047 ) ;
#56150=DIRECTION ( 'NONE',  ( -1.000000000000000000, 0.000000000000000000, 0.000000000000000000 ) ) ;
#56152=CARTESIAN_POINT ( 'NONE',  ( -3.000000000000000000, 0.000000000000000000, 0.000000000000000000 ) ) ;
#56162=AXIS2_PLACEMENT_3D ( 'NONE', #60631, #3133, #14744 ) ;
#56164=CARTESIAN_POINT ( 'NONE',  ( 0.000000000000000000, 0.000000000000000000, 0.000000000000000000 ) ) ;
#56168=FACE_OUTER_BOUND ( 'NONE', #53737, .T. ) ;
#56179=CARTESIAN_POINT ( 'NONE',  ( 0.000000000000000000, 0.000000000000000000, 0.000000000000000000 ) ) ;
#56187=AXIS2_PLACEMENT_3D ( 'NONE', #72993, #44455, #57596 ) ;
#56198=VERTEX_POINT ( 'NONE', #58961 ) ;
#56201=VERTEX_POINT ( 'NONE', #30365 ) ;
#56204=EDGE_CURVE ( 'NONE', #39671, #44028, #59228, .T. ) ;
#56214=ORIENTED_EDGE ( 'NONE', *, *, #47858, .F. ) ;
#56224=EDGE_CURVE ( 'NONE', #74280, #16188, #7815, .T. ) ;
#56227=ORIENTED_EDGE ( 'NONE', *, *, #32810, .T. ) ;
#56247=LINE ( 'NONE', #51333, #40617 ) ;
#56276=FACE_OUTER_BOUND ( 'NONE', #13647, .T. ) ;
#56288=VERTEX_POINT ( 'NONE', #4415 ) ;
#56292=EDGE_CURVE ( 'NONE', #18301, #16255, #67595, .T. ) ;
#56308=DIRECTION ( 'NONE',  ( -1.000000000000000000, 0.000000000000000000, 0.000000000000000000 ) ) ;
#56319=ORIENTED_EDGE ( 'NONE', *, *, #41866, .T. ) ;
#56321=CIRCLE ( 'NONE', #13100, 37.49900000000000233 ) ;
#56328=VERTEX_POINT ( 'NONE', #54417 ) ;
#56354=CYLINDRICAL_SURFACE ( 'NONE', #34758, 15.99999999999999645 ) ;
#56367=CARTESIAN_POINT ( 'NONE',  ( -3.000000000000000000, 24.81905959214261514, 9.408202855044825341 ) ) ;
#56369=FACE_OUTER_BOUND ( 'NONE', #42161, .T. ) ;
#56388=DIRECTION ( 'NONE',  ( -1.000000000000000000, -0.000000000000000000, -0.000000000000000000 ) ) ;
#56396=EDGE_CURVE ( 'NONE', #8203, #29480, #68889, .T. ) ;
#56398=AXIS2_PLACEMENT_3D ( 'NONE', #35170, #41186, #64127 ) ;
#56403=AXIS2_PLACEMENT_3D ( 'NONE', #5177, #46128, #17182 ) ;
#56406=DIRECTION ( 'NONE',  ( 0.000000000000000000, 0.000000000000000000, 1.000000000000000000 ) ) ;
#56425=ORIENTED_EDGE ( 'NONE', *, *, #23878, .T. ) ;
#56426=ORIENTED_EDGE ( 'NONE', *, *, #9485, .F. ) ;
#56428=DIRECTION ( 'NONE',  ( 0.000000000000000000, 0.4999999999999920064, 0.8660254037844432595 ) ) ;
#56429=ORIENTED_EDGE ( 'NONE', *, *, #40841, .F. ) ;
#56440=ADVANCED_FACE ( 'NONE', ( #16799 ), #11876, .F. ) ;
#56457=AXIS2_PLACEMENT_3D ( 'NONE', #27952, #68568, #16683 ) ;
#56462=CARTESIAN_POINT ( 'NONE',  ( 10.00000000000000000, 0.000000000000000000, 0.000000000000000000 ) ) ;
#56463=DIRECTION ( 'NONE',  ( -0.000000000000000000, 0.7431448254773946882, -0.6691306063588577935 ) ) ;
#56465=CARTESIAN_POINT ( 'NONE',  ( 0.000000000000000000, 0.000000000000000000, 0.000000000000000000 ) ) ;
#56470=AXIS2_PLACEMENT_3D ( 'NONE', #53323, #47320, #70590 ) ;
#56481=DIRECTION ( 'NONE',  ( 0.000000000000000000, 0.000000000000000000, 1.000000000000000000 ) ) ;
#56490=ORIENTED_EDGE ( 'NONE', *, *, #47032, .F. ) ;
#56495=DIRECTION ( 'NONE',  ( 0.000000000000000000, -0.4999999999999912847, -0.8660254037844435926 ) ) ;
#56509=DIRECTION ( 'NONE',  ( 0.000000000000000000, 0.3090169943749411230, 0.9510565162951555296 ) ) ;
#56511=ORIENTED_EDGE ( 'NONE', *, *, #17925, .T. ) ;
#56518=VERTEX_POINT ( 'NONE', #69043 ) ;
#56526=CARTESIAN_POINT ( 'NONE',  ( 10.00000000000000000, -37.22597642581153821, 10.79786254984320415 ) ) ;
#56548=VECTOR ( 'NONE', #13714, 1000.000000000000114 ) ;
#56551=ORIENTED_EDGE ( 'NONE', *, *, #73309, .F. ) ;
#56553=DIRECTION ( 'NONE',  ( -1.000000000000000000, 0.000000000000000000, -0.000000000000000000 ) ) ;
#56557=APPLICATION_CONTEXT ( 'automotive_design' ) ;
#56561=EDGE_CURVE ( 'NONE', #34086, #7754, #47259, .T. ) ;
#56568=CIRCLE ( 'NONE', #18121, 16.00000000000000000 ) ;
#56579=ORIENTED_EDGE ( 'NONE', *, *, #10954, .T. ) ;
#56588=CARTESIAN_POINT ( 'NONE',  ( -3.000000000000000000, -10.45096189432344147, 21.10159698893426494 ) ) ;
#56591=CIRCLE ( 'NONE', #20513, 37.49900000000001654 ) ;
#56597=ORIENTED_EDGE ( 'NONE', *, *, #12038, .T. ) ;
#56608=ORIENTED_EDGE ( 'NONE', *, *, #28508, .F. ) ;
#56622=ORIENTED_EDGE ( 'NONE', *, *, #12537, .F. ) ;
#56627=VECTOR ( 'NONE', #31578, 1000.000000000000000 ) ;
#56632=CARTESIAN_POINT ( 'NONE',  ( -3.000000000000000000, 0.000000000000000000, 0.000000000000000000 ) ) ;
#56633=DIRECTION ( 'NONE',  ( -1.000000000000000000, -0.000000000000000000, 0.000000000000000000 ) ) ;
#56639=DIRECTION ( 'NONE',  ( 1.000000000000000000, 0.000000000000000000, 0.000000000000000000 ) ) ;
#56649=FACE_OUTER_BOUND ( 'NONE', #22007, .T. ) ;
#56650=EDGE_CURVE ( 'NONE', #53734, #12406, #71226, .T. ) ;
#56675=LINE ( 'NONE', #57399, #33865 ) ;
#56676=EDGE_LOOP ( 'NONE', ( #12107, #41894, #19135, #19654 ) ) ;
#56679=CYLINDRICAL_SURFACE ( 'NONE', #8396, 16.00000000000000000 ) ;
#56682=VERTEX_POINT ( 'NONE', #20395 ) ;
#56685=CARTESIAN_POINT ( 'NONE',  ( -3.000000000000000000, 0.000000000000000000, 0.000000000000000000 ) ) ;
#56692=AXIS2_PLACEMENT_3D ( 'NONE', #19165, #54494, #2295 ) ;
#56694=EDGE_CURVE ( 'NONE', #39132, #55889, #4974, .T. ) ;
#56697=ORIENTED_EDGE ( 'NONE', *, *, #8397, .T. ) ;
#56704=CARTESIAN_POINT ( 'NONE',  ( 50.00005079999999680, 0.000000000000000000, 0.000000000000000000 ) ) ;
#56709=FACE_OUTER_BOUND ( 'NONE', #2264, .T. ) ;
#56713=ORIENTED_EDGE ( 'NONE', *, *, #40653, .F. ) ;
#56724=CARTESIAN_POINT ( 'NONE',  ( 0.000000000000000000, 0.000000000000000000, 0.000000000000000000 ) ) ;
#56733=ORIENTED_EDGE ( 'NONE', *, *, #22929, .T. ) ;
#56740=CYLINDRICAL_SURFACE ( 'NONE', #32034, 16.00000000000000000 ) ;
#56763=DIRECTION ( 'NONE',  ( 0.000000000000000000, 0.000000000000000000, 1.000000000000000000 ) ) ;
#56787=DIRECTION ( 'NONE',  ( 0.000000000000000000, 0.000000000000000000, 1.000000000000000000 ) ) ;
#56794=EDGE_CURVE ( 'NONE', #46417, #44028, #15484, .T. ) ;
#56801=ORIENTED_EDGE ( 'NONE', *, *, #5064, .T. ) ;
#56822=DIRECTION ( 'NONE',  ( -1.000000000000000000, -0.000000000000000000, -0.000000000000000000 ) ) ;
#56833=CARTESIAN_POINT ( 'NONE',  ( 0.000000000000000000, 39.04073710021366139, -15.48615015657542315 ) ) ;
#56849=DIRECTION ( 'NONE',  ( 1.000000000000000000, 0.000000000000000000, 0.000000000000000000 ) ) ;
#56851=VECTOR ( 'NONE', #39015, 1000.000000000000000 ) ;
#56859=FACE_OUTER_BOUND ( 'NONE', #10993, .T. ) ;
#56877=ADVANCED_FACE ( 'NONE', ( #33137 ), #11684, .F. ) ;
#56884=VERTEX_POINT ( 'NONE', #57943 ) ;
#56903=AXIS2_PLACEMENT_3D ( 'NONE', #58731, #54565, #2732 ) ;
#56913=DIRECTION ( 'NONE',  ( 0.000000000000000000, 0.000000000000000000, -1.000000000000000000 ) ) ;
#56914=FACE_OUTER_BOUND ( 'NONE', #29894, .T. ) ;
#56918=ORIENTED_EDGE ( 'NONE', *, *, #47630, .F. ) ;
#56932=CIRCLE ( 'NONE', #24491, 16.00000000000000000 ) ;
#56934=DIRECTION ( 'NONE',  ( 0.000000000000000000, 0.000000000000000000, 1.000000000000000000 ) ) ;
#56940=EDGE_CURVE ( 'NONE', #3129, #28069, #43727, .T. ) ;
#56966=LINE ( 'NONE', #73492, #23213 ) ;
#56982=VECTOR ( 'NONE', #67738, 1000.000000000000000 ) ;
#57001=CARTESIAN_POINT ( 'NONE',  ( 0.000000000000000000, -3.925862922255855647, -41.81611651403866858 ) ) ;
#57032=ADVANCED_FACE ( 'NONE', ( #62866 ), #63224, .T. ) ;
#57033=DIRECTION ( 'NONE',  ( 1.000000000000000000, -0.000000000000000000, 0.000000000000000000 ) ) ;
#57044=EDGE_CURVE ( 'NONE', #54476, #40343, #30458, .T. ) ;
#57048=VERTEX_POINT ( 'NONE', #30827 ) ;
#57054=LINE ( 'NONE', #38645, #71162 ) ;
#57072=ORIENTED_EDGE ( 'NONE', *, *, #2745, .T. ) ;
#57074=ORIENTED_EDGE ( 'NONE', *, *, #33861, .T. ) ;
#57085=DIRECTION ( 'NONE',  ( -1.000000000000000000, -0.000000000000000000, -0.000000000000000000 ) ) ;
#57095=DIRECTION ( 'NONE',  ( -1.000000000000000000, -0.000000000000000000, -0.000000000000000000 ) ) ;
#57100=VERTEX_POINT ( 'NONE', #54516 ) ;
#57107=CIRCLE ( 'NONE', #69126, 16.00000000000000000 ) ;
#57109=CIRCLE ( 'NONE', #19886, 16.00000000000000000 ) ;
#57110=CYLINDRICAL_SURFACE ( 'NONE', #60160, 37.49900000000000233 ) ;
#57120=EDGE_CURVE ( 'NONE', #55748, #23136, #64125, .T. ) ;
#57131=CARTESIAN_POINT ( 'NONE',  ( 10.00000000000000000, 38.55633173627034438, -16.65560815589369881 ) ) ;
#57142=AXIS2_PLACEMENT_3D ( 'NONE', #3944, #31740, #2847 ) ;
#57143=ADVANCED_FACE ( 'NONE', ( #25935 ), #19552, .F. ) ;
#57159=ORIENTED_EDGE ( 'NONE', *, *, #1906, .T. ) ;
#57184=ORIENTED_EDGE ( 'NONE', *, *, #62568, .F. ) ;
#57187=CARTESIAN_POINT ( 'NONE',  ( -10.00000000000000000, 0.000000000000000000, 0.000000000000000000 ) ) ;
#57194=DIRECTION ( 'NONE',  ( -1.000000000000000000, 0.000000000000000000, 0.000000000000000000 ) ) ;
#57200=AXIS2_PLACEMENT_3D ( 'NONE', #48850, #19902, #42853 ) ;
#57217=CARTESIAN_POINT ( 'NONE',  ( 0.000000000000000000, 2.571758278209441661E-15, -21.00000000000000000 ) ) ;
#57218=CARTESIAN_POINT ( 'NONE',  ( 10.00000000000000000, 2.663952781846149254, 41.91543099594818500 ) ) ;
#57225=VERTEX_POINT ( 'NONE', #32677 ) ;
#57229=ORIENTED_EDGE ( 'NONE', *, *, #69857, .F. ) ;
#57236=EDGE_CURVE ( 'NONE', #21580, #59943, #50902, .T. ) ;
#57243=DIRECTION ( 'NONE',  ( 1.000000000000000000, -0.000000000000000000, -0.000000000000000000 ) ) ;
#57258=CARTESIAN_POINT ( 'NONE',  ( 0.000000000000000000, 27.75498641678786527, -31.52238457039571173 ) ) ;
#57287=ORIENTED_EDGE ( 'NONE', *, *, #8125, .F. ) ;
#57295=EDGE_CURVE ( 'NONE', #36593, #51805, #35345, .T. ) ;
#57306=VERTEX_POINT ( 'NONE', #10131 ) ;
#57318=DIRECTION ( 'NONE',  ( 0.000000000000000000, -0.000000000000000000, 1.000000000000000000 ) ) ;
#57320=DIRECTION ( 'NONE',  ( -1.000000000000000000, 0.000000000000000000, -0.000000000000000000 ) ) ;
#57323=ORIENTED_EDGE ( 'NONE', *, *, #55454, .F. ) ;
#57330=VECTOR ( 'NONE', #71306, 1000.000000000000000 ) ;
#57334=VERTEX_POINT ( 'NONE', #69144 ) ;
#57335=EDGE_LOOP ( 'NONE', ( #70745, #69405, #6250, #65393 ) ) ;
#57363=LINE ( 'NONE', #57741, #58969 ) ;
#57374=CARTESIAN_POINT ( 'NONE',  ( 0.000000000000000000, 0.000000000000000000, 0.000000000000000000 ) ) ;
#57381=DIRECTION ( 'NONE',  ( -1.000000000000000000, -0.000000000000000000, 0.000000000000000000 ) ) ;
#57395=CARTESIAN_POINT ( 'NONE',  ( 10.00000000000000000, 35.47612816024556537, -22.48208911017461631 ) ) ;
#57399=CARTESIAN_POINT ( 'NONE',  ( -3.000000000000000000, -18.13022148937243472, -15.02647892043568767 ) ) ;
#57447=AXIS2_PLACEMENT_3D ( 'NONE', #58124, #53972, #58488 ) ;
#57461=DIRECTION ( 'NONE',  ( -1.000000000000000000, 0.000000000000000000, 0.000000000000000000 ) ) ;
#57463=EDGE_LOOP ( 'NONE', ( #41348, #24550, #52577, #47536 ) ) ;
#57474=CARTESIAN_POINT ( 'NONE',  ( 5.000000000000000000, 2.663952781846149254, 41.91543099594818500 ) ) ;
#57479=CIRCLE ( 'NONE', #20260, 42.00000000000000000 ) ;
#57489=LINE ( 'NONE', #6006, #68340 ) ;
#57497=CARTESIAN_POINT ( 'NONE',  ( 0.000000000000000000, 0.000000000000000000, 0.000000000000000000 ) ) ;
#57502=DIRECTION ( 'NONE',  ( 0.000000000000000000, 0.000000000000000000, -1.000000000000000000 ) ) ;
#57510=ORIENTED_EDGE ( 'NONE', *, *, #1398, .F. ) ;
#57515=AXIS2_PLACEMENT_3D ( 'NONE', #4044, #38981, #61917 ) ;
#57535=ORIENTED_EDGE ( 'NONE', *, *, #19286, .F. ) ;
#57557=FACE_OUTER_BOUND ( 'NONE', #37658, .T. ) ;
#57562=CIRCLE ( 'NONE', #10752, 16.00000000000000000 ) ;
#57574=EDGE_CURVE ( 'NONE', #13600, #11350, #55729, .T. ) ;
#57589=AXIS2_PLACEMENT_3D ( 'NONE', #6369, #73284, #68415 ) ;
#57591=EDGE_CURVE ( 'NONE', #59274, #41967, #38938, .T. ) ;
#57594=CARTESIAN_POINT ( 'NONE',  ( 0.000000000000000000, 0.000000000000000000, 0.000000000000000000 ) ) ;
#57595=CARTESIAN_POINT ( 'NONE',  ( -10.00000000000000000, 0.000000000000000000, 0.000000000000000000 ) ) ;
#57596=DIRECTION ( 'NONE',  ( 0.000000000000000000, 0.000000000000000000, 1.000000000000000000 ) ) ;
#57604=AXIS2_PLACEMENT_3D ( 'NONE', #35705, #58652, #7153 ) ;
#57606=CARTESIAN_POINT ( 'NONE',  ( 10.00000000000000000, 35.53030884539102630, -12.26510123303222599 ) ) ;
#57614=CARTESIAN_POINT ( 'NONE',  ( 5.000000000000000000, -31.52238457039579345, -27.75498641678775158 ) ) ;
#57621=ORIENTED_EDGE ( 'NONE', *, *, #47480, .T. ) ;
#57653=DIRECTION ( 'NONE',  ( 1.000000000000000000, 0.000000000000000000, 0.000000000000000000 ) ) ;
#57662=DIRECTION ( 'NONE',  ( -0.000000000000000000, -0.8660254037844427044, 0.4999999999999929501 ) ) ;
#57675=CARTESIAN_POINT ( 'NONE',  ( 10.00000000000000000, 6.736453364084091788, -36.88895765772625879 ) ) ;
#57688=DIRECTION ( 'NONE',  ( -1.000000000000000000, 0.000000000000000000, 0.000000000000000000 ) ) ;
#57698=ORIENTED_EDGE ( 'NONE', *, *, #28477, .T. ) ;
#57701=ORIENTED_EDGE ( 'NONE', *, *, #11683, .T. ) ;
#57708=ORIENTED_EDGE ( 'NONE', *, *, #68176, .T. ) ;
#57712=VERTEX_POINT ( 'NONE', #6909 ) ;
#57733=ORIENTED_EDGE ( 'NONE', *, *, #13332, .F. ) ;
#57735=DIRECTION ( 'NONE',  ( 0.000000000000000000, 0.000000000000000000, 1.000000000000000000 ) ) ;
#57741=CARTESIAN_POINT ( 'NONE',  ( -3.000000000000000000, 23.50000000000000000, 1.499999999999997780 ) ) ;
#57746=EDGE_CURVE ( 'NONE', #16255, #31252, #28193, .T. ) ;
#57749=CARTESIAN_POINT ( 'NONE',  ( 10.00000000000000000, -10.41901085202050403, -40.68715046381940681 ) ) ;
#57753=FACE_OUTER_BOUND ( 'NONE', #34587, .T. ) ;
#57759=DIRECTION ( 'NONE',  ( -1.000000000000000000, 0.000000000000000000, 0.000000000000000000 ) ) ;
#57770=DIRECTION ( 'NONE',  ( -1.000000000000000000, -0.000000000000000000, 0.000000000000000000 ) ) ;
#57795=DIRECTION ( 'NONE',  ( 0.000000000000000000, 0.000000000000000000, -1.000000000000000000 ) ) ;
#57802=DIRECTION ( 'NONE',  ( 1.000000000000000000, 0.000000000000000000, 0.000000000000000000 ) ) ;
#57834=VECTOR ( 'NONE', #23891, 1000.000000000000000 ) ;
#57835=ORIENTED_EDGE ( 'NONE', *, *, #57120, .T. ) ;
#57846=CARTESIAN_POINT ( 'NONE',  ( -3.000000000000000000, 8.688484142253939169, 21.88630264137371029 ) ) ;
#57847=CIRCLE ( 'NONE', #51871, 42.00000000000000000 ) ;
#57848=LINE ( 'NONE', #56367, #48164 ) ;
#57857=DIRECTION ( 'NONE',  ( -1.000000000000000000, -0.000000000000000000, 0.000000000000000000 ) ) ;
#57866=CYLINDRICAL_SURFACE ( 'NONE', #29902, 16.00000000000000000 ) ;
#57908=ORIENTED_EDGE ( 'NONE', *, *, #5012, .F. ) ;
#57912=ORIENTED_EDGE ( 'NONE', *, *, #38907, .F. ) ;
#57919=DIRECTION ( 'NONE',  ( 0.000000000000000000, 0.000000000000000000, 1.000000000000000000 ) ) ;
#57925=LINE ( 'NONE', #64307, #21792 ) ;
#57943=CARTESIAN_POINT ( 'NONE',  ( 10.00000000000000000, -33.80338159004296017, 16.23288003029484727 ) ) ;
#57945=CYLINDRICAL_SURFACE ( 'NONE', #58674, 42.00000000000000000 ) ;
#57959=CARTESIAN_POINT ( 'NONE',  ( 10.00000000000000000, 0.000000000000000000, 0.000000000000000000 ) ) ;
#57961=FACE_OUTER_BOUND ( 'NONE', #3662, .T. ) ;
#57966=DIRECTION ( 'NONE',  ( 0.000000000000000000, 0.000000000000000000, -1.000000000000000000 ) ) ;
#57970=DIRECTION ( 'NONE',  ( 0.000000000000000000, 0.000000000000000000, 1.000000000000000000 ) ) ;
#57981=VERTEX_POINT ( 'NONE', #1128 ) ;
#57986=EDGE_LOOP ( 'NONE', ( #36190, #39395, #27912, #61686 ) ) ;
#58007=CARTESIAN_POINT ( 'NONE',  ( 0.000000000000000000, -23.29833615347104825, -3.418703333116803744 ) ) ;
#58009=CARTESIAN_POINT ( 'NONE',  ( -3.000000000000000000, -13.04903810567675038, 19.60159698893425428 ) ) ;
#58010=DIRECTION ( 'NONE',  ( -1.000000000000000000, -0.000000000000000000, -0.000000000000000000 ) ) ;
#58012=CARTESIAN_POINT ( 'NONE',  ( -3.000000000000000000, 16.83928648764923253, 16.46020748918050458 ) ) ;
#58031=CARTESIAN_POINT ( 'NONE',  ( 4.999999999999999112, -40.68715046381937128, 10.41901085202062660 ) ) ;
#58035=AXIS2_PLACEMENT_3D ( 'NONE', #36302, #57770, #12994 ) ;
#58050=LINE ( 'NONE', #58412, #39718 ) ;
#58055=EDGE_CURVE ( 'NONE', #54369, #913, #8984, .T. ) ;
#58059=CARTESIAN_POINT ( 'NONE',  ( 10.00000000000000000, 17.67226234102874116, -33.17418723428288274 ) ) ;
#58062=ORIENTED_EDGE ( 'NONE', *, *, #58458, .T. ) ;
#58073=EDGE_LOOP ( 'NONE', ( #12299, #38916, #54098, #67710 ) ) ;
#58082=CARTESIAN_POINT ( 'NONE',  ( 0.000000000000000000, -22.32062822937489344, 14.36278369418800160 ) ) ;
#58096=VERTEX_POINT ( 'NONE', #70593 ) ;
#58106=VECTOR ( 'NONE', #12800, 1000.000000000000000 ) ;
#58107=DIRECTION ( 'NONE',  ( -1.000000000000000000, 0.000000000000000000, 0.000000000000000000 ) ) ;
#58118=LINE ( 'NONE', #69763, #14018 ) ;
#58119=CARTESIAN_POINT ( 'NONE',  ( 0.000000000000000000, -2.663952781846440576, 41.91543099594817789 ) ) ;
#58124=CARTESIAN_POINT ( 'NONE',  ( 10.00000000000000000, 22.64427369931212297, -30.00120703465181293 ) ) ;
#58144=AXIS2_PLACEMENT_3D ( 'NONE', #68221, #67474, #16718 ) ;
#58153=CARTESIAN_POINT ( 'NONE',  ( 0.000000000000000000, 2.663952781846728790, -41.91543099594814947 ) ) ;
#58159=VERTEX_POINT ( 'NONE', #36764 ) ;
#58174=ORIENTED_EDGE ( 'NONE', *, *, #14364, .F. ) ;
#58181=LINE ( 'NONE', #30340, #32972 ) ;
#58183=ORIENTED_EDGE ( 'NONE', *, *, #66280, .F. ) ;
#58184=LINE ( 'NONE', #34891, #54342 ) ;
#58190=DIRECTION ( 'NONE',  ( -1.000000000000000000, -0.000000000000000000, -0.000000000000000000 ) ) ;
#58192=ORIENTED_EDGE ( 'NONE', *, *, #48893, .F. ) ;
#58197=FACE_OUTER_BOUND ( 'NONE', #6914, .T. ) ;
#58201=CARTESIAN_POINT ( 'NONE',  ( 10.00000000000000000, -4.992566952385247170, 37.16516213103275845 ) ) ;
#58207=DIRECTION ( 'NONE',  ( 0.000000000000000000, 0.000000000000000000, 1.000000000000000000 ) ) ;
#58212=AXIS2_PLACEMENT_3D ( 'NONE', #49903, #21325, #36778 ) ;
#58213=CARTESIAN_POINT ( 'NONE',  ( 10.00000000000000000, 0.000000000000000000, 0.000000000000000000 ) ) ;
#58219=EDGE_CURVE ( 'NONE', #43524, #41055, #30744, .T. ) ;
#58227=DIRECTION ( 'NONE',  ( 0.000000000000000000, -1.000000000000000000, -1.047444401652940007E-14 ) ) ;
#58267=FILL_AREA_STYLE_COLOUR ( '', #19428 ) ;
#58274=AXIS2_PLACEMENT_3D ( 'NONE', #4697, #15206, #21204 ) ;
#58288=LINE ( 'NONE', #42485, #27265 ) ;
#58301=CARTESIAN_POINT ( 'NONE',  ( 10.00000000000000000, -41.91543099594816368, -2.663952781846588014 ) ) ;
#58309=FACE_OUTER_BOUND ( 'NONE', #5139, .T. ) ;
#58323=ORIENTED_EDGE ( 'NONE', *, *, #51789, .T. ) ;
#58334=ORIENTED_EDGE ( 'NONE', *, *, #25456, .F. ) ;
#58339=VERTEX_POINT ( 'NONE', #10416 ) ;
#58340=DIRECTION ( 'NONE',  ( 0.000000000000000000, 0.000000000000000000, 1.000000000000000000 ) ) ;
#58354=DIRECTION ( 'NONE',  ( 0.000000000000000000, 0.000000000000000000, 1.000000000000000000 ) ) ;
#58363=VERTEX_POINT ( 'NONE', #33335 ) ;
#58381=ORIENTED_EDGE ( 'NONE', *, *, #41039, .F. ) ;
#58392=EDGE_CURVE ( 'NONE', #779, #26982, #72809, .T. ) ;
#58395=CIRCLE ( 'NONE', #41589, 37.49900000000000944 ) ;
#58401=EDGE_CURVE ( 'NONE', #19772, #15350, #29417, .T. ) ;
#58408=DIRECTION ( 'NONE',  ( -1.000000000000000000, -0.000000000000000000, 0.000000000000000000 ) ) ;
#58412=CARTESIAN_POINT ( 'NONE',  ( 5.000000000000000000, -39.04073710021356192, 15.48615015657568073 ) ) ;
#58431=DIRECTION ( 'NONE',  ( 0.000000000000000000, 0.000000000000000000, 1.000000000000000000 ) ) ;
#58444=CARTESIAN_POINT ( 'NONE',  ( 0.000000000000000000, -10.96151621346461447, -35.95386929396268272 ) ) ;
#58446=ORIENTED_EDGE ( 'NONE', *, *, #66727, .T. ) ;
#58456=CYLINDRICAL_SURFACE ( 'NONE', #73359, 37.49900000000000233 ) ;
#58458=EDGE_CURVE ( 'NONE', #30220, #6668, #74319, .T. ) ;
#58471=VECTOR ( 'NONE', #53677, 1000.000000000000000 ) ;
#58476=ORIENTED_EDGE ( 'NONE', *, *, #18994, .F. ) ;
#58488=DIRECTION ( 'NONE',  ( 0.000000000000000000, -0.4539904997395352027, -0.8910065241883737830 ) ) ;
#58510=AXIS2_PLACEMENT_3D ( 'NONE', #51535, #46273, #52274 ) ;
#58558=ORIENTED_EDGE ( 'NONE', *, *, #29121, .T. ) ;
#58562=DIRECTION ( 'NONE',  ( 0.000000000000000000, -0.4539904997395351471, -0.8910065241883737830 ) ) ;
#58568=CARTESIAN_POINT ( 'NONE',  ( 0.000000000000000000, -30.84782396557233142, 21.32104025579104345 ) ) ;
#58577=DIRECTION ( 'NONE',  ( 0.000000000000000000, 0.000000000000000000, 1.000000000000000000 ) ) ;
#58584=EDGE_CURVE ( 'NONE', #54986, #11705, #4000, .T. ) ;
#58595=CARTESIAN_POINT ( 'NONE',  ( 0.000000000000000000, 40.98264845739749518, 9.188173127307448951 ) ) ;
#58596=CARTESIAN_POINT ( 'NONE',  ( -3.000000000000000000, 20.85821328998741109, 10.92862929874522315 ) ) ;
#58604=VECTOR ( 'NONE', #67130, 1000.000000000000000 ) ;
#58611=VERTEX_POINT ( 'NONE', #28013 ) ;
#58624=ORIENTED_EDGE ( 'NONE', *, *, #4695, .T. ) ;
#58627=ORIENTED_EDGE ( 'NONE', *, *, #73044, .T. ) ;
#58635=ORIENTED_EDGE ( 'NONE', *, *, #38792, .F. ) ;
#58642=CARTESIAN_POINT ( 'NONE',  ( 10.00000000000000000, -27.13269053701078448, -25.88420570971428702 ) ) ;
#58645=EDGE_CURVE ( 'NONE', #60587, #30754, #39095, .T. ) ;
#58650=LINE ( 'NONE', #30070, #29852 ) ;
#58651=ORIENTED_EDGE ( 'NONE', *, *, #44669, .F. ) ;
#58652=DIRECTION ( 'NONE',  ( 0.000000000000000000, 0.3090169943749450088, 0.9510565162951544194 ) ) ;
#58672=CARTESIAN_POINT ( 'NONE',  ( 10.00000000000000000, -12.26510123303234501, -35.53030884539098366 ) ) ;
#58674=AXIS2_PLACEMENT_3D ( 'NONE', #12073, #28615, #7180 ) ;
#58681=FACE_OUTER_BOUND ( 'NONE', #62371, .T. ) ;
#58682=CARTESIAN_POINT ( 'NONE',  ( -3.000000000000000000, -3.948201729842038432, -23.21447184625298021 ) ) ;
#58684=AXIS2_PLACEMENT_3D ( 'NONE', #49250, #9029, #60907 ) ;
#58690=CARTESIAN_POINT ( 'NONE',  ( 10.00000000000000000, 0.000000000000000000, 0.000000000000000000 ) ) ;
#58694=CARTESIAN_POINT ( 'NONE',  ( 10.00000000000000178, 0.000000000000000000, 0.000000000000000000 ) ) ;
#58707=ORIENTED_EDGE ( 'NONE', *, *, #72738, .T. ) ;
#58724=ORIENTED_EDGE ( 'NONE', *, *, #31062, .T. ) ;
#58731=CARTESIAN_POINT ( 'NONE',  ( 10.00000000000000000, 17.67226234102826510, 33.17418723428314564 ) ) ;
#58755=DIRECTION ( 'NONE',  ( -1.000000000000000000, -0.000000000000000000, 0.000000000000000000 ) ) ;
#58758=FACE_OUTER_BOUND ( 'NONE', #65207, .T. ) ;
#58767=EDGE_CURVE ( 'NONE', #67688, #8512, #51110, .T. ) ;
#58769=DIRECTION ( 'NONE',  ( 1.000000000000000000, 0.000000000000000000, 0.000000000000000000 ) ) ;
#58770=CARTESIAN_POINT ( 'NONE',  ( 0.000000000000000000, 23.50000000000000000, -1.500000000000001332 ) ) ;
#58773=ORIENTED_EDGE ( 'NONE', *, *, #31579, .F. ) ;
#58801=VECTOR ( 'NONE', #29128, 1000.000000000000114 ) ;
#58822=ORIENTED_EDGE ( 'NONE', *, *, #31050, .T. ) ;
#58826=DIRECTION ( 'NONE',  ( -1.000000000000000000, 0.000000000000000000, 0.000000000000000000 ) ) ;
#58840=LINE ( 'NONE', #18965, #36668 ) ;
#58846=ORIENTED_EDGE ( 'NONE', *, *, #48443, .T. ) ;
#58867=DIRECTION ( 'NONE',  ( -1.000000000000000000, 0.000000000000000000, 0.000000000000000000 ) ) ;
#58878=CARTESIAN_POINT ( 'NONE',  ( 10.00000000000000000, -37.16516213103280108, 4.992566952384862589 ) ) ;
#58879=ORIENTED_EDGE ( 'NONE', *, *, #7958, .T. ) ;
#58880=CARTESIAN_POINT ( 'NONE',  ( 0.000000000000000000, -39.04073710021332744, -15.48615015657624028 ) ) ;
#58900=DIRECTION ( 'NONE',  ( -1.000000000000000000, -0.000000000000000000, 0.000000000000000000 ) ) ;
#58907=VECTOR ( 'NONE', #68479, 1000.000000000000000 ) ;
#58912=ORIENTED_EDGE ( 'NONE', *, *, #6291, .T. ) ;
#58913=DIRECTION ( 'NONE',  ( 0.000000000000000000, 0.000000000000000000, -1.000000000000000000 ) ) ;
#58941=ORIENTED_EDGE ( 'NONE', *, *, #28074, .F. ) ;
#58944=DIRECTION ( 'NONE',  ( -1.000000000000000000, 0.000000000000000000, 0.000000000000000000 ) ) ;
#58961=CARTESIAN_POINT ( 'NONE',  ( 10.00000000000000000, 36.88895765772633695, 6.736453364083687667 ) ) ;
#58969=VECTOR ( 'NONE', #69744, 1000.000000000000000 ) ;
#58978=EDGE_CURVE ( 'NONE', #64121, #11255, #54297, .T. ) ;
#58991=ORIENTED_EDGE ( 'NONE', *, *, #29050, .F. ) ;
#59009=ORIENTED_EDGE ( 'NONE', *, *, #32684, .F. ) ;
#59017=ORIENTED_EDGE ( 'NONE', *, *, #29514, .F. ) ;
#59045=CARTESIAN_POINT ( 'NONE',  ( -3.000000000000000000, -1.278221433540145391, -26.51162292216073979 ) ) ;
#59056=CARTESIAN_POINT ( 'NONE',  ( 10.00000000000000000, -0.6853352020787742971, -37.58145647212455032 ) ) ;
#59068=CARTESIAN_POINT ( 'NONE',  ( 0.000000000000000000, 41.91543099594818500, -2.663952781846294915 ) ) ;
#59076=EDGE_CURVE ( 'NONE', #60432, #24766, #53418, .T. ) ;
#59086=ORIENTED_EDGE ( 'NONE', *, *, #58645, .F. ) ;
#59099=ORIENTED_EDGE ( 'NONE', *, *, #72039, .T. ) ;
#59103=ORIENTED_EDGE ( 'NONE', *, *, #10502, .F. ) ;
#59105=CYLINDRICAL_SURFACE ( 'NONE', #56903, 16.00000000000000000 ) ;
#59113=LINE ( 'NONE', #24518, #68522 ) ;
#59119=AXIS2_PLACEMENT_3D ( 'NONE', #32187, #49853, #27287 ) ;
#59121=ORIENTED_EDGE ( 'NONE', *, *, #51648, .T. ) ;
#59122=CARTESIAN_POINT ( 'NONE',  ( 0.000000000000000000, -6.555932627142143865, -37.01155633439065440 ) ) ;
#59145=DIRECTION ( 'NONE',  ( 0.000000000000000000, 0.000000000000000000, 1.000000000000000000 ) ) ;
#59167=ORIENTED_EDGE ( 'NONE', *, *, #69686, .T. ) ;
#59179=EDGE_CURVE ( 'NONE', #43284, #57981, #64223, .T. ) ;
#59181=EDGE_LOOP ( 'NONE', ( #52419, #53069, #25795, #59998 ) ) ;
#59182=EDGE_LOOP ( 'NONE', ( #71763, #72016, #42636, #40018 ) ) ;
#59184=CARTESIAN_POINT ( 'NONE',  ( -10.00000000000000000, 0.000000000000000000, 0.000000000000000000 ) ) ;
#59214=AXIS2_PLACEMENT_3D ( 'NONE', #28637, #73386, #56495 ) ;
#59223=VERTEX_POINT ( 'NONE', #44114 ) ;
#59228=CIRCLE ( 'NONE', #54396, 16.00000000000000000 ) ;
#59232=CARTESIAN_POINT ( 'NONE',  ( 10.00000000000000000, -37.01155633439063308, 6.555932627142289526 ) ) ;
#59236=DIRECTION ( 'NONE',  ( -1.000000000000000000, 0.000000000000000000, 0.000000000000000000 ) ) ;
#59243=DIRECTION ( 'NONE',  ( -1.000000000000000000, 0.000000000000000000, -0.000000000000000000 ) ) ;
#59251=ORIENTED_EDGE ( 'NONE', *, *, #56396, .T. ) ;
#59258=ORIENTED_EDGE ( 'NONE', *, *, #50637, .T. ) ;
#59274=VERTEX_POINT ( 'NONE', #40704 ) ;
#59302=CYLINDRICAL_SURFACE ( 'NONE', #70804, 16.00000000000000000 ) ;
#59306=ORIENTED_EDGE ( 'NONE', *, *, #53570, .F. ) ;
#59307=CARTESIAN_POINT ( 'NONE',  ( 10.00000000000000000, 6.736453364083557105, 36.88895765772635826 ) ) ;
#59320=CYLINDRICAL_SURFACE ( 'NONE', #51692, 37.49900000000000233 ) ;
#59338=VECTOR ( 'NONE', #30989, 1000.000000000000000 ) ;
#59343=EDGE_CURVE ( 'NONE', #11526, #44329, #29361, .T. ) ;
#59358=ORIENTED_EDGE ( 'NONE', *, *, #68693, .T. ) ;
#59363=CIRCLE ( 'NONE', #55767, 16.00000000000000000 ) ;
#59374=EDGE_LOOP ( 'NONE', ( #30914, #19142, #19396, #33653 ) ) ;
#59381=( NAMED_UNIT ( * ) SI_UNIT ( $, .STERADIAN. ) SOLID_ANGLE_UNIT ( ) );
#59410=EDGE_CURVE ( 'NONE', #32352, #32355, #7598, .T. ) ;
#59433=CARTESIAN_POINT ( 'NONE',  ( 0.000000000000000000, 30.80686688397041451, -21.53537804866048688 ) ) ;
#59439=ORIENTED_EDGE ( 'NONE', *, *, #60185, .F. ) ;
#59455=VECTOR ( 'NONE', #33984, 1000.000000000000000 ) ;
#59470=CARTESIAN_POINT ( 'NONE',  ( 10.00000000000000000, -37.58145647212453611, -0.6853352020794456489 ) ) ;
#59471=AXIS2_PLACEMENT_3D ( 'NONE', #31349, #54300, #71569 ) ;
#59493=LINE ( 'NONE', #7984, #59509 ) ;
#59501=EDGE_CURVE ( 'NONE', #60926, #9559, #61806, .T. ) ;
#59506=CYLINDRICAL_SURFACE ( 'NONE', #46603, 16.00000000000000000 ) ;
#59509=VECTOR ( 'NONE', #46365, 1000.000000000000000 ) ;
#59511=ORIENTED_EDGE ( 'NONE', *, *, #41231, .T. ) ;
#59530=DIRECTION ( 'NONE',  ( 0.000000000000000000, 0.000000000000000000, 1.000000000000000000 ) ) ;
#59538=FACE_OUTER_BOUND ( 'NONE', #51402, .T. ) ;
#59546=ORIENTED_EDGE ( 'NONE', *, *, #30115, .F. ) ;
#59565=AXIS2_PLACEMENT_3D ( 'NONE', #37256, #54532, #65822 ) ;
#59586=LINE ( 'NONE', #52838, #4792 ) ;
#59588=ADVANCED_FACE ( 'NONE', ( #3455 ), #56045, .F. ) ;
#59598=AXIS2_PLACEMENT_3D ( 'NONE', #32376, #38030, #60960 ) ;
#59606=CARTESIAN_POINT ( 'NONE',  ( -10.00000000000000000, 0.000000000000000000, 0.000000000000000000 ) ) ;
#59614=AXIS2_PLACEMENT_3D ( 'NONE', #63580, #53393, #47019 ) ;
#59643=ORIENTED_EDGE ( 'NONE', *, *, #66787, .T. ) ;
#59649=VECTOR ( 'NONE', #3247, 1000.000000000000000 ) ;
#59652=AXIS2_PLACEMENT_3D ( 'NONE', #62635, #69001, #28387 ) ;
#59659=DIRECTION ( 'NONE',  ( -1.000000000000000000, 0.000000000000000000, -0.000000000000000000 ) ) ;
#59662=ORIENTED_EDGE ( 'NONE', *, *, #72039, .F. ) ;
#59687=DIRECTION ( 'NONE',  ( 0.000000000000000000, -0.3090169943749449533, -0.9510565162951543083 ) ) ;
#59708=DIRECTION ( 'NONE',  ( 0.000000000000000000, 0.000000000000000000, 1.000000000000000000 ) ) ;
#59744=FACE_OUTER_BOUND ( 'NONE', #6922, .T. ) ;
#59748=CIRCLE ( 'NONE', #66919, 42.00000000000000000 ) ;
#59765=CARTESIAN_POINT ( 'NONE',  ( 0.000000000000000000, 3.925862922256160736, 41.81611651403863306 ) ) ;
#59768=VERTEX_POINT ( 'NONE', #6765 ) ;
#59776=DIRECTION ( 'NONE',  ( 0.000000000000000000, 0.000000000000000000, 1.000000000000000000 ) ) ;
#59779=CIRCLE ( 'NONE', #24994, 37.49900000000000944 ) ;
#59783=VECTOR ( 'NONE', #32882, 1000.000000000000000 ) ;
#59791=DIRECTION ( 'NONE',  ( 0.000000000000000000, -0.1045284632676429099, -0.9945218953682744001 ) ) ;
#59806=CARTESIAN_POINT ( 'NONE',  ( -3.000000000000000000, -22.67460108101774807, -6.353146135318215038 ) ) ;
#59831=EDGE_CURVE ( 'NONE', #13480, #44329, #66425, .T. ) ;
#59835=CARTESIAN_POINT ( 'NONE',  ( 10.00000000000000000, -12.42422080174614862, -35.38097989696524337 ) ) ;
#59836=ORIENTED_EDGE ( 'NONE', *, *, #46257, .T. ) ;
#59838=ORIENTED_EDGE ( 'NONE', *, *, #5700, .F. ) ;
#59875=EDGE_LOOP ( 'NONE', ( #2623, #29217, #25378, #16914 ) ) ;
#59876=AXIS2_PLACEMENT_3D ( 'NONE', #32757, #21863, #44807 ) ;
#59878=CARTESIAN_POINT ( 'NONE',  ( 0.000000000000000000, -37.16516213103280108, 4.992566952384862589 ) ) ;
#59895=CARTESIAN_POINT ( 'NONE',  ( 10.00000000000000000, 0.000000000000000000, 0.000000000000000000 ) ) ;
#59900=CARTESIAN_POINT ( 'NONE',  ( 0.000000000000000000, 0.000000000000000000, 0.000000000000000000 ) ) ;
#59921=EDGE_CURVE ( 'NONE', #69710, #55743, #12765, .T. ) ;
#59942=CARTESIAN_POINT ( 'NONE',  ( 10.00000000000000000, 33.00180498840072829, -17.80606268964504935 ) ) ;
#59943=VERTEX_POINT ( 'NONE', #33675 ) ;
#59948=DIRECTION ( 'NONE',  ( 1.000000000000000000, 0.000000000000000000, 0.000000000000000000 ) ) ;
#59966=DIRECTION ( 'NONE',  ( 0.000000000000000000, 0.000000000000000000, 1.000000000000000000 ) ) ;
#59982=AXIS2_PLACEMENT_3D ( 'NONE', #24528, #48572, #42939 ) ;
#59998=ORIENTED_EDGE ( 'NONE', *, *, #28612, .F. ) ;
#59999=DIRECTION ( 'NONE',  ( 1.000000000000000000, -0.000000000000000000, -0.000000000000000000 ) ) ;
#60023=EDGE_CURVE ( 'NONE', #57334, #63672, #55892, .T. ) ;
#60029=ORIENTED_EDGE ( 'NONE', *, *, #7418, .F. ) ;
#60037=FACE_OUTER_BOUND ( 'NONE', #49267, .T. ) ;
#60042=DIRECTION ( 'NONE',  ( 1.000000000000000000, 0.000000000000000000, 0.000000000000000000 ) ) ;
#60102=AXIS2_PLACEMENT_3D ( 'NONE', #68404, #73275, #51095 ) ;
#60105=EDGE_CURVE ( 'NONE', #28069, #8551, #18240, .T. ) ;
#60130=EDGE_CURVE ( 'NONE', #57334, #32561, #58840, .T. ) ;
#60131=CARTESIAN_POINT ( 'NONE',  ( 10.00000000000000000, 27.13269053701132094, -25.88420570971372570 ) ) ;
#60133=VERTEX_POINT ( 'NONE', #64478 ) ;
#60136=ORIENTED_EDGE ( 'NONE', *, *, #73058, .T. ) ;
#60140=ORIENTED_EDGE ( 'NONE', *, *, #56292, .T. ) ;
#60146=DIRECTION ( 'NONE',  ( 0.000000000000000000, -0.7071067811865389130, -0.7071067811865561215 ) ) ;
#60159=DIRECTION ( 'NONE',  ( 0.000000000000000000, 0.4067366430757887730, 0.9135454576426059736 ) ) ;
#60160=AXIS2_PLACEMENT_3D ( 'NONE', #63492, #33402, #40928 ) ;
#60164=DIRECTION ( 'NONE',  ( 0.000000000000000000, 0.000000000000000000, 1.000000000000000000 ) ) ;
#60166=CYLINDRICAL_SURFACE ( 'NONE', #63962, 16.00000000000000000 ) ;
#60169=CARTESIAN_POINT ( 'NONE',  ( 10.00000000000000000, -0.8828120875898013420, -37.48860685352291711 ) ) ;
#60172=DIRECTION ( 'NONE',  ( -1.000000000000000000, -0.000000000000000000, -0.000000000000000000 ) ) ;
#60185=EDGE_CURVE ( 'NONE', #59223, #12564, #42687, .T. ) ;
#60188=CARTESIAN_POINT ( 'NONE',  ( 0.000000000000000000, 0.000000000000000000, 0.000000000000000000 ) ) ;
#60189=CARTESIAN_POINT ( 'NONE',  ( 4.999999999999999112, -41.91543099594819921, 2.663952781846001816 ) ) ;
#60214=DIRECTION ( 'NONE',  ( 0.000000000000000000, -0.8910065241883722287, 0.4539904997395382558 ) ) ;
#60219=ORIENTED_EDGE ( 'NONE', *, *, #41039, .T. ) ;
#60225=ORIENTED_EDGE ( 'NONE', *, *, #59410, .F. ) ;
#60227=CARTESIAN_POINT ( 'NONE',  ( 0.000000000000000000, -12.42422080174663712, 35.38097989696507994 ) ) ;
#60229=ORIENTED_EDGE ( 'NONE', *, *, #30538, .F. ) ;
#60233=ORIENTED_EDGE ( 'NONE', *, *, #25779, .F. ) ;
#60235=FACE_OUTER_BOUND ( 'NONE', #39979, .T. ) ;
#60244=PLANE ( 'NONE',  #69149 ) ;
#60266=VECTOR ( 'NONE', #12303, 1000.000000000000000 ) ;
#60267=DIRECTION ( 'NONE',  ( 0.000000000000000000, 0.8090169943749447867, 0.5877852522924769119 ) ) ;
#60312=ORIENTED_EDGE ( 'NONE', *, *, #35419, .T. ) ;
#60320=CARTESIAN_POINT ( 'NONE',  ( 5.000000000000000000, 39.04073710021344112, 15.48615015657596850 ) ) ;
#60337=VERTEX_POINT ( 'NONE', #2099 ) ;
#60338=VERTEX_POINT ( 'NONE', #26090 ) ;
#60339=CARTESIAN_POINT ( 'NONE',  ( 4.999999999999999112, -9.188173127307592836, 40.98264845739746676 ) ) ;
#60356=CARTESIAN_POINT ( 'NONE',  ( -3.000000000000000000, -25.60904388321925396, 6.976881207771172377 ) ) ;
#60358=DIRECTION ( 'NONE',  ( 0.000000000000000000, -0.8660254037844427044, 0.4999999999999929501 ) ) ;
#60375=EDGE_CURVE ( 'NONE', #7056, #64121, #14814, .T. ) ;
#60379=CARTESIAN_POINT ( 'NONE',  ( 10.00000000000000000, -21.53537804866058991, -30.80686688397033635 ) ) ;
#60382=ORIENTED_EDGE ( 'NONE', *, *, #68495, .T. ) ;
#60385=EDGE_CURVE ( 'NONE', #13857, #21232, #67056, .T. ) ;
#60425=ORIENTED_EDGE ( 'NONE', *, *, #2176, .F. ) ;
#60432=VERTEX_POINT ( 'NONE', #73052 ) ;
#60436=LINE ( 'NONE', #25473, #55146 ) ;
#60452=ORIENTED_EDGE ( 'NONE', *, *, #65058, .F. ) ;
#60454=CARTESIAN_POINT ( 'NONE',  ( 0.000000000000000000, 0.000000000000000000, 0.000000000000000000 ) ) ;
#60455=CIRCLE ( 'NONE', #40006, 16.00000000000000711 ) ;
#60467=EDGE_CURVE ( 'NONE', #67018, #20918, #34358, .T. ) ;
#60477=CARTESIAN_POINT ( 'NONE',  ( 10.00000000000000000, -39.04073710021333454, -15.48615015657624738 ) ) ;
#60506=ORIENTED_EDGE ( 'NONE', *, *, #21384, .T. ) ;
#60525=AXIS2_PLACEMENT_3D ( 'NONE', #28613, #29349, #51554 ) ;
#60533=CARTESIAN_POINT ( 'NONE',  ( 10.00000000000000000, 5.202137450156389953, 37.22597642581160216 ) ) ;
#60538=VECTOR ( 'NONE', #15167, 1000.000000000000000 ) ;
#60539=CARTESIAN_POINT ( 'NONE',  ( 10.00000000000000000, -16.45098606841149902, 33.79645857604508308 ) ) ;
#60540=CARTESIAN_POINT ( 'NONE',  ( -3.000000000000000000, -10.45096189432344147, 21.10159698893426494 ) ) ;
#60544=EDGE_CURVE ( 'NONE', #19238, #26842, #53577, .T. ) ;
#60556=VERTEX_POINT ( 'NONE', #64029 ) ;
#60567=ORIENTED_EDGE ( 'NONE', *, *, #12659, .T. ) ;
#60569=DIRECTION ( 'NONE',  ( 0.000000000000000000, 0.9510565162951544194, -0.3090169943749447867 ) ) ;
#60577=DIRECTION ( 'NONE',  ( 0.000000000000000000, 0.000000000000000000, 1.000000000000000000 ) ) ;
#60587=VERTEX_POINT ( 'NONE', #12866 ) ;
#60594=ORIENTED_EDGE ( 'NONE', *, *, #71898, .T. ) ;
#60609=EDGE_CURVE ( 'NONE', #68659, #67909, #33115, .T. ) ;
#60616=CARTESIAN_POINT ( 'NONE',  ( 10.00000000000000000, 40.68715046381944234, -10.41901085202036192 ) ) ;
#60628=DIRECTION ( 'NONE',  ( 1.000000000000000000, -0.000000000000000000, -0.000000000000000000 ) ) ;
#60631=CARTESIAN_POINT ( 'NONE',  ( 10.00000000000000000, 0.000000000000000000, 0.000000000000000000 ) ) ;
#60637=ADVANCED_FACE ( 'NONE', ( #533 ), #47105, .T. ) ;
#60640=CARTESIAN_POINT ( 'NONE',  ( 0.000000000000000000, -40.98264845739755202, 9.188173127307159405 ) ) ;
#60646=VECTOR ( 'NONE', #67082, 999.9999999999998863 ) ;
#60667=AXIS2_PLACEMENT_3D ( 'NONE', #9875, #61011, #15889 ) ;
#60671=ORIENTED_EDGE ( 'NONE', *, *, #16193, .F. ) ;
#60678=CARTESIAN_POINT ( 'NONE',  ( -3.000000000000000000, 8.688484142253939169, 21.88630264137371029 ) ) ;
#60682=EDGE_CURVE ( 'NONE', #14108, #66145, #12722, .T. ) ;
#60683=AXIS2_PLACEMENT_3D ( 'NONE', #12335, #24002, #41288 ) ;
#60695=CARTESIAN_POINT ( 'NONE',  ( -3.000000000000000000, 9.615535125378775305, 24.73947219025917121 ) ) ;
#60711=CARTESIAN_POINT ( 'NONE',  ( 5.000000000000000000, 22.48208911017500355, 35.47612816024530957 ) ) ;
#60764=DIRECTION ( 'NONE',  ( -1.000000000000000000, -0.000000000000000000, 0.000000000000000000 ) ) ;
#60777=AXIS2_PLACEMENT_3D ( 'NONE', #6870, #11751, #18149 ) ;
#60784=ORIENTED_EDGE ( 'NONE', *, *, #5359, .T. ) ;
#60791=CARTESIAN_POINT ( 'NONE',  ( -3.000000000000000000, 16.83928648764923253, 16.46020748918050458 ) ) ;
#60793=EDGE_CURVE ( 'NONE', #66201, #23719, #2387, .T. ) ;
#60812=DIRECTION ( 'NONE',  ( 0.000000000000000000, -0.7071067811865389130, -0.7071067811865563435 ) ) ;
#60820=ORIENTED_EDGE ( 'NONE', *, *, #634, .T. ) ;
#60827=AXIS2_PLACEMENT_3D ( 'NONE', #9219, #61105, #37812 ) ;
#60832=CIRCLE ( 'NONE', #64490, 42.00000000000000000 ) ;
#60835=DIRECTION ( 'NONE',  ( 0.000000000000000000, 0.5877852522924797984, -0.8090169943749426773 ) ) ;
#60846=VERTEX_POINT ( 'NONE', #31640 ) ;
#60849=ADVANCED_FACE ( 'NONE', ( #2012 ), #60244, .F. ) ;
#60854=DIRECTION ( 'NONE',  ( -1.000000000000000000, 0.000000000000000000, 0.000000000000000000 ) ) ;
#60862=EDGE_LOOP ( 'NONE', ( #46960, #46322, #61802, #65654 ) ) ;
#60870=ADVANCED_FACE ( 'NONE', ( #43687 ), #61709, .T. ) ;
#60897=LINE ( 'NONE', #19548, #29529 ) ;
#60907=DIRECTION ( 'NONE',  ( 0.000000000000000000, 0.000000000000000000, 1.000000000000000000 ) ) ;
#60910=ORIENTED_EDGE ( 'NONE', *, *, #10206, .T. ) ;
#60926=VERTEX_POINT ( 'NONE', #10193 ) ;
#60960=DIRECTION ( 'NONE',  ( 0.000000000000000000, 0.9876883405951372152, 0.1564344650402346160 ) ) ;
#60968=EDGE_CURVE ( 'NONE', #23196, #53520, #62467, .T. ) ;
#60997=EDGE_CURVE ( 'NONE', #69599, #2465, #816, .T. ) ;
#61011=DIRECTION ( 'NONE',  ( -1.000000000000000000, 0.000000000000000000, 0.000000000000000000 ) ) ;
#61023=CARTESIAN_POINT ( 'NONE',  ( 10.00000000000000000, 33.80338159004283938, 16.23288003029508886 ) ) ;
#61024=EDGE_CURVE ( 'NONE', #27107, #24755, #18788, .T. ) ;
#61031=EDGE_LOOP ( 'NONE', ( #20409, #38902, #50701, #20995 ) ) ;
#61052=ORIENTED_EDGE ( 'NONE', *, *, #55658, .F. ) ;
#61065=CIRCLE ( 'NONE', #40668, 16.00000000000000355 ) ;
#61081=DIRECTION ( 'NONE',  ( -1.000000000000000000, 0.000000000000000000, -0.000000000000000000 ) ) ;
#61082=DIRECTION ( 'NONE',  ( -0.000000000000000000, 0.2079116908177543743, 0.9781476007338066880 ) ) ;
#61105=DIRECTION ( 'NONE',  ( -1.000000000000000000, -0.000000000000000000, -0.000000000000000000 ) ) ;
#61136=DIRECTION ( 'NONE',  ( -1.000000000000000000, 0.000000000000000000, -0.000000000000000000 ) ) ;
#61142=CARTESIAN_POINT ( 'NONE',  ( -3.000000000000000000, -1.278221433540502217, 26.51162292216071847 ) ) ;
#61155=CIRCLE ( 'NONE', #68507, 42.00000000000000000 ) ;
#61160=ORIENTED_EDGE ( 'NONE', *, *, #61748, .F. ) ;
#61166=LINE ( 'NONE', #9653, #61725 ) ;
#61172=CARTESIAN_POINT ( 'NONE',  ( 0.000000000000000000, -13.04903810567647682, -19.60159698893442126 ) ) ;
#61174=FACE_BOUND ( 'NONE', #42074, .T. ) ;
#61180=DIRECTION ( 'NONE',  ( -1.000000000000000000, -0.000000000000000000, -0.000000000000000000 ) ) ;
#61191=ORIENTED_EDGE ( 'NONE', *, *, #15148, .T. ) ;
#61201=CIRCLE ( 'NONE', #38393, 42.00000000000000000 ) ;
#61203=ORIENTED_EDGE ( 'NONE', *, *, #44547, .T. ) ;
#61230=AXIS2_PLACEMENT_3D ( 'NONE', #38635, #31493, #48787 ) ;
#61245=VERTEX_POINT ( 'NONE', #42118 ) ;
#61246=VERTEX_POINT ( 'NONE', #70286 ) ;
#61247=DIRECTION ( 'NONE',  ( -1.000000000000000000, -0.000000000000000000, -0.000000000000000000 ) ) ;
#61273=AXIS2_PLACEMENT_3D ( 'NONE', #62476, #63949, #29700 ) ;
#61280=EDGE_CURVE ( 'NONE', #61428, #71727, #41728, .T. ) ;
#61289=AXIS2_PLACEMENT_3D ( 'NONE', #7827, #24381, #36761 ) ;
#61292=ORIENTED_EDGE ( 'NONE', *, *, #24304, .T. ) ;
#61310=ORIENTED_EDGE ( 'NONE', *, *, #53646, .T. ) ;
#61324=VERTEX_POINT ( 'NONE', #48115 ) ;
#61327=CIRCLE ( 'NONE', #68584, 37.49900000000000233 ) ;
#61344=CARTESIAN_POINT ( 'NONE',  ( 10.00000000000000000, -27.05870788708250885, 26.08949754953014022 ) ) ;
#61354=DIRECTION ( 'NONE',  ( -1.000000000000000000, -0.000000000000000000, -0.000000000000000000 ) ) ;
#61358=CYLINDRICAL_SURFACE ( 'NONE', #49536, 16.00000000000000000 ) ;
#61409=VERTEX_POINT ( 'NONE', #4492 ) ;
#61427=AXIS2_PLACEMENT_3D ( 'NONE', #66058, #14532, #2188 ) ;
#61428=VERTEX_POINT ( 'NONE', #31923 ) ;
#61434=DIRECTION ( 'NONE',  ( -1.000000000000000000, 0.000000000000000000, 0.000000000000000000 ) ) ;
#61440=ORIENTED_EDGE ( 'NONE', *, *, #65183, .T. ) ;
#61441=AXIS2_PLACEMENT_3D ( 'NONE', #40894, #59659, #65308 ) ;
#61442=EDGE_LOOP ( 'NONE', ( #9655, #7574, #58381, #47441 ) ) ;
#61452=ORIENTED_EDGE ( 'NONE', *, *, #68781, .F. ) ;
#61488=CIRCLE ( 'NONE', #51875, 42.00000000000000000 ) ;
#61489=ORIENTED_EDGE ( 'NONE', *, *, #43047, .F. ) ;
#61493=DIRECTION ( 'NONE',  ( -1.000000000000000000, -0.000000000000000000, -0.000000000000000000 ) ) ;
#61505=DIRECTION ( 'NONE',  ( 1.000000000000000000, 0.000000000000000000, 0.000000000000000000 ) ) ;
#61510=ORIENTED_EDGE ( 'NONE', *, *, #6229, .T. ) ;
#61527=EDGE_LOOP ( 'NONE', ( #52620, #13850, #10639, #41797 ) ) ;
#61534=DIRECTION ( 'NONE',  ( 1.000000000000000000, -0.000000000000000000, -0.000000000000000000 ) ) ;
#61544=AXIS2_PLACEMENT_3D ( 'NONE', #31785, #70518, #7763 ) ;
#61545=CIRCLE ( 'NONE', #71125, 15.99999999999999822 ) ;
#61561=DIRECTION ( 'NONE',  ( 0.000000000000000000, 0.000000000000000000, 1.000000000000000000 ) ) ;
#61586=ORIENTED_EDGE ( 'NONE', *, *, #32016, .F. ) ;
#61596=VERTEX_POINT ( 'NONE', #52182 ) ;
#61599=EDGE_LOOP ( 'NONE', ( #39156, #62355, #39061, #6799 ) ) ;
#61602=ORIENTED_EDGE ( 'NONE', *, *, #37550, .F. ) ;
#61618=DIRECTION ( 'NONE',  ( 0.000000000000000000, 0.000000000000000000, 1.000000000000000000 ) ) ;
#61619=ORIENTED_EDGE ( 'NONE', *, *, #20287, .T. ) ;
#61625=DIRECTION ( 'NONE',  ( -1.000000000000000000, 0.000000000000000000, -0.000000000000000000 ) ) ;
#61626=ADVANCED_FACE ( 'NONE', ( #12332 ), #56740, .T. ) ;
#61640=EDGE_CURVE ( 'NONE', #45606, #58096, #63484, .T. ) ;
#61644=DIRECTION ( 'NONE',  ( 0.000000000000000000, 1.000000000000000000, 3.469446951953614189E-15 ) ) ;
#61646=AXIS2_PLACEMENT_3D ( 'NONE', #30642, #52858, #63780 ) ;
#61651=ADVANCED_FACE ( 'NONE', ( #58197 ), #1105, .T. ) ;
#61655=FACE_OUTER_BOUND ( 'NONE', #4534, .T. ) ;
#61668=ADVANCED_FACE ( 'NONE', ( #66365 ), #66001, .T. ) ;
#61681=EDGE_CURVE ( 'NONE', #24224, #29448, #16877, .T. ) ;
#61682=AXIS2_PLACEMENT_3D ( 'NONE', #15058, #67687, #27071 ) ;
#61686=ORIENTED_EDGE ( 'NONE', *, *, #68155, .F. ) ;
#61705=VERTEX_POINT ( 'NONE', #59307 ) ;
#61707=ORIENTED_EDGE ( 'NONE', *, *, #5174, .T. ) ;
#61709=CYLINDRICAL_SURFACE ( 'NONE', #41598, 42.00000000000000000 ) ;
#61718=ORIENTED_EDGE ( 'NONE', *, *, #37358, .T. ) ;
#61720=CARTESIAN_POINT ( 'NONE',  ( 0.000000000000000000, 0.000000000000000000, 0.000000000000000000 ) ) ;
#61725=VECTOR ( 'NONE', #44239, 1000.000000000000000 ) ;
#61726=EDGE_CURVE ( 'NONE', #48459, #56518, #14059, .T. ) ;
#61729=DIRECTION ( 'NONE',  ( 0.000000000000000000, 0.6691306063588676745, -0.7431448254773856954 ) ) ;
#61734=DIRECTION ( 'NONE',  ( 1.000000000000000000, -0.000000000000000000, -0.000000000000000000 ) ) ;
#61736=DIRECTION ( 'NONE',  ( 0.000000000000000000, 0.000000000000000000, 1.000000000000000000 ) ) ;
#61742=EDGE_LOOP ( 'NONE', ( #33549, #16183, #71174, #12514 ) ) ;
#61747=ORIENTED_EDGE ( 'NONE', *, *, #11523, .T. ) ;
#61748=EDGE_CURVE ( 'NONE', #21151, #71560, #24725, .T. ) ;
#61749=DIRECTION ( 'NONE',  ( 0.000000000000000000, 0.8090169943749445647, 0.5877852522924771339 ) ) ;
#61792=FACE_OUTER_BOUND ( 'NONE', #66601, .T. ) ;
#61802=ORIENTED_EDGE ( 'NONE', *, *, #24273, .F. ) ;
#61804=CIRCLE ( 'NONE', #29358, 37.49900000000001654 ) ;
#61806=CIRCLE ( 'NONE', #38993, 16.00000000000000000 ) ;
#61809=DIRECTION ( 'NONE',  ( -1.000000000000000000, -0.000000000000000000, 0.000000000000000000 ) ) ;
#61811=CARTESIAN_POINT ( 'NONE',  ( -3.000000000000000000, -3.948201729842038432, -23.21447184625298021 ) ) ;
#61839=EDGE_LOOP ( 'NONE', ( #41060, #21674 ) ) ;
#61846=ORIENTED_EDGE ( 'NONE', *, *, #34640, .F. ) ;
#61872=ORIENTED_EDGE ( 'NONE', *, *, #64968, .F. ) ;
#61877=VECTOR ( 'NONE', #53964, 1000.000000000000000 ) ;
#61886=CARTESIAN_POINT ( 'NONE',  ( -3.000000000000000000, 24.81905959214261514, 9.408202855044825341 ) ) ;
#61890=EDGE_CURVE ( 'NONE', #61324, #39410, #59748, .T. ) ;
#61893=DIRECTION ( 'NONE',  ( -1.000000000000000000, 0.000000000000000000, -0.000000000000000000 ) ) ;
#61896=DIRECTION ( 'NONE',  ( 0.000000000000000000, 0.000000000000000000, 1.000000000000000000 ) ) ;
#61915=ADVANCED_FACE ( 'NONE', ( #66802 ), #32573, .T. ) ;
#61917=DIRECTION ( 'NONE',  ( 0.000000000000000000, 0.000000000000000000, -1.000000000000000000 ) ) ;
#61923=CARTESIAN_POINT ( 'NONE',  ( 10.00000000000000000, -35.47612816024539484, 22.48208911017487921 ) ) ;
#61927=CIRCLE ( 'NONE', #72726, 16.00000000000000355 ) ;
#61945=ADVANCED_FACE ( 'NONE', ( #56649 ), #52753, .T. ) ;
#61952=DIRECTION ( 'NONE',  ( -1.000000000000000000, -0.000000000000000000, -0.000000000000000000 ) ) ;
#61957=ORIENTED_EDGE ( 'NONE', *, *, #7418, .T. ) ;
#61964=AXIS2_PLACEMENT_3D ( 'NONE', #32857, #38515, #21960 ) ;
#61980=ORIENTED_EDGE ( 'NONE', *, *, #68003, .F. ) ;
#61993=ORIENTED_EDGE ( 'NONE', *, *, #35034, .F. ) ;
#61996=DIRECTION ( 'NONE',  ( -0.000000000000000000, 0.5000000000000031086, -0.8660254037844369313 ) ) ;
#62003=CARTESIAN_POINT ( 'NONE',  ( 0.000000000000000000, 37.22597642581158084, -5.202137450156524068 ) ) ;
#62025=ADVANCED_FACE ( 'NONE', ( #68807 ), #56023, .T. ) ;
#62035=ORIENTED_EDGE ( 'NONE', *, *, #10796, .F. ) ;
#62036=ADVANCED_FACE ( 'NONE', ( #44382 ), #73678, .T. ) ;
#62056=CARTESIAN_POINT ( 'NONE',  ( 10.00000000000000000, -37.58145647212455032, 0.6853352020789044152 ) ) ;
#62067=VERTEX_POINT ( 'NONE', #36053 ) ;
#62094=FACE_OUTER_BOUND ( 'NONE', #70699, .T. ) ;
#62103=CARTESIAN_POINT ( 'NONE',  ( 10.00000000000000000, -37.22597642581153821, -5.202137450156795850 ) ) ;
#62109=ORIENTED_EDGE ( 'NONE', *, *, #41430, .T. ) ;
#62113=DIRECTION ( 'NONE',  ( -1.000000000000000000, -0.000000000000000000, -0.000000000000000000 ) ) ;
#62116=DIRECTION ( 'NONE',  ( 0.000000000000000000, -0.9135454576426009776, -0.4067366430758000417 ) ) ;
#62118=EDGE_CURVE ( 'NONE', #64733, #32803, #35737, .T. ) ;
#62128=CARTESIAN_POINT ( 'NONE',  ( 0.000000000000000000, 32.34446384429971033, 26.79245525562726371 ) ) ;
#62133=CARTESIAN_POINT ( 'NONE',  ( 10.00000000000000000, -4.992566952384716927, -37.16516213103282951 ) ) ;
#62136=ORIENTED_EDGE ( 'NONE', *, *, #6807, .F. ) ;
#62140=VERTEX_POINT ( 'NONE', #23308 ) ;
#62172=CARTESIAN_POINT ( 'NONE',  ( 0.000000000000000000, 8.688484142254221609, -21.88630264137359660 ) ) ;
#62177=CARTESIAN_POINT ( 'NONE',  ( 0.000000000000000000, -4.992566952384716927, -37.16516213103282951 ) ) ;
#62184=DIRECTION ( 'NONE',  ( 0.000000000000000000, 0.000000000000000000, 1.000000000000000000 ) ) ;
#62190=VERTEX_POINT ( 'NONE', #25879 ) ;
#62196=DIRECTION ( 'NONE',  ( 0.000000000000000000, -0.9945218953682742891, 0.1045284632676436315 ) ) ;
#62198=LINE ( 'NONE', #43807, #18474 ) ;
#62220=ADVANCED_FACE ( 'NONE', ( #8217 ), #20617, .F. ) ;
#62221=AXIS2_PLACEMENT_3D ( 'NONE', #23578, #57802, #58913 ) ;
#62226=LINE ( 'NONE', #74230, #59783 ) ;
#62228=VERTEX_POINT ( 'NONE', #49181 ) ;
#62257=ORIENTED_EDGE ( 'NONE', *, *, #60023, .T. ) ;
#62278=FACE_OUTER_BOUND ( 'NONE', #71576, .T. ) ;
#62320=CARTESIAN_POINT ( 'NONE',  ( 0.000000000000000000, -10.45096189432344147, 21.10159698893426494 ) ) ;
#62335=AXIS2_PLACEMENT_3D ( 'NONE', #6822, #52689, #6107 ) ;
#62354=LINE ( 'NONE', #21731, #72894 ) ;
#62355=ORIENTED_EDGE ( 'NONE', *, *, #52461, .T. ) ;
#62368=CIRCLE ( 'NONE', #10715, 16.00000000000000355 ) ;
#62371=EDGE_LOOP ( 'NONE', ( #47422, #17480, #54179, #72908 ) ) ;
#62374=AXIS2_PLACEMENT_3D ( 'NONE', #40202, #45487, #67661 ) ;
#62379=EDGE_LOOP ( 'NONE', ( #16542, #27918, #63919, #48837 ) ) ;
#62395=CARTESIAN_POINT ( 'NONE',  ( -3.000000000000000000, 23.59884966291538078, -12.14883922797231541 ) ) ;
#62413=LINE ( 'NONE', #10894, #64824 ) ;
#62418=CIRCLE ( 'NONE', #29975, 37.49900000000000233 ) ;
#62438=VERTEX_POINT ( 'NONE', #4836 ) ;
#62442=CYLINDRICAL_SURFACE ( 'NONE', #25098, 16.00000000000000000 ) ;
#62445=AXIS2_PLACEMENT_3D ( 'NONE', #19025, #41976, #36691 ) ;
#62446=ORIENTED_EDGE ( 'NONE', *, *, #55018, .T. ) ;
#62454=EDGE_LOOP ( 'NONE', ( #27439, #50060, #73664, #7932 ) ) ;
#62467=LINE ( 'NONE', #44048, #48788 ) ;
#62475=AXIS2_PLACEMENT_3D ( 'NONE', #71123, #43693, #72594 ) ;
#62476=CARTESIAN_POINT ( 'NONE',  ( -3.000000000000000000, -25.60904388321925396, 6.976881207771172377 ) ) ;
#62479=VECTOR ( 'NONE', #10606, 1000.000000000000000 ) ;
#62501=CARTESIAN_POINT ( 'NONE',  ( -3.000000000000000000, 24.81905959214261514, 9.408202855044825341 ) ) ;
#62509=CARTESIAN_POINT ( 'NONE',  ( 4.999999999999999112, -38.55633173627022359, 16.65560815589396526 ) ) ;
#62514=DIRECTION ( 'NONE',  ( -1.000000000000000000, -0.000000000000000000, 0.000000000000000000 ) ) ;
#62528=DIRECTION ( 'NONE',  ( -1.000000000000000000, 0.000000000000000000, -0.000000000000000000 ) ) ;
#62535=ORIENTED_EDGE ( 'NONE', *, *, #63586, .F. ) ;
#62563=DIRECTION ( 'NONE',  ( -1.000000000000000000, 0.000000000000000000, 0.000000000000000000 ) ) ;
#62568=EDGE_CURVE ( 'NONE', #27866, #63232, #67027, .T. ) ;
#62570=ADVANCED_FACE ( 'NONE', ( #7021 ), #29204, .F. ) ;
#62576=DIRECTION ( 'NONE',  ( -1.000000000000000000, 0.000000000000000000, 0.000000000000000000 ) ) ;
#62581=VECTOR ( 'NONE', #35897, 1000.000000000000114 ) ;
#62605=CARTESIAN_POINT ( 'NONE',  ( 10.00000000000000000, -10.74501242461308159, 35.92658777277507909 ) ) ;
#62608=AXIS2_PLACEMENT_3D ( 'NONE', #61344, #38772, #20735 ) ;
#62611=AXIS2_PLACEMENT_3D ( 'NONE', #46374, #64044, #12518 ) ;
#62612=ORIENTED_EDGE ( 'NONE', *, *, #21083, .F. ) ;
#62626=ORIENTED_EDGE ( 'NONE', *, *, #47392, .T. ) ;
#62633=DIRECTION ( 'NONE',  ( -1.000000000000000000, -0.000000000000000000, -0.000000000000000000 ) ) ;
#62635=CARTESIAN_POINT ( 'NONE',  ( 10.00000000000000000, 0.6853352020795618893, -37.58145647212453611 ) ) ;
#62656=CARTESIAN_POINT ( 'NONE',  ( -3.000000000000000000, -11.95096189432345390, 23.69967320028757385 ) ) ;
#62657=DIRECTION ( 'NONE',  ( -1.000000000000000000, 0.000000000000000000, 0.000000000000000000 ) ) ;
#62684=CARTESIAN_POINT ( 'NONE',  ( 0.000000000000000000, -33.80338159004296017, 16.23288003029484727 ) ) ;
#62693=DIRECTION ( 'NONE',  ( 0.000000000000000000, 0.4067366430757887730, 0.9135454576426059736 ) ) ;
#62710=ORIENTED_EDGE ( 'NONE', *, *, #50751, .F. ) ;
#62719=AXIS2_PLACEMENT_3D ( 'NONE', #17607, #68754, #11582 ) ;
#62725=CIRCLE ( 'NONE', #54331, 16.00000000000000000 ) ;
#62746=ORIENTED_EDGE ( 'NONE', *, *, #2534, .T. ) ;
#62767=CARTESIAN_POINT ( 'NONE',  ( 0.000000000000000000, -22.74946021919110706, -29.81001611431033282 ) ) ;
#62769=ADVANCED_FACE ( 'NONE', ( #71648 ), #66039, .T. ) ;
#62775=EDGE_CURVE ( 'NONE', #31441, #31980, #74226, .T. ) ;
#62815=DIRECTION ( 'NONE',  ( -0.000000000000000000, -0.5877852522924789103, 0.8090169943749432324 ) ) ;
#62819=ORIENTED_EDGE ( 'NONE', *, *, #31719, .F. ) ;
#62827=DIRECTION ( 'NONE',  ( -1.000000000000000000, 0.000000000000000000, -0.000000000000000000 ) ) ;
#62830=ORIENTED_EDGE ( 'NONE', *, *, #53128, .T. ) ;
#62833=EDGE_CURVE ( 'NONE', #58096, #51229, #22383, .T. ) ;
#62834=VERTEX_POINT ( 'NONE', #4746 ) ;
#62842=ORIENTED_EDGE ( 'NONE', *, *, #38555, .F. ) ;
#62848=DIRECTION ( 'NONE',  ( 1.000000000000000000, 0.000000000000000000, -0.000000000000000000 ) ) ;
#62863=CARTESIAN_POINT ( 'NONE',  ( 0.000000000000000000, 22.07842321921492612, -8.187992925817130896 ) ) ;
#62866=FACE_OUTER_BOUND ( 'NONE', #25989, .T. ) ;
#62870=DIRECTION ( 'NONE',  ( 0.000000000000000000, -0.4067366430758010409, 0.9135454576426005335 ) ) ;
#62895=EDGE_CURVE ( 'NONE', #46530, #8777, #28011, .T. ) ;
#62896=DIRECTION ( 'NONE',  ( 0.000000000000000000, 0.8910065241883656784, 0.4539904997395510788 ) ) ;
#62900=VERTEX_POINT ( 'NONE', #17115 ) ;
#62904=DIRECTION ( 'NONE',  ( -1.000000000000000000, -0.000000000000000000, -0.000000000000000000 ) ) ;
#62919=ORIENTED_EDGE ( 'NONE', *, *, #50737, .F. ) ;
#62930=ORIENTED_EDGE ( 'NONE', *, *, #51726, .T. ) ;
#62955=CARTESIAN_POINT ( 'NONE',  ( 10.00000000000000000, 37.58145647212453611, 16.68533520207917675 ) ) ;
#62957=DIRECTION ( 'NONE',  ( 0.000000000000000000, 0.6691306063588563502, 0.7431448254773960205 ) ) ;
#62984=CARTESIAN_POINT ( 'NONE',  ( -3.000000000000000000, -19.89357724624987256, -12.59942793731086041 ) ) ;
#62989=VERTEX_POINT ( 'NONE', #6932 ) ;
#63000=ORIENTED_EDGE ( 'NONE', *, *, #5012, .T. ) ;
#63049=DIRECTION ( 'NONE',  ( -1.000000000000000000, 0.000000000000000000, -0.000000000000000000 ) ) ;
#63053=DIRECTION ( 'NONE',  ( -1.000000000000000000, 0.000000000000000000, 0.000000000000000000 ) ) ;
#63068=DIRECTION ( 'NONE',  ( 0.000000000000000000, 0.000000000000000000, 1.000000000000000000 ) ) ;
#63077=ORIENTED_EDGE ( 'NONE', *, *, #13167, .F. ) ;
#63080=DIRECTION ( 'NONE',  ( 0.000000000000000000, 0.5877852522924685852, 0.8090169943749508930 ) ) ;
#63082=CARTESIAN_POINT ( 'NONE',  ( -3.000000000000000000, 23.50000000000000000, -1.500000000000001332 ) ) ;
#63095=CARTESIAN_POINT ( 'NONE',  ( 10.00000000000000000, 29.81001611431009479, 22.74946021919143391 ) ) ;
#63151=DIRECTION ( 'NONE',  ( 1.000000000000000000, 0.000000000000000000, 0.000000000000000000 ) ) ;
#63152=EDGE_CURVE ( 'NONE', #56518, #74246, #30967, .T. ) ;
#63153=CARTESIAN_POINT ( 'NONE',  ( 10.00000000000000000, 29.81001611431009479, 22.74946021919143391 ) ) ;
#63157=CIRCLE ( 'NONE', #37914, 21.00000000000000000 ) ;
#63164=VECTOR ( 'NONE', #3211, 1000.000000000000000 ) ;
#63165=FACE_OUTER_BOUND ( 'NONE', #66573, .T. ) ;
#63183=ORIENTED_EDGE ( 'NONE', *, *, #1906, .F. ) ;
#63184=LINE ( 'NONE', #23319, #70869 ) ;
#63190=EDGE_CURVE ( 'NONE', #38975, #6686, #63514, .T. ) ;
#63192=EDGE_LOOP ( 'NONE', ( #19791, #31500, #50099, #66504 ) ) ;
#63200=DIRECTION ( 'NONE',  ( 0.000000000000000000, 0.000000000000000000, -1.000000000000000000 ) ) ;
#63206=AXIS2_PLACEMENT_3D ( 'NONE', #67806, #61434, #27947 ) ;
#63218=PLANE ( 'NONE',  #8218 ) ;
#63224=CYLINDRICAL_SURFACE ( 'NONE', #46089, 42.00000000000000000 ) ;
#63232=VERTEX_POINT ( 'NONE', #50504 ) ;
#63233=DIRECTION ( 'NONE',  ( 0.000000000000000000, 0.000000000000000000, 1.000000000000000000 ) ) ;
#63242=DIRECTION ( 'NONE',  ( 0.000000000000000000, -0.9510565162951565288, 0.3090169943749382364 ) ) ;
#63247=DIRECTION ( 'NONE',  ( -0.000000000000000000, 0.4999999999999919509, 0.8660254037844432595 ) ) ;
#63254=ORIENTED_EDGE ( 'NONE', *, *, #36681, .F. ) ;
#63263=EDGE_CURVE ( 'NONE', #27990, #16188, #68173, .T. ) ;
#63280=CARTESIAN_POINT ( 'NONE',  ( 0.000000000000000000, -19.89357724625003598, 12.59942793731059574 ) ) ;
#63315=DIRECTION ( 'NONE',  ( 1.000000000000000000, 0.000000000000000000, 0.000000000000000000 ) ) ;
#63318=ADVANCED_FACE ( 'NONE', ( #73798 ), #22313, .T. ) ;
#63319=CIRCLE ( 'NONE', #66931, 37.49900000000000233 ) ;
#63361=LINE ( 'NONE', #11826, #39947 ) ;
#63374=EDGE_LOOP ( 'NONE', ( #31243, #42761, #38550, #16780 ) ) ;
#63406=DIRECTION ( 'NONE',  ( 0.000000000000000000, 0.6691306063588672304, -0.7431448254773862505 ) ) ;
#63408=DIRECTION ( 'NONE',  ( -1.000000000000000000, 0.000000000000000000, 0.000000000000000000 ) ) ;
#63411=VECTOR ( 'NONE', #38519, 1000.000000000000000 ) ;
#63422=DIRECTION ( 'NONE',  ( 0.000000000000000000, 0.7071067811865487940, -0.7071067811865462405 ) ) ;
#63428=CARTESIAN_POINT ( 'NONE',  ( 10.00000000000000000, 22.48208911017551515, -35.47612816024499693 ) ) ;
#63433=VERTEX_POINT ( 'NONE', #6149 ) ;
#63438=DIRECTION ( 'NONE',  ( 0.000000000000000000, -0.8910065241883627918, -0.4539904997395568520 ) ) ;
#63448=ORIENTED_EDGE ( 'NONE', *, *, #63263, .T. ) ;
#63461=AXIS2_PLACEMENT_3D ( 'NONE', #37466, #26156, #72019 ) ;
#63463=ORIENTED_EDGE ( 'NONE', *, *, #58767, .F. ) ;
#63471=DIRECTION ( 'NONE',  ( 0.000000000000000000, 0.8660254037844432595, -0.4999999999999919509 ) ) ;
#63484=LINE ( 'NONE', #46552, #71640 ) ;
#63490=FACE_OUTER_BOUND ( 'NONE', #67303, .T. ) ;
#63491=VECTOR ( 'NONE', #49191, 1000.000000000000000 ) ;
#63492=CARTESIAN_POINT ( 'NONE',  ( 10.00000000000000000, 0.000000000000000000, 0.000000000000000000 ) ) ;
#63501=LINE ( 'NONE', #24009, #3232 ) ;
#63514=CIRCLE ( 'NONE', #69506, 37.49900000000000944 ) ;
#63518=LINE ( 'NONE', #65639, #8192 ) ;
#63521=CARTESIAN_POINT ( 'NONE',  ( 0.000000000000000000, 31.52238457039637609, -27.75498641678709788 ) ) ;
#63526=EDGE_CURVE ( 'NONE', #33020, #47477, #53959, .T. ) ;
#63533=AXIS2_PLACEMENT_3D ( 'NONE', #37314, #43334, #53847 ) ;
#63534=ORIENTED_EDGE ( 'NONE', *, *, #69177, .F. ) ;
#63542=EDGE_LOOP ( 'NONE', ( #40312, #13003, #22564, #52905 ) ) ;
#63546=ORIENTED_EDGE ( 'NONE', *, *, #30696, .F. ) ;
#63549=CIRCLE ( 'NONE', #10552, 16.00000000000000000 ) ;
#63562=VECTOR ( 'NONE', #8342, 1000.000000000000000 ) ;
#63573=CARTESIAN_POINT ( 'NONE',  ( 10.00000000000000000, 16.65560815589411092, 38.55633173627015964 ) ) ;
#63580=CARTESIAN_POINT ( 'NONE',  ( 0.000000000000000000, 0.000000000000000000, 0.000000000000000000 ) ) ;
#63586=EDGE_CURVE ( 'NONE', #36276, #39410, #9501, .T. ) ;
#63613=EDGE_CURVE ( 'NONE', #22472, #44000, #56059, .T. ) ;
#63625=EDGE_LOOP ( 'NONE', ( #45437, #38760, #1344, #31083 ) ) ;
#63647=CIRCLE ( 'NONE', #45622, 16.00000000000000000 ) ;
#63668=ADVANCED_FACE ( 'NONE', ( #43684 ), #66960, .T. ) ;
#63672=VERTEX_POINT ( 'NONE', #32005 ) ;
#63694=EDGE_CURVE ( 'NONE', #7677, #13386, #44348, .T. ) ;
#63709=VERTEX_POINT ( 'NONE', #28968 ) ;
#63735=DIRECTION ( 'NONE',  ( 0.000000000000000000, -0.9945218953682730678, -0.1045284632676570791 ) ) ;
#63738=LINE ( 'NONE', #53552, #23643 ) ;
#63755=CARTESIAN_POINT ( 'NONE',  ( 0.000000000000000000, 18.84667830672579925, 18.68964196561269020 ) ) ;
#63773=CYLINDRICAL_SURFACE ( 'NONE', #18695, 16.00000000000000000 ) ;
#63775=LINE ( 'NONE', #64139, #51422 ) ;
#63780=DIRECTION ( 'NONE',  ( 0.000000000000000000, -0.5877852522924802425, 0.8090169943749422332 ) ) ;
#63788=VERTEX_POINT ( 'NONE', #12412 ) ;
#63830=LINE ( 'NONE', #12670, #60266 ) ;
#63838=LINE ( 'NONE', #7785, #66199 ) ;
#63839=DIRECTION ( 'NONE',  ( 0.000000000000000000, -0.5000000000000046629, 0.8660254037844359321 ) ) ;
#63844=VECTOR ( 'NONE', #2215, 1000.000000000000000 ) ;
#63855=VERTEX_POINT ( 'NONE', #51151 ) ;
#63861=DIRECTION ( 'NONE',  ( -1.000000000000000000, -0.000000000000000000, -0.000000000000000000 ) ) ;
#63863=CIRCLE ( 'NONE', #61441, 16.00000000000000000 ) ;
#63871=DIRECTION ( 'NONE',  ( -1.000000000000000000, -0.000000000000000000, 0.000000000000000000 ) ) ;
#63881=DIRECTION ( 'NONE',  ( -1.000000000000000000, -0.000000000000000000, -0.000000000000000000 ) ) ;
#63898=CIRCLE ( 'NONE', #3855, 42.00000000000000000 ) ;
#63919=ORIENTED_EDGE ( 'NONE', *, *, #64279, .F. ) ;
#63929=ORIENTED_EDGE ( 'NONE', *, *, #64585, .F. ) ;
#63941=EDGE_CURVE ( 'NONE', #70819, #48459, #49160, .T. ) ;
#63946=CARTESIAN_POINT ( 'NONE',  ( 10.00000000000000000, 0.000000000000000000, 0.000000000000000000 ) ) ;
#63949=DIRECTION ( 'NONE',  ( -0.000000000000000000, 0.9781476007338066880, -0.2079116908177543743 ) ) ;
#63951=DIRECTION ( 'NONE',  ( 0.000000000000000000, 0.5877852522924685852, 0.8090169943749508930 ) ) ;
#63956=CARTESIAN_POINT ( 'NONE',  ( 10.00000000000000000, -30.80686688397025108, 21.53537804866070715 ) ) ;
#63962=AXIS2_PLACEMENT_3D ( 'NONE', #43612, #72879, #3763 ) ;
#63967=DIRECTION ( 'NONE',  ( -0.000000000000000000, -0.6691306063588671194, 0.7431448254773862505 ) ) ;
#63971=ORIENTED_EDGE ( 'NONE', *, *, #56204, .F. ) ;
#63975=DIRECTION ( 'NONE',  ( -1.000000000000000000, 0.000000000000000000, 0.000000000000000000 ) ) ;
#63980=ADVANCED_FACE ( 'NONE', ( #47011 ), #12777, .F. ) ;
#64029=CARTESIAN_POINT ( 'NONE',  ( 10.00000000000000000, -37.22597642581153821, 10.79786254984320415 ) ) ;
#64032=DIRECTION ( 'NONE',  ( 0.000000000000000000, 0.000000000000000000, -1.000000000000000000 ) ) ;
#64038=VERTEX_POINT ( 'NONE', #9360 ) ;
#64044=DIRECTION ( 'NONE',  ( -1.000000000000000000, -0.000000000000000000, -0.000000000000000000 ) ) ;
#64047=DIRECTION ( 'NONE',  ( -1.000000000000000000, -0.000000000000000000, -0.000000000000000000 ) ) ;
#64055=CARTESIAN_POINT ( 'NONE',  ( 0.000000000000000000, -0.6853352020787742971, -37.58145647212455032 ) ) ;
#64061=VECTOR ( 'NONE', #62693, 1000.000000000000000 ) ;
#64076=ORIENTED_EDGE ( 'NONE', *, *, #67118, .F. ) ;
#64079=AXIS2_PLACEMENT_3D ( 'NONE', #1270, #34683, #58354 ) ;
#64097=ORIENTED_EDGE ( 'NONE', *, *, #69679, .T. ) ;
#64099=DIRECTION ( 'NONE',  ( 0.000000000000000000, 0.8910065241883656784, 0.4539904997395511899 ) ) ;
#64102=CYLINDRICAL_SURFACE ( 'NONE', #44691, 16.00000000000000355 ) ;
#64114=ORIENTED_EDGE ( 'NONE', *, *, #6151, .T. ) ;
#64121=VERTEX_POINT ( 'NONE', #19762 ) ;
#64125=CIRCLE ( 'NONE', #5312, 37.49900000000000944 ) ;
#64127=DIRECTION ( 'NONE',  ( 0.000000000000000000, 0.000000000000000000, 1.000000000000000000 ) ) ;
#64139=CARTESIAN_POINT ( 'NONE',  ( -3.000000000000000000, 16.83928648764923253, 16.46020748918050458 ) ) ;
#64152=CARTESIAN_POINT ( 'NONE',  ( 10.00000000000000000, -22.48208911017525580, 35.47612816024516036 ) ) ;
#64155=VECTOR ( 'NONE', #62815, 1000.000000000000000 ) ;
#64163=ADVANCED_FACE ( 'NONE', ( #54361 ), #53998, .T. ) ;
#64164=CIRCLE ( 'NONE', #24387, 16.00000000000000000 ) ;
#64169=ORIENTED_EDGE ( 'NONE', *, *, #43828, .F. ) ;
#64182=CIRCLE ( 'NONE', #42600, 16.00000000000000000 ) ;
#64199=ORIENTED_EDGE ( 'NONE', *, *, #7385, .F. ) ;
#64223=CIRCLE ( 'NONE', #11396, 37.49900000000001654 ) ;
#64245=EDGE_CURVE ( 'NONE', #60337, #36560, #67088, .T. ) ;
#64246=PLANE ( 'NONE',  #56470 ) ;
#64254=VECTOR ( 'NONE', #14892, 1000.000000000000000 ) ;
#64260=ORIENTED_EDGE ( 'NONE', *, *, #3175, .F. ) ;
#64279=EDGE_CURVE ( 'NONE', #35203, #30584, #139, .T. ) ;
#64281=CARTESIAN_POINT ( 'NONE',  ( 0.000000000000000000, 0.000000000000000000, 0.000000000000000000 ) ) ;
#64297=ORIENTED_EDGE ( 'NONE', *, *, #22924, .T. ) ;
#64303=DIRECTION ( 'NONE',  ( 0.000000000000000000, 0.000000000000000000, 1.000000000000000000 ) ) ;
#64304=ORIENTED_EDGE ( 'NONE', *, *, #15292, .F. ) ;
#64307=CARTESIAN_POINT ( 'NONE',  ( 10.00000000000000000, 17.80606268964540462, 33.00180498840053644 ) ) ;
#64311=DIRECTION ( 'NONE',  ( 0.000000000000000000, -1.000000000000000000, -1.040834085586084257E-14 ) ) ;
#64319=DIRECTION ( 'NONE',  ( -1.000000000000000000, -0.000000000000000000, 0.000000000000000000 ) ) ;
#64320=FACE_OUTER_BOUND ( 'NONE', #42012, .T. ) ;
#64324=AXIS2_PLACEMENT_3D ( 'NONE', #38939, #21636, #67880 ) ;
#64326=DIRECTION ( 'NONE',  ( -1.000000000000000000, 0.000000000000000000, -0.000000000000000000 ) ) ;
#64339=LINE ( 'NONE', #12811, #25085 ) ;
#64343=EDGE_CURVE ( 'NONE', #13949, #43951, #50840, .T. ) ;
#64359=VERTEX_POINT ( 'NONE', #56118 ) ;
#64368=ORIENTED_EDGE ( 'NONE', *, *, #56650, .T. ) ;
#64374=ORIENTED_EDGE ( 'NONE', *, *, #45851, .T. ) ;
#64420=DIRECTION ( 'NONE',  ( 0.000000000000000000, -0.4067366430758010409, 0.9135454576426005335 ) ) ;
#64424=CARTESIAN_POINT ( 'NONE',  ( 4.999999999999999112, 40.68715046381943523, -10.41901085202036370 ) ) ;
#64427=CARTESIAN_POINT ( 'NONE',  ( 0.000000000000000000, 17.67226234102874116, -33.17418723428288274 ) ) ;
#64447=ORIENTED_EDGE ( 'NONE', *, *, #68193, .T. ) ;
#64478=CARTESIAN_POINT ( 'NONE',  ( 0.000000000000000000, 29.81001611431041098, -22.74946021919100403 ) ) ;
#64481=DIRECTION ( 'NONE',  ( 0.000000000000000000, 0.000000000000000000, 1.000000000000000000 ) ) ;
#64482=ORIENTED_EDGE ( 'NONE', *, *, #88, .T. ) ;
#64483=LINE ( 'NONE', #12958, #62581 ) ;
#64490=AXIS2_PLACEMENT_3D ( 'NONE', #17621, #744, #23633 ) ;
#64491=CARTESIAN_POINT ( 'NONE',  ( 10.00000000000000000, 37.58145647212455032, -0.6853352020786441789 ) ) ;
#64503=LINE ( 'NONE', #53223, #48529 ) ;
#64524=VECTOR ( 'NONE', #23685, 1000.000000000000000 ) ;
#64527=EDGE_CURVE ( 'NONE', #70418, #46611, #28650, .T. ) ;
#64533=CARTESIAN_POINT ( 'NONE',  ( 10.00000000000000000, 10.96151621346540317, -35.95386929396244113 ) ) ;
#64537=CARTESIAN_POINT ( 'NONE',  ( 5.000000000000000000, -32.34446384429951138, -26.79245525562750530 ) ) ;
#64571=DIRECTION ( 'NONE',  ( -1.000000000000000000, 0.000000000000000000, 0.000000000000000000 ) ) ;
#64573=CARTESIAN_POINT ( 'NONE',  ( 4.999999999999999112, -10.41901085202107247, 40.68715046381925049 ) ) ;
#64582=CARTESIAN_POINT ( 'NONE',  ( 5.000000000000000000, -26.79245525562690844, -32.34446384430000876 ) ) ;
#64585=EDGE_CURVE ( 'NONE', #64719, #18846, #56143, .T. ) ;
#64615=ADVANCED_FACE ( 'NONE', ( #4662 ), #51237, .T. ) ;
#64621=LINE ( 'NONE', #40962, #65415 ) ;
#64628=VERTEX_POINT ( 'NONE', #50108 ) ;
#64634=CIRCLE ( 'NONE', #50179, 37.49900000000000233 ) ;
#64645=EDGE_LOOP ( 'NONE', ( #49947, #35137, #46922, #58846 ) ) ;
#64648=SURFACE_SIDE_STYLE ('',( #41710 ) ) ;
#64653=CIRCLE ( 'NONE', #13009, 21.00000000000000000 ) ;
#64654=ORIENTED_EDGE ( 'NONE', *, *, #27120, .T. ) ;
#64656=FACE_OUTER_BOUND ( 'NONE', #55690, .T. ) ;
#64658=VECTOR ( 'NONE', #44758, 1000.000000000000000 ) ;
#64677=DIRECTION ( 'NONE',  ( 0.000000000000000000, 0.6691306063588569053, 0.7431448254773954654 ) ) ;
#64684=DIRECTION ( 'NONE',  ( 0.000000000000000000, -0.3090169943749349057, -0.9510565162951577500 ) ) ;
#64709=CIRCLE ( 'NONE', #1158, 37.49900000000000233 ) ;
#64714=DIRECTION ( 'NONE',  ( -1.000000000000000000, 0.000000000000000000, 0.000000000000000000 ) ) ;
#64719=VERTEX_POINT ( 'NONE', #69277 ) ;
#64726=ORIENTED_EDGE ( 'NONE', *, *, #19287, .F. ) ;
#64733=VERTEX_POINT ( 'NONE', #7238 ) ;
#64739=ORIENTED_EDGE ( 'NONE', *, *, #14142, .F. ) ;
#64748=DIRECTION ( 'NONE',  ( -1.000000000000000000, -0.000000000000000000, 0.000000000000000000 ) ) ;
#64772=ORIENTED_EDGE ( 'NONE', *, *, #43746, .F. ) ;
#64815=ORIENTED_EDGE ( 'NONE', *, *, #70494, .T. ) ;
#64819=VECTOR ( 'NONE', #53567, 1000.000000000000000 ) ;
#64824=VECTOR ( 'NONE', #36029, 1000.000000000000114 ) ;
#64874=CARTESIAN_POINT ( 'NONE',  ( 10.00000000000000000, 15.48615015657638239, -39.04073710021328480 ) ) ;
#64903=CARTESIAN_POINT ( 'NONE',  ( 10.00000000000000000, -0.6853352020793173072, 37.58145647212453611 ) ) ;
#64914=CARTESIAN_POINT ( 'NONE',  ( -3.000000000000000000, -3.948201729842038432, -23.21447184625298021 ) ) ;
#64920=ORIENTED_EDGE ( 'NONE', *, *, #15615, .T. ) ;
#64923=ORIENTED_EDGE ( 'NONE', *, *, #65848, .T. ) ;
#64944=CARTESIAN_POINT ( 'NONE',  ( 4.999999999999999112, -3.925862922255855647, -41.81611651403866858 ) ) ;
#64951=ORIENTED_EDGE ( 'NONE', *, *, #30115, .T. ) ;
#64952=VERTEX_POINT ( 'NONE', #71477 ) ;
#64953=LINE ( 'NONE', #30713, #72150 ) ;
#64968=EDGE_CURVE ( 'NONE', #20059, #67482, #41927, .T. ) ;
#64982=EDGE_CURVE ( 'NONE', #35679, #11281, #3100, .T. ) ;
#64993=DIRECTION ( 'NONE',  ( -1.000000000000000000, -0.000000000000000000, 0.000000000000000000 ) ) ;
#65013=ADVANCED_FACE ( 'NONE', ( #60235 ), #8712, .T. ) ;
#65031=VERTEX_POINT ( 'NONE', #22213 ) ;
#65035=ORIENTED_EDGE ( 'NONE', *, *, #56940, .F. ) ;
#65058=EDGE_CURVE ( 'NONE', #1375, #27107, #40692, .T. ) ;
#65070=DIRECTION ( 'NONE',  ( 0.000000000000000000, -0.4539904997395541320, 0.8910065241883640130 ) ) ;
#65073=LINE ( 'NONE', #67188, #12999 ) ;
#65074=AXIS2_PLACEMENT_3D ( 'NONE', #49595, #50716, #55619 ) ;
#65080=ORIENTED_EDGE ( 'NONE', *, *, #14757, .F. ) ;
#65087=DIRECTION ( 'NONE',  ( -1.000000000000000000, 0.000000000000000000, 0.000000000000000000 ) ) ;
#65097=ADVANCED_BREP_SHAPE_REPRESENTATION ( '', ( #39004, #43395 ), #39845 ) ;
#65105=ORIENTED_EDGE ( 'NONE', *, *, #48119, .F. ) ;
#65109=CARTESIAN_POINT ( 'NONE',  ( -3.000000000000000000, 20.85821328998756385, -10.92862929874494959 ) ) ;
#65121=DIRECTION ( 'NONE',  ( 0.000000000000000000, 0.5877852522924797984, -0.8090169943749426773 ) ) ;
#65130=EDGE_CURVE ( 'NONE', #12484, #56884, #56568, .T. ) ;
#65132=AXIS2_PLACEMENT_3D ( 'NONE', #36648, #8824, #2849 ) ;
#65136=CIRCLE ( 'NONE', #345, 42.00000000000000000 ) ;
#65139=PLANE ( 'NONE',  #16774 ) ;
#65168=CYLINDRICAL_SURFACE ( 'NONE', #40103, 37.49900000000000233 ) ;
#65182=ORIENTED_EDGE ( 'NONE', *, *, #55588, .T. ) ;
#65183=EDGE_CURVE ( 'NONE', #10228, #25590, #12770, .T. ) ;
#65200=CARTESIAN_POINT ( 'NONE',  ( 0.000000000000000000, 16.61724383029390140, -20.69703378468904020 ) ) ;
#65207=EDGE_LOOP ( 'NONE', ( #31430, #26800, #56622, #8038 ) ) ;
#65222=VERTEX_POINT ( 'NONE', #58642 ) ;
#65230=ORIENTED_EDGE ( 'NONE', *, *, #40309, .F. ) ;
#65241=VECTOR ( 'NONE', #69427, 1000.000000000000000 ) ;
#65246=CARTESIAN_POINT ( 'NONE',  ( 10.00000000000000000, -21.40280677340398441, 36.13751322684410638 ) ) ;
#65249=AXIS2_PLACEMENT_3D ( 'NONE', #13362, #59236, #46473 ) ;
#65250=CARTESIAN_POINT ( 'NONE',  ( 0.000000000000000000, -26.79245525562690844, -32.34446384430000876 ) ) ;
#65251=CARTESIAN_POINT ( 'NONE',  ( 10.00000000000000000, -37.58145647212455032, 16.68533520207890319 ) ) ;
#65252=DIRECTION ( 'NONE',  ( -1.000000000000000000, 0.000000000000000000, -0.000000000000000000 ) ) ;
#65270=VECTOR ( 'NONE', #48553, 1000.000000000000000 ) ;
#65308=DIRECTION ( 'NONE',  ( 0.000000000000000000, 0.4539904997395479702, -0.8910065241883673437 ) ) ;
#65313=CARTESIAN_POINT ( 'NONE',  ( 10.00000000000000000, 33.79645857604513992, -16.45098606841138178 ) ) ;
#65328=ORIENTED_EDGE ( 'NONE', *, *, #30992, .F. ) ;
#65333=AXIS2_PLACEMENT_3D ( 'NONE', #67121, #33648, #44946 ) ;
#65348=CARTESIAN_POINT ( 'NONE',  ( 10.00000000000000000, 9.188173127307898369, -40.98264845739739570 ) ) ;
#65349=ORIENTED_EDGE ( 'NONE', *, *, #53449, .T. ) ;
#65357=AXIS2_PLACEMENT_3D ( 'NONE', #15323, #49172, #71346 ) ;
#65366=ORIENTED_EDGE ( 'NONE', *, *, #32976, .T. ) ;
#65369=AXIS2_PLACEMENT_3D ( 'NONE', #57374, #46097, #16031 ) ;
#65376=ORIENTED_EDGE ( 'NONE', *, *, #17184, .T. ) ;
#65380=ORIENTED_EDGE ( 'NONE', *, *, #69994, .F. ) ;
#65387=ORIENTED_EDGE ( 'NONE', *, *, #2246, .T. ) ;
#65393=ORIENTED_EDGE ( 'NONE', *, *, #7951, .T. ) ;
#65415=VECTOR ( 'NONE', #7841, 999.9999999999998863 ) ;
#65416=CYLINDRICAL_SURFACE ( 'NONE', #34702, 16.00000000000000000 ) ;
#65420=ORIENTED_EDGE ( 'NONE', *, *, #42616, .F. ) ;
#65429=DIRECTION ( 'NONE',  ( 0.000000000000000000, 0.000000000000000000, 1.000000000000000000 ) ) ;
#65437=CARTESIAN_POINT ( 'NONE',  ( 0.000000000000000000, 21.53537804866126137, -30.80686688396986028 ) ) ;
#65438=EDGE_CURVE ( 'NONE', #66007, #68543, #55307, .T. ) ;
#65458=ORIENTED_EDGE ( 'NONE', *, *, #71635, .T. ) ;
#65480=DIRECTION ( 'NONE',  ( -1.000000000000000000, 0.000000000000000000, -0.000000000000000000 ) ) ;
#65486=ORIENTED_EDGE ( 'NONE', *, *, #5359, .F. ) ;
#65487=EDGE_LOOP ( 'NONE', ( #66819, #52051, #51931, #55367 ) ) ;
#65489=DIRECTION ( 'NONE',  ( 0.000000000000000000, 0.000000000000000000, 1.000000000000000000 ) ) ;
#65497=CARTESIAN_POINT ( 'NONE',  ( 10.00000000000000000, -37.16516213103280108, 4.992566952384862589 ) ) ;
#65505=CIRCLE ( 'NONE', #42686, 16.00000000000000000 ) ;
#65506=VECTOR ( 'NONE', #1731, 1000.000000000000000 ) ;
#65523=ORIENTED_EDGE ( 'NONE', *, *, #7714, .T. ) ;
#65539=DIRECTION ( 'NONE',  ( 0.000000000000000000, -0.6691306063588577935, -0.7431448254773946882 ) ) ;
#65552=CARTESIAN_POINT ( 'NONE',  ( 0.000000000000000000, -21.53537804866058991, -30.80686688397033635 ) ) ;
#65553=AXIS2_PLACEMENT_3D ( 'NONE', #39982, #46730, #41097 ) ;
#65555=LINE ( 'NONE', #14029, #50199 ) ;
#65558=EDGE_CURVE ( 'NONE', #64952, #70364, #50576, .T. ) ;
#65562=VECTOR ( 'NONE', #23451, 1000.000000000000000 ) ;
#65567=CIRCLE ( 'NONE', #29472, 42.00000000000000000 ) ;
#65568=VECTOR ( 'NONE', #53028, 1000.000000000000000 ) ;
#65583=FACE_OUTER_BOUND ( 'NONE', #124, .T. ) ;
#65598=DIRECTION ( 'NONE',  ( 0.000000000000000000, 0.4539904997395412534, 0.8910065241883706744 ) ) ;
#65600=EDGE_LOOP ( 'NONE', ( #51018, #19311, #6840, #50010 ) ) ;
#65602=EDGE_CURVE ( 'NONE', #42918, #66947, #33793, .T. ) ;
#65611=ORIENTED_EDGE ( 'NONE', *, *, #4159, .F. ) ;
#65618=DIRECTION ( 'NONE',  ( 0.000000000000000000, 0.8090169943749445647, 0.5877852522924770229 ) ) ;
#65624=VECTOR ( 'NONE', #19543, 1000.000000000000227 ) ;
#65638=ADVANCED_FACE ( 'NONE', ( #17231 ), #7052, .T. ) ;
#65639=CARTESIAN_POINT ( 'NONE',  ( -3.000000000000000000, -4.261787119645322974, 26.19803753235774835 ) ) ;
#65646=DIRECTION ( 'NONE',  ( -1.000000000000000000, 0.000000000000000000, 0.000000000000000000 ) ) ;
#65647=DIRECTION ( 'NONE',  ( 0.000000000000000000, 0.000000000000000000, 1.000000000000000000 ) ) ;
#65648=CARTESIAN_POINT ( 'NONE',  ( 10.00000000000000000, 33.17418723428307459, 17.67226234102837878 ) ) ;
#65654=ORIENTED_EDGE ( 'NONE', *, *, #13987, .T. ) ;
#65656=EDGE_LOOP ( 'NONE', ( #3456, #15804, #26267, #7061 ) ) ;
#65657=EDGE_LOOP ( 'NONE', ( #72290, #67788, #65105, #51138 ) ) ;
#65664=LINE ( 'NONE', #14519, #11551 ) ;
#65665=ORIENTED_EDGE ( 'NONE', *, *, #3350, .F. ) ;
#65684=VECTOR ( 'NONE', #40872, 1000.000000000000000 ) ;
#65689=ADVANCED_FACE ( 'NONE', ( #69470 ), #35260, .T. ) ;
#65723=DIRECTION ( 'NONE',  ( 0.000000000000000000, -0.8660254037844363761, -0.5000000000000039968 ) ) ;
#65724=ADVANCED_FACE ( 'NONE', ( #7794 ), #2930, .T. ) ;
#65735=PRESENTATION_STYLE_ASSIGNMENT (( #31139 ) ) ;
#65743=DIRECTION ( 'NONE',  ( 0.000000000000000000, 0.2079116908177525702, 0.9781476007338071321 ) ) ;
#65751=ORIENTED_EDGE ( 'NONE', *, *, #56204, .T. ) ;
#65767=EDGE_CURVE ( 'NONE', #51229, #22980, #43139, .T. ) ;
#65773=CARTESIAN_POINT ( 'NONE',  ( 4.999999999999999112, 41.81611651403868990, -3.925862922255709542 ) ) ;
#65777=VERTEX_POINT ( 'NONE', #20174 ) ;
#65788=DIRECTION ( 'NONE',  ( -1.000000000000000000, -0.000000000000000000, -0.000000000000000000 ) ) ;
#65798=CARTESIAN_POINT ( 'NONE',  ( -3.000000000000000000, 16.61724383029390140, -20.69703378468903665 ) ) ;
#65822=DIRECTION ( 'NONE',  ( 0.000000000000000000, 0.000000000000000000, -1.000000000000000000 ) ) ;
#65834=EDGE_LOOP ( 'NONE', ( #39667, #37668, #35985, #51148 ) ) ;
#65841=VECTOR ( 'NONE', #12801, 1000.000000000000000 ) ;
#65847=ORIENTED_EDGE ( 'NONE', *, *, #55749, .T. ) ;
#65848=EDGE_CURVE ( 'NONE', #22283, #63788, #64953, .T. ) ;
#65849=EDGE_LOOP ( 'NONE', ( #40078, #73027, #40035, #6426 ) ) ;
#65861=EDGE_LOOP ( 'NONE', ( #12768, #49646, #52983, #52171 ) ) ;
#65885=CIRCLE ( 'NONE', #5893, 16.00000000000000000 ) ;
#65887=DIRECTION ( 'NONE',  ( 0.000000000000000000, 0.000000000000000000, 1.000000000000000000 ) ) ;
#65893=DIRECTION ( 'NONE',  ( -1.000000000000000000, -0.000000000000000000, 0.000000000000000000 ) ) ;
#65914=LINE ( 'NONE', #44078, #34636 ) ;
#65947=ORIENTED_EDGE ( 'NONE', *, *, #48876, .T. ) ;
#65993=LINE ( 'NONE', #71223, #720 ) ;
#65995=EDGE_CURVE ( 'NONE', #56884, #29668, #32191, .T. ) ;
#66001=CYLINDRICAL_SURFACE ( 'NONE', #67408, 42.00000000000000000 ) ;
#66007=VERTEX_POINT ( 'NONE', #67811 ) ;
#66011=AXIS2_PLACEMENT_3D ( 'NONE', #29491, #47175, #35517 ) ;
#66019=VERTEX_POINT ( 'NONE', #62177 ) ;
#66020=DIRECTION ( 'NONE',  ( -1.000000000000000000, -0.000000000000000000, 0.000000000000000000 ) ) ;
#66033=ADVANCED_FACE ( 'NONE', ( #56914 ), #28316, .T. ) ;
#66037=ORIENTED_EDGE ( 'NONE', *, *, #58219, .F. ) ;
#66039=CYLINDRICAL_SURFACE ( 'NONE', #63461, 16.00000000000000000 ) ;
#66042=CARTESIAN_POINT ( 'NONE',  ( 0.000000000000000000, 0.000000000000000000, 0.000000000000000000 ) ) ;
#66051=EDGE_LOOP ( 'NONE', ( #39673, #49255, #55195, #7390 ) ) ;
#66053=EDGE_CURVE ( 'NONE', #33537, #11359, #59493, .T. ) ;
#66058=CARTESIAN_POINT ( 'NONE',  ( 10.00000000000000000, 10.96151621346487914, 35.95386929396260456 ) ) ;
#66063=LINE ( 'NONE', #7789, #48325 ) ;
#66072=VECTOR ( 'NONE', #28634, 1000.000000000000000 ) ;
#66080=ORIENTED_EDGE ( 'NONE', *, *, #43997, .F. ) ;
#66100=CARTESIAN_POINT ( 'NONE',  ( 10.00000000000000000, -35.47612816024506088, -22.48208911017539435 ) ) ;
#66101=ORIENTED_EDGE ( 'NONE', *, *, #43379, .T. ) ;
#66115=CARTESIAN_POINT ( 'NONE',  ( 0.000000000000000000, 35.53030884539102630, -12.26510123303222599 ) ) ;
#66145=VERTEX_POINT ( 'NONE', #29416 ) ;
#66147=ORIENTED_EDGE ( 'NONE', *, *, #26837, .F. ) ;
#66156=EDGE_LOOP ( 'NONE', ( #67911, #58183, #60425, #26422 ) ) ;
#66166=PLANE ( 'NONE',  #57200 ) ;
#66195=EDGE_CURVE ( 'NONE', #68891, #68659, #2016, .T. ) ;
#66197=DIRECTION ( 'NONE',  ( -1.000000000000000000, 0.000000000000000000, 0.000000000000000000 ) ) ;
#66199=VECTOR ( 'NONE', #47279, 1000.000000000000000 ) ;
#66201=VERTEX_POINT ( 'NONE', #48579 ) ;
#66211=VECTOR ( 'NONE', #538, 1000.000000000000000 ) ;
#66213=AXIS2_PLACEMENT_3D ( 'NONE', #38306, #61247, #73617 ) ;
#66216=LINE ( 'NONE', #3440, #50896 ) ;
#66237=DIRECTION ( 'NONE',  ( 0.000000000000000000, 0.000000000000000000, 1.000000000000000000 ) ) ;
#66247=CARTESIAN_POINT ( 'NONE',  ( 5.000000000000000000, 26.79245525562762253, -32.34446384429941901 ) ) ;
#66251=CARTESIAN_POINT ( 'NONE',  ( -3.000000000000000000, 8.688484142253939169, 21.88630264137371029 ) ) ;
#66252=DIRECTION ( 'NONE',  ( -1.000000000000000000, 0.000000000000000000, -0.000000000000000000 ) ) ;
#66258=DIRECTION ( 'NONE',  ( 0.000000000000000000, -0.1045284632676578424, 0.9945218953682729568 ) ) ;
#66262=DIRECTION ( 'NONE',  ( 0.000000000000000000, 0.1564344650402311743, -0.9876883405951377704 ) ) ;
#66280=EDGE_CURVE ( 'NONE', #54186, #73246, #31645, .T. ) ;
#66292=EDGE_LOOP ( 'NONE', ( #72103, #41519, #57701, #40600 ) ) ;
#66312=CARTESIAN_POINT ( 'NONE',  ( 10.00000000000000000, 10.74501242461282757, 35.92658777277515014 ) ) ;
#66313=EDGE_CURVE ( 'NONE', #47006, #25402, #61927, .T. ) ;
#66315=ORIENTED_EDGE ( 'NONE', *, *, #10954, .F. ) ;
#66319=CIRCLE ( 'NONE', #61544, 16.00000000000000000 ) ;
#66333=EDGE_CURVE ( 'NONE', #46613, #23253, #72593, .T. ) ;
#66340=DIRECTION ( 'NONE',  ( -1.000000000000000000, -0.000000000000000000, 0.000000000000000000 ) ) ;
#66359=DIRECTION ( 'NONE',  ( 1.000000000000000000, -0.000000000000000000, -0.000000000000000000 ) ) ;
#66362=DIRECTION ( 'NONE',  ( 1.000000000000000000, 0.000000000000000000, -0.000000000000000000 ) ) ;
#66365=FACE_OUTER_BOUND ( 'NONE', #71562, .T. ) ;
#66374=DIRECTION ( 'NONE',  ( -1.000000000000000000, 0.000000000000000000, 0.000000000000000000 ) ) ;
#66389=DIRECTION ( 'NONE',  ( 0.000000000000000000, 0.000000000000000000, 1.000000000000000000 ) ) ;
#66402=VERTEX_POINT ( 'NONE', #28229 ) ;
#66413=CARTESIAN_POINT ( 'NONE',  ( 10.00000000000000000, -25.88420570971381807, -27.13269053701123212 ) ) ;
#66425=LINE ( 'NONE', #18408, #46230 ) ;
#66440=ORIENTED_EDGE ( 'NONE', *, *, #18565, .F. ) ;
#66442=FACE_BOUND ( 'NONE', #11641, .T. ) ;
#66459=EDGE_CURVE ( 'NONE', #35679, #17553, #36736, .T. ) ;
#66461=CARTESIAN_POINT ( 'NONE',  ( -3.000000000000000000, 24.81905959214275370, -9.408202855044498492 ) ) ;
#66477=CARTESIAN_POINT ( 'NONE',  ( 0.000000000000000000, 0.000000000000000000, 0.000000000000000000 ) ) ;
#66483=ORIENTED_EDGE ( 'NONE', *, *, #476, .F. ) ;
#66504=ORIENTED_EDGE ( 'NONE', *, *, #24141, .T. ) ;
#66505=AXIS2_PLACEMENT_3D ( 'NONE', #38430, #4610, #27513 ) ;
#66514=VERTEX_POINT ( 'NONE', #27861 ) ;
#66527=LINE ( 'NONE', #37222, #25944 ) ;
#66537=CARTESIAN_POINT ( 'NONE',  ( 10.00000000000000000, 0.000000000000000000, 0.000000000000000000 ) ) ;
#66538=FACE_OUTER_BOUND ( 'NONE', #9426, .T. ) ;
#66562=EDGE_CURVE ( 'NONE', #17707, #62140, #16349, .T. ) ;
#66569=ORIENTED_EDGE ( 'NONE', *, *, #5057, .T. ) ;
#66571=ORIENTED_EDGE ( 'NONE', *, *, #41400, .F. ) ;
#66573=EDGE_LOOP ( 'NONE', ( #56319, #19124, #71839, #37829 ) ) ;
#66577=ORIENTED_EDGE ( 'NONE', *, *, #69005, .T. ) ;
#66579=AXIS2_PLACEMENT_3D ( 'NONE', #65437, #42136, #30092 ) ;
#66581=CARTESIAN_POINT ( 'NONE',  ( 10.00000000000000000, 41.81611651403867569, -3.925862922255714871 ) ) ;
#66583=ORIENTED_EDGE ( 'NONE', *, *, #37863, .F. ) ;
#66598=DIRECTION ( 'NONE',  ( -1.000000000000000000, -0.000000000000000000, -0.000000000000000000 ) ) ;
#66601=EDGE_LOOP ( 'NONE', ( #51043, #20844, #56425, #19507 ) ) ;
#66610=DIRECTION ( 'NONE',  ( 0.000000000000000000, 0.000000000000000000, -1.000000000000000000 ) ) ;
#66617=EDGE_CURVE ( 'NONE', #15277, #55743, #18792, .T. ) ;
#66622=FACE_OUTER_BOUND ( 'NONE', #20640, .T. ) ;
#66623=DIRECTION ( 'NONE',  ( -1.000000000000000000, 0.000000000000000000, -0.000000000000000000 ) ) ;
#66625=ORIENTED_EDGE ( 'NONE', *, *, #60609, .T. ) ;
#66629=EDGE_CURVE ( 'NONE', #31252, #72829, #23546, .T. ) ;
#66638=ADVANCED_FACE ( 'NONE', ( #41376 ), #24448, .T. ) ;
#66644=DIRECTION ( 'NONE',  ( 0.000000000000000000, 0.1045284632676448111, 0.9945218953682742891 ) ) ;
#66656=EDGE_CURVE ( 'NONE', #13671, #31995, #30080, .T. ) ;
#66670=LINE ( 'NONE', #61023, #40 ) ;
#66709=ADVANCED_FACE ( 'NONE', ( #1562 ), #47386, .T. ) ;
#66722=CARTESIAN_POINT ( 'NONE',  ( -3.000000000000000000, -18.13022148937243472, -15.02647892043568767 ) ) ;
#66727=EDGE_CURVE ( 'NONE', #16859, #27537, #19928, .T. ) ;
#66728=EDGE_CURVE ( 'NONE', #55130, #56682, #66527, .T. ) ;
#66745=CARTESIAN_POINT ( 'NONE',  ( 0.000000000000000000, -20.55727247249748046, 16.78983467731285018 ) ) ;
#66746=EDGE_LOOP ( 'NONE', ( #22184, #63971, #51824, #37019 ) ) ;
#66748=ORIENTED_EDGE ( 'NONE', *, *, #21222, .T. ) ;
#66769=ORIENTED_EDGE ( 'NONE', *, *, #35882, .F. ) ;
#66772=CARTESIAN_POINT ( 'NONE',  ( 0.000000000000000000, 16.65560815589464028, -38.55633173626993226 ) ) ;
#66783=ORIENTED_EDGE ( 'NONE', *, *, #1042, .F. ) ;
#66784=DIRECTION ( 'NONE',  ( 0.000000000000000000, 0.000000000000000000, 1.000000000000000000 ) ) ;
#66787=EDGE_CURVE ( 'NONE', #37478, #12484, #73976, .T. ) ;
#66802=FACE_OUTER_BOUND ( 'NONE', #14193, .T. ) ;
#66806=FACE_BOUND ( 'NONE', #49465, .T. ) ;
#66815=CARTESIAN_POINT ( 'NONE',  ( 10.00000000000000000, 2.663952781846733675, -41.91543099594814947 ) ) ;
#66817=ADVANCED_FACE ( 'NONE', ( #8262 ), #66166, .F. ) ;
#66818=CARTESIAN_POINT ( 'NONE',  ( 5.000000000000000000, 27.75498641678786527, -31.52238457039571173 ) ) ;
#66819=ORIENTED_EDGE ( 'NONE', *, *, #1042, .T. ) ;
#66823=CARTESIAN_POINT ( 'NONE',  ( 10.00000000000000000, 0.000000000000000000, 0.000000000000000000 ) ) ;
#66826=VERTEX_POINT ( 'NONE', #4130 ) ;
#66836=AXIS2_PLACEMENT_3D ( 'NONE', #54877, #36843, #2682 ) ;
#66848=VERTEX_POINT ( 'NONE', #4880 ) ;
#66856=ORIENTED_EDGE ( 'NONE', *, *, #61748, .T. ) ;
#66865=ORIENTED_EDGE ( 'NONE', *, *, #74327, .F. ) ;
#66879=VERTEX_POINT ( 'NONE', #62767 ) ;
#66895=EDGE_CURVE ( 'NONE', #32355, #35859, #32665, .T. ) ;
#66909=CARTESIAN_POINT ( 'NONE',  ( 10.00000000000000000, -21.32104025579091910, -30.84782396557241313 ) ) ;
#66919=AXIS2_PLACEMENT_3D ( 'NONE', #55142, #3673, #9656 ) ;
#66924=CARTESIAN_POINT ( 'NONE',  ( 0.000000000000000000, -21.32104025579091910, -30.84782396557241313 ) ) ;
#66931=AXIS2_PLACEMENT_3D ( 'NONE', #3224, #71601, #65618 ) ;
#66933=CARTESIAN_POINT ( 'NONE',  ( 0.000000000000000000, 10.41901085202135491, -40.68715046381917944 ) ) ;
#66937=ORIENTED_EDGE ( 'NONE', *, *, #72449, .F. ) ;
#66947=VERTEX_POINT ( 'NONE', #15373 ) ;
#66948=ORIENTED_EDGE ( 'NONE', *, *, #44389, .F. ) ;
#66951=CARTESIAN_POINT ( 'NONE',  ( 0.000000000000000000, 6.762365576493310826, 25.66652317338401090 ) ) ;
#66952=DIRECTION ( 'NONE',  ( 0.000000000000000000, -0.9510565162951500895, -0.3090169943749581649 ) ) ;
#66960=CYLINDRICAL_SURFACE ( 'NONE', #45545, 16.00000000000000000 ) ;
#66961=CARTESIAN_POINT ( 'NONE',  ( 10.00000000000000000, 33.17418723428307459, 17.67226234102837878 ) ) ;
#66970=EDGE_LOOP ( 'NONE', ( #29947, #60229, #32337, #56801 ) ) ;
#66973=PLANE ( 'NONE',  #19495 ) ;
#66978=CARTESIAN_POINT ( 'NONE',  ( 10.00000000000000000, 0.000000000000000000, 0.000000000000000000 ) ) ;
#66986=CARTESIAN_POINT ( 'NONE',  ( -3.000000000000000000, 22.07842321921481243, 8.187992925817422218 ) ) ;
#66996=CARTESIAN_POINT ( 'NONE',  ( 10.00000000000000000, -36.88895765772628010, -6.736453364083947015 ) ) ;
#67004=VERTEX_POINT ( 'NONE', #16501 ) ;
#67018=VERTEX_POINT ( 'NONE', #24365 ) ;
#67019=EDGE_CURVE ( 'NONE', #44110, #42446, #17614, .T. ) ;
#67023=ORIENTED_EDGE ( 'NONE', *, *, #54518, .F. ) ;
#67027=CIRCLE ( 'NONE', #62221, 16.00000000000000000 ) ;
#67029=AXIS2_PLACEMENT_3D ( 'NONE', #18260, #41202, #12613 ) ;
#67030=VERTEX_POINT ( 'NONE', #17982 ) ;
#67044=CARTESIAN_POINT ( 'NONE',  ( 10.00000000000000000, 0.000000000000000000, 0.000000000000000000 ) ) ;
#67055=DIRECTION ( 'NONE',  ( 0.000000000000000000, -0.5877852522924797984, 0.8090169943749426773 ) ) ;
#67056=LINE ( 'NONE', #38862, #12674 ) ;
#67059=CARTESIAN_POINT ( 'NONE',  ( 10.00000000000000000, -22.48208911017474065, -35.47612816024548721 ) ) ;
#67062=LINE ( 'NONE', #32474, #11998 ) ;
#67067=CIRCLE ( 'NONE', #34650, 37.49900000000001654 ) ;
#67078=EDGE_CURVE ( 'NONE', #13867, #16540, #46556, .T. ) ;
#67082=DIRECTION ( 'NONE',  ( 0.000000000000000000, -0.8090169943749422332, -0.5877852522924803536 ) ) ;
#67086=PLANE ( 'NONE',  #69775 ) ;
#67088=CIRCLE ( 'NONE', #62445, 16.00000000000000000 ) ;
#67099=AXIS2_PLACEMENT_3D ( 'NONE', #1572, #60172, #41743 ) ;
#67100=VECTOR ( 'NONE', #32319, 1000.000000000000000 ) ;
#67112=VERTEX_POINT ( 'NONE', #70203 ) ;
#67114=EDGE_CURVE ( 'NONE', #53177, #17752, #36779, .T. ) ;
#67118=EDGE_CURVE ( 'NONE', #68543, #20059, #71432, .T. ) ;
#67119=CARTESIAN_POINT ( 'NONE',  ( 10.00000000000000000, 0.000000000000000000, 0.000000000000000000 ) ) ;
#67121=CARTESIAN_POINT ( 'NONE',  ( 0.000000000000000000, -37.22597642581161637, 5.202137450156258502 ) ) ;
#67130=DIRECTION ( 'NONE',  ( 0.000000000000000000, 1.000000000000000000, 7.228014483236689653E-16 ) ) ;
#67143=ORIENTED_EDGE ( 'NONE', *, *, #44597, .T. ) ;
#67146=EDGE_LOOP ( 'NONE', ( #8402, #15806, #29180, #21520 ) ) ;
#67165=ADVANCED_FACE ( 'NONE', ( #63490 ), #11967, .F. ) ;
#67169=ORIENTED_EDGE ( 'NONE', *, *, #2702, .T. ) ;
#67170=DIRECTION ( 'NONE',  ( -1.000000000000000000, 0.000000000000000000, 0.000000000000000000 ) ) ;
#67180=CARTESIAN_POINT ( 'NONE',  ( 10.00000000000000000, 26.08949754953024325, 27.05870788708241648 ) ) ;
#67188=CARTESIAN_POINT ( 'NONE',  ( 5.000000000000000000, 32.34446384430010113, -26.79245525562679831 ) ) ;
#67194=ADVANCED_FACE ( 'NONE', ( #55145 ), #70564, .T. ) ;
#67207=VERTEX_POINT ( 'NONE', #2209 ) ;
#67231=PLANE ( 'NONE',  #52747 ) ;
#67249=ORIENTED_EDGE ( 'NONE', *, *, #20644, .F. ) ;
#67258=ORIENTED_EDGE ( 'NONE', *, *, #48973, .F. ) ;
#67264=EDGE_CURVE ( 'NONE', #24766, #46530, #67864, .T. ) ;
#67273=DIRECTION ( 'NONE',  ( -1.000000000000000000, 0.000000000000000000, -0.000000000000000000 ) ) ;
#67275=DIRECTION ( 'NONE',  ( 0.000000000000000000, 0.000000000000000000, 1.000000000000000000 ) ) ;
#67303=EDGE_LOOP ( 'NONE', ( #39552, #24538, #26335, #34768 ) ) ;
#67333=VECTOR ( 'NONE', #14940, 1000.000000000000000 ) ;
#67334=DIRECTION ( 'NONE',  ( -1.000000000000000000, 0.000000000000000000, 0.000000000000000000 ) ) ;
#67336=ORIENTED_EDGE ( 'NONE', *, *, #16990, .T. ) ;
#67343=CARTESIAN_POINT ( 'NONE',  ( 0.000000000000000000, -5.202137450156129717, -37.22597642581163768 ) ) ;
#67355=DIRECTION ( 'NONE',  ( 0.000000000000000000, 0.000000000000000000, 1.000000000000000000 ) ) ;
#67356=FACE_OUTER_BOUND ( 'NONE', #59182, .T. ) ;
#67374=DIRECTION ( 'NONE',  ( 0.000000000000000000, 0.000000000000000000, 1.000000000000000000 ) ) ;
#67408=AXIS2_PLACEMENT_3D ( 'NONE', #14845, #32122, #37791 ) ;
#67413=ORIENTED_EDGE ( 'NONE', *, *, #41582, .T. ) ;
#67438=AXIS2_PLACEMENT_3D ( 'NONE', #6071, #56822, #68844 ) ;
#67442=VERTEX_POINT ( 'NONE', #61172 ) ;
#67474=DIRECTION ( 'NONE',  ( -1.000000000000000000, -0.000000000000000000, 0.000000000000000000 ) ) ;
#67482=VERTEX_POINT ( 'NONE', #35181 ) ;
#67494=ADVANCED_FACE ( 'NONE', ( #57753 ), #63773, .T. ) ;
#67530=CARTESIAN_POINT ( 'NONE',  ( 10.00000000000000000, 0.000000000000000000, 0.000000000000000000 ) ) ;
#67531=DIRECTION ( 'NONE',  ( 0.000000000000000000, 1.000000000000000000, 3.491481338843133750E-15 ) ) ;
#67547=CIRCLE ( 'NONE', #53162, 16.00000000000000000 ) ;
#67548=FACE_BOUND ( 'NONE', #72096, .T. ) ;
#67573=DIRECTION ( 'NONE',  ( 0.000000000000000000, 0.000000000000000000, 1.000000000000000000 ) ) ;
#67576=AXIS2_PLACEMENT_3D ( 'NONE', #31712, #57318, #23117 ) ;
#67586=EDGE_CURVE ( 'NONE', #60556, #62067, #49872, .T. ) ;
#67595=CIRCLE ( 'NONE', #35183, 37.49900000000000233 ) ;
#67624=ADVANCED_FACE ( 'NONE', ( #18257 ), #280, .T. ) ;
#67640=LINE ( 'NONE', #33406, #45820 ) ;
#67656=AXIS2_PLACEMENT_3D ( 'NONE', #39736, #16045, #68304 ) ;
#67660=EDGE_CURVE ( 'NONE', #56288, #12067, #65993, .T. ) ;
#67661=DIRECTION ( 'NONE',  ( 0.000000000000000000, 0.000000000000000000, 1.000000000000000000 ) ) ;
#67669=VERTEX_POINT ( 'NONE', #8086 ) ;
#67670=ORIENTED_EDGE ( 'NONE', *, *, #8987, .T. ) ;
#67678=ORIENTED_EDGE ( 'NONE', *, *, #23673, .T. ) ;
#67687=DIRECTION ( 'NONE',  ( -1.000000000000000000, -0.000000000000000000, -0.000000000000000000 ) ) ;
#67688=VERTEX_POINT ( 'NONE', #65246 ) ;
#67691=ORIENTED_EDGE ( 'NONE', *, *, #36598, .T. ) ;
#67701=AXIS2_PLACEMENT_3D ( 'NONE', #12435, #39540, #23721 ) ;
#67710=ORIENTED_EDGE ( 'NONE', *, *, #56940, .T. ) ;
#67724=DIRECTION ( 'NONE',  ( 0.000000000000000000, 0.7431448254773960205, -0.6691306063588563502 ) ) ;
#67738=DIRECTION ( 'NONE',  ( 1.000000000000000000, 0.000000000000000000, -0.000000000000000000 ) ) ;
#67759=UNCERTAINTY_MEASURE_WITH_UNIT (LENGTH_MEASURE( 1.000000000000000082E-05 ), #52252, 'distance_accuracy_value', 'NONE');
#67760=DIRECTION ( 'NONE',  ( -1.000000000000000000, 0.000000000000000000, -0.000000000000000000 ) ) ;
#67788=ORIENTED_EDGE ( 'NONE', *, *, #5064, .F. ) ;
#67795=CYLINDRICAL_SURFACE ( 'NONE', #12786, 42.00000000000000000 ) ;
#67797=CARTESIAN_POINT ( 'NONE',  ( -3.000000000000000000, -23.29833615347104825, -3.418703333116803744 ) ) ;
#67800=VERTEX_POINT ( 'NONE', #64874 ) ;
#67806=CARTESIAN_POINT ( 'NONE',  ( 10.00000000000000000, -37.58145647212453611, -0.6853352020794456489 ) ) ;
#67811=CARTESIAN_POINT ( 'NONE',  ( 0.000000000000000000, 22.74946021919175720, -29.81001611430984255 ) ) ;
#67814=ORIENTED_EDGE ( 'NONE', *, *, #57044, .F. ) ;
#67823=DIRECTION ( 'NONE',  ( 0.000000000000000000, 0.000000000000000000, 1.000000000000000000 ) ) ;
#67833=DIRECTION ( 'NONE',  ( 0.000000000000000000, -0.1564344650402382242, 0.9876883405951366601 ) ) ;
#67839=ADVANCED_FACE ( 'NONE', ( #49420 ), #49780, .T. ) ;
#67845=LINE ( 'NONE', #27979, #54493 ) ;
#67855=VERTEX_POINT ( 'NONE', #55808 ) ;
#67864=CIRCLE ( 'NONE', #39054, 16.00000000000000355 ) ;
#67868=CARTESIAN_POINT ( 'NONE',  ( 5.000000000000000000, 35.47612816024523852, 22.48208911017513145 ) ) ;
#67873=AXIS2_PLACEMENT_3D ( 'NONE', #16392, #56633, #45731 ) ;
#67880=DIRECTION ( 'NONE',  ( 0.000000000000000000, 0.3090169943749480619, -0.9510565162951533091 ) ) ;
#67883=FACE_OUTER_BOUND ( 'NONE', #55765, .T. ) ;
#67887=VERTEX_POINT ( 'NONE', #44909 ) ;
#67902=CYLINDRICAL_SURFACE ( 'NONE', #67873, 37.49900000000000233 ) ;
#67909=VERTEX_POINT ( 'NONE', #22338 ) ;
#67911=ORIENTED_EDGE ( 'NONE', *, *, #18354, .T. ) ;
#67913=CYLINDRICAL_SURFACE ( 'NONE', #6572, 16.00000000000000000 ) ;
#67920=ORIENTED_EDGE ( 'NONE', *, *, #32976, .F. ) ;
#67923=FACE_BOUND ( 'NONE', #45888, .T. ) ;
#67947=PLANE ( 'NONE',  #56403 ) ;
#67961=ORIENTED_EDGE ( 'NONE', *, *, #51348, .T. ) ;
#67971=DIRECTION ( 'NONE',  ( -1.000000000000000000, 0.000000000000000000, 0.000000000000000000 ) ) ;
#67975=VERTEX_POINT ( 'NONE', #46380 ) ;
#67979=AXIS2_PLACEMENT_3D ( 'NONE', #13532, #24816, #64311 ) ;
#67997=CARTESIAN_POINT ( 'NONE',  ( -3.000000000000000000, -23.29833615347104825, -3.418703333116803744 ) ) ;
#67998=CARTESIAN_POINT ( 'NONE',  ( 0.000000000000000000, 32.34446384430010113, -26.79245525562679831 ) ) ;
#68003=EDGE_CURVE ( 'NONE', #31034, #14108, #40365, .T. ) ;
#68015=LINE ( 'NONE', #37957, #42866 ) ;
#68023=CYLINDRICAL_SURFACE ( 'NONE', #60102, 16.00000000000000000 ) ;
#68031=PRODUCT ( 'fast gear_ISO - Spur gear 2M 40T 20PA 10FW ---S40A75H50L38.0N', 'fast gear_ISO - Spur gear 2M 40T 20PA 10FW ---S40A75H50L38.0N', '', ( #39966 ) ) ;
#68033=VERTEX_POINT ( 'NONE', #18173 ) ;
#68039=ORIENTED_EDGE ( 'NONE', *, *, #28931, .T. ) ;
#68059=ORIENTED_EDGE ( 'NONE', *, *, #66459, .F. ) ;
#68071=ORIENTED_EDGE ( 'NONE', *, *, #7634, .F. ) ;
#68072=VERTEX_POINT ( 'NONE', #5803 ) ;
#68103=DIRECTION ( 'NONE',  ( 0.000000000000000000, 0.000000000000000000, 1.000000000000000000 ) ) ;
#68105=EDGE_CURVE ( 'NONE', #10838, #57712, #31567, .T. ) ;
#68117=AXIS2_PLACEMENT_3D ( 'NONE', #7622, #73539, #5152 ) ;
#68120=CARTESIAN_POINT ( 'NONE',  ( 10.00000000000000000, 0.000000000000000000, 0.000000000000000000 ) ) ;
#68134=CARTESIAN_POINT ( 'NONE',  ( 10.00000000000000000, 0.000000000000000000, 0.000000000000000000 ) ) ;
#68136=DIRECTION ( 'NONE',  ( -0.000000000000000000, 0.8660254037844368202, 0.5000000000000031086 ) ) ;
#68141=ORIENTED_EDGE ( 'NONE', *, *, #19318, .F. ) ;
#68155=EDGE_CURVE ( 'NONE', #55889, #18738, #49232, .T. ) ;
#68172=ORIENTED_EDGE ( 'NONE', *, *, #29780, .T. ) ;
#68173=LINE ( 'NONE', #16300, #71851 ) ;
#68176=EDGE_CURVE ( 'NONE', #47415, #43524, #60897, .T. ) ;
#68189=ORIENTED_EDGE ( 'NONE', *, *, #3686, .T. ) ;
#68193=EDGE_CURVE ( 'NONE', #1816, #9559, #12790, .T. ) ;
#68196=LINE ( 'NONE', #10306, #23111 ) ;
#68221=CARTESIAN_POINT ( 'NONE',  ( 10.00000000000000000, 12.26510123303308752, -35.53030884539072787 ) ) ;
#68225=DIRECTION ( 'NONE',  ( 0.000000000000000000, 0.000000000000000000, 1.000000000000000000 ) ) ;
#68228=FACE_OUTER_BOUND ( 'NONE', #7792, .T. ) ;
#68232=ADVANCED_FACE ( 'NONE', ( #48500 ), #71412, .F. ) ;
#68250=ORIENTED_EDGE ( 'NONE', *, *, #19318, .T. ) ;
#68251=ORIENTED_EDGE ( 'NONE', *, *, #12913, .F. ) ;
#68257=CIRCLE ( 'NONE', #16616, 16.00000000000000000 ) ;
#68258=CARTESIAN_POINT ( 'NONE',  ( -3.000000000000000000, 0.000000000000000000, 0.000000000000000000 ) ) ;
#68260=VECTOR ( 'NONE', #68136, 999.9999999999998863 ) ;
#68287=DIRECTION ( 'NONE',  ( -1.000000000000000000, 0.000000000000000000, 0.000000000000000000 ) ) ;
#68294=ORIENTED_EDGE ( 'NONE', *, *, #31789, .F. ) ;
#68304=DIRECTION ( 'NONE',  ( 0.000000000000000000, -0.7431448254773862505, -0.6691306063588671194 ) ) ;
#68309=AXIS2_PLACEMENT_3D ( 'NONE', #3207, #26096, #49026 ) ;
#68317=VECTOR ( 'NONE', #72264, 1000.000000000000000 ) ;
#68340=VECTOR ( 'NONE', #17629, 1000.000000000000000 ) ;
#68369=CARTESIAN_POINT ( 'NONE',  ( -3.000000000000000000, 26.50000000000000000, -1.500000000000001332 ) ) ;
#68395=CARTESIAN_POINT ( 'NONE',  ( 10.00000000000000000, 37.22597642581150268, 5.202137450157037435 ) ) ;
#68399=DIRECTION ( 'NONE',  ( -1.000000000000000000, 0.000000000000000000, -0.000000000000000000 ) ) ;
#68404=CARTESIAN_POINT ( 'NONE',  ( 10.00000000000000000, -16.45098606841149902, 33.79645857604508308 ) ) ;
#68411=EDGE_CURVE ( 'NONE', #56682, #27079, #65664, .T. ) ;
#68415=DIRECTION ( 'NONE',  ( 0.000000000000000000, 0.000000000000000000, 1.000000000000000000 ) ) ;
#68417=FACE_OUTER_BOUND ( 'NONE', #9494, .T. ) ;
#68418=EDGE_CURVE ( 'NONE', #65777, #17753, #4005, .T. ) ;
#68427=CIRCLE ( 'NONE', #17970, 37.49900000000000233 ) ;
#68428=DIRECTION ( 'NONE',  ( -1.000000000000000000, -0.000000000000000000, 0.000000000000000000 ) ) ;
#68432=EDGE_CURVE ( 'NONE', #4640, #26852, #9988, .T. ) ;
#68440=VERTEX_POINT ( 'NONE', #37090 ) ;
#68443=ORIENTED_EDGE ( 'NONE', *, *, #33243, .F. ) ;
#68473=CIRCLE ( 'NONE', #42059, 37.49900000000001654 ) ;
#68475=DIRECTION ( 'NONE',  ( 0.000000000000000000, 0.1564344650402243742, 0.9876883405951387696 ) ) ;
#68479=DIRECTION ( 'NONE',  ( -1.000000000000000000, 0.000000000000000000, 0.000000000000000000 ) ) ;
#68495=EDGE_CURVE ( 'NONE', #27109, #39671, #20539, .T. ) ;
#68499=CYLINDRICAL_SURFACE ( 'NONE', #22708, 37.49900000000000233 ) ;
#68500=LINE ( 'NONE', #39931, #50242 ) ;
#68504=EDGE_CURVE ( 'NONE', #29668, #60926, #74026, .T. ) ;
#68507=AXIS2_PLACEMENT_3D ( 'NONE', #70928, #19430, #25451 ) ;
#68522=VECTOR ( 'NONE', #24887, 1000.000000000000000 ) ;
#68537=CARTESIAN_POINT ( 'NONE',  ( 0.000000000000000000, -22.64427369931191336, 30.00120703465197280 ) ) ;
#68540=ORIENTED_EDGE ( 'NONE', *, *, #68693, .F. ) ;
#68543=VERTEX_POINT ( 'NONE', #71655 ) ;
#68564=CIRCLE ( 'NONE', #2583, 42.00000000000000000 ) ;
#68567=CIRCLE ( 'NONE', #12086, 16.00000000000000000 ) ;
#68568=DIRECTION ( 'NONE',  ( -1.000000000000000000, 0.000000000000000000, -0.000000000000000000 ) ) ;
#68570=ORIENTED_EDGE ( 'NONE', *, *, #5902, .F. ) ;
#68584=AXIS2_PLACEMENT_3D ( 'NONE', #67530, #25907, #60146 ) ;
#68588=FACE_OUTER_BOUND ( 'NONE', #55968, .T. ) ;
#68632=AXIS2_PLACEMENT_3D ( 'NONE', #15566, #39617, #56913 ) ;
#68640=DIRECTION ( 'NONE',  ( 0.000000000000000000, 0.9876883405951372152, 0.1564344650402347547 ) ) ;
#68643=ORIENTED_EDGE ( 'NONE', *, *, #17608, .F. ) ;
#68656=DIRECTION ( 'NONE',  ( -1.000000000000000000, -0.000000000000000000, 0.000000000000000000 ) ) ;
#68659=VERTEX_POINT ( 'NONE', #45337 ) ;
#68662=CARTESIAN_POINT ( 'NONE',  ( 10.00000000000000000, 41.81611651403861885, 3.925862922256313503 ) ) ;
#68670=LINE ( 'NONE', #28805, #71450 ) ;
#68673=CARTESIAN_POINT ( 'NONE',  ( 10.00000000000000000, -21.32104025579135964, 30.84782396557210760 ) ) ;
#68681=EDGE_CURVE ( 'NONE', #7439, #2929, #52451, .T. ) ;
#68688=LINE ( 'NONE', #45764, #22027 ) ;
#68693=EDGE_CURVE ( 'NONE', #2465, #13867, #21209, .T. ) ;
#68694=CARTESIAN_POINT ( 'NONE',  ( 0.000000000000000000, 35.53030884539084866, 12.26510123303271982 ) ) ;
#68710=CARTESIAN_POINT ( 'NONE',  ( 10.00000000000000000, -12.42422080174663712, 35.38097989696507994 ) ) ;
#68714=VERTEX_POINT ( 'NONE', #29866 ) ;
#68718=ORIENTED_EDGE ( 'NONE', *, *, #1563, .T. ) ;
#68722=FACE_OUTER_BOUND ( 'NONE', #24586, .T. ) ;
#68741=EDGE_LOOP ( 'NONE', ( #58323, #37213, #34863, #8780 ) ) ;
#68746=ORIENTED_EDGE ( 'NONE', *, *, #29176, .F. ) ;
#68754=DIRECTION ( 'NONE',  ( -1.000000000000000000, 0.000000000000000000, -0.000000000000000000 ) ) ;
#68766=DIRECTION ( 'NONE',  ( 0.000000000000000000, 0.1564344650402243742, 0.9876883405951387696 ) ) ;
#68774=EDGE_CURVE ( 'NONE', #30420, #55313, #35645, .T. ) ;
#68781=EDGE_CURVE ( 'NONE', #3354, #30420, #63738, .T. ) ;
#68789=CARTESIAN_POINT ( 'NONE',  ( 10.00000000000000000, -29.81001611431024756, 22.74946021919122785 ) ) ;
#68792=CIRCLE ( 'NONE', #34000, 37.49900000000000944 ) ;
#68793=EDGE_CURVE ( 'NONE', #40041, #3329, #70830, .T. ) ;
#68796=VERTEX_POINT ( 'NONE', #52817 ) ;
#68807=FACE_OUTER_BOUND ( 'NONE', #22460, .T. ) ;
#68819=ORIENTED_EDGE ( 'NONE', *, *, #59179, .T. ) ;
#68825=VERTEX_POINT ( 'NONE', #7327 ) ;
#68828=EDGE_CURVE ( 'NONE', #50573, #8248, #44036, .T. ) ;
#68838=DIRECTION ( 'NONE',  ( 0.000000000000000000, 0.2079116908177532363, 0.9781476007338069101 ) ) ;
#68844=DIRECTION ( 'NONE',  ( 0.000000000000000000, 0.000000000000000000, 1.000000000000000000 ) ) ;
#68858=FACE_OUTER_BOUND ( 'NONE', #15720, .T. ) ;
#68862=CARTESIAN_POINT ( 'NONE',  ( -3.000000000000000000, 20.85821328998756385, -10.92862929874494959 ) ) ;
#68866=CARTESIAN_POINT ( 'NONE',  ( -3.000000000000000000, 5.835314593368772229, -22.81335362449846826 ) ) ;
#68872=ORIENTED_EDGE ( 'NONE', *, *, #29780, .F. ) ;
#68889=CIRCLE ( 'NONE', #10012, 42.00000000000000000 ) ;
#68891=VERTEX_POINT ( 'NONE', #33313 ) ;
#68895=LINE ( 'NONE', #69257, #51268 ) ;
#68898=ORIENTED_EDGE ( 'NONE', *, *, #13005, .T. ) ;
#68929=ADVANCED_FACE ( 'NONE', ( #7361 ), #24644, .T. ) ;
#68959=CIRCLE ( 'NONE', #13718, 37.49900000000000944 ) ;
#68962=VERTEX_POINT ( 'NONE', #70480 ) ;
#68965=DIRECTION ( 'NONE',  ( 0.000000000000000000, -0.8910065241883722287, 0.4539904997395382003 ) ) ;
#68977=VERTEX_POINT ( 'NONE', #47212 ) ;
#68985=AXIS2_PLACEMENT_3D ( 'NONE', #23051, #29396, #12851 ) ;
#68996=CARTESIAN_POINT ( 'NONE',  ( -3.000000000000000000, -25.60904388321916159, -6.976881207771517879 ) ) ;
#69001=DIRECTION ( 'NONE',  ( -1.000000000000000000, -0.000000000000000000, 0.000000000000000000 ) ) ;
#69005=EDGE_CURVE ( 'NONE', #10635, #24265, #58118, .T. ) ;
#69018=CARTESIAN_POINT ( 'NONE',  ( 10.00000000000000000, 0.000000000000000000, 0.000000000000000000 ) ) ;
#69028=DIRECTION ( 'NONE',  ( 1.000000000000000000, 0.000000000000000000, 0.000000000000000000 ) ) ;
#69031=EDGE_CURVE ( 'NONE', #27537, #31441, #12251, .T. ) ;
#69032=VERTEX_POINT ( 'NONE', #41943 ) ;
#69036=AXIS2_PLACEMENT_3D ( 'NONE', #72752, #62633, #44210 ) ;
#69043=CARTESIAN_POINT ( 'NONE',  ( 10.00000000000000000, 33.00180498840072829, -17.80606268964504935 ) ) ;
#69059=DIRECTION ( 'NONE',  ( -1.000000000000000000, 0.000000000000000000, -0.000000000000000000 ) ) ;
#69078=VERTEX_POINT ( 'NONE', #46848 ) ;
#69081=AXIS2_PLACEMENT_3D ( 'NONE', #37748, #53550, #9162 ) ;
#69088=EDGE_CURVE ( 'NONE', #63433, #22473, #20850, .T. ) ;
#69098=CIRCLE ( 'NONE', #1877, 42.00000000000000000 ) ;
#69105=ADVANCED_FACE ( 'NONE', ( #14090 ), #49783, .F. ) ;
#69119=ORIENTED_EDGE ( 'NONE', *, *, #60385, .T. ) ;
#69121=ORIENTED_EDGE ( 'NONE', *, *, #40070, .F. ) ;
#69126=AXIS2_PLACEMENT_3D ( 'NONE', #35445, #57653, #64032 ) ;
#69143=CARTESIAN_POINT ( 'NONE',  ( -3.000000000000000000, -22.32062822937489344, 14.36278369418800160 ) ) ;
#69144=CARTESIAN_POINT ( 'NONE',  ( 10.00000000000000000, -35.38097989696520074, 12.42422080174625520 ) ) ;
#69145=CARTESIAN_POINT ( 'NONE',  ( 0.000000000000000000, 5.835314593368772229, -22.81335362449846826 ) ) ;
#69149=AXIS2_PLACEMENT_3D ( 'NONE', #24899, #47827, #70748 ) ;
#69164=ORIENTED_EDGE ( 'NONE', *, *, #32684, .T. ) ;
#69174=ORIENTED_EDGE ( 'NONE', *, *, #50045, .F. ) ;
#69177=EDGE_CURVE ( 'NONE', #2347, #60338, #63319, .T. ) ;
#69179=EDGE_LOOP ( 'NONE', ( #64951, #42701, #58062, #47976 ) ) ;
#69180=DIRECTION ( 'NONE',  ( 0.000000000000000000, 0.000000000000000000, 1.000000000000000000 ) ) ;
#69186=LINE ( 'NONE', #39880, #74122 ) ;
#69192=CARTESIAN_POINT ( 'NONE',  ( 4.999999999999999112, -3.925862922256468046, 41.81611651403860463 ) ) ;
#69203=DIRECTION ( 'NONE',  ( 0.000000000000000000, 0.000000000000000000, 1.000000000000000000 ) ) ;
#69218=AXIS2_PLACEMENT_3D ( 'NONE', #70289, #23351, #1201 ) ;
#69224=FACE_OUTER_BOUND ( 'NONE', #53296, .T. ) ;
#69225=LINE ( 'NONE', #12074, #32147 ) ;
#69230=ORIENTED_EDGE ( 'NONE', *, *, #35034, .T. ) ;
#69236=ORIENTED_EDGE ( 'NONE', *, *, #31323, .F. ) ;
#69245=CIRCLE ( 'NONE', #46448, 16.00000000000000000 ) ;
#69257=CARTESIAN_POINT ( 'NONE',  ( -3.000000000000000000, 23.50000000000000000, -1.500000000000001332 ) ) ;
#69261=AXIS2_PLACEMENT_3D ( 'NONE', #74014, #41295, #29255 ) ;
#69265=VECTOR ( 'NONE', #33426, 1000.000000000000000 ) ;
#69269=ORIENTED_EDGE ( 'NONE', *, *, #69031, .T. ) ;
#69275=CARTESIAN_POINT ( 'NONE',  ( 10.00000000000000000, -17.80606268964563554, 33.00180498840040855 ) ) ;
#69277=CARTESIAN_POINT ( 'NONE',  ( -3.000000000000000000, -23.29833615347104825, -3.418703333116803744 ) ) ;
#69279=ADVANCED_FACE ( 'NONE', ( #34352 ), #4326, .F. ) ;
#69289=CARTESIAN_POINT ( 'NONE',  ( 10.00000000000000000, -41.81611651403864727, 3.925862922256025289 ) ) ;
#69308=DIRECTION ( 'NONE',  ( -1.000000000000000000, -0.000000000000000000, 0.000000000000000000 ) ) ;
#69312=DIRECTION ( 'NONE',  ( -1.000000000000000000, -0.000000000000000000, -0.000000000000000000 ) ) ;
#69319=ORIENTED_EDGE ( 'NONE', *, *, #34922, .F. ) ;
#69322=DIRECTION ( 'NONE',  ( -1.000000000000000000, 0.000000000000000000, -0.000000000000000000 ) ) ;
#69328=EDGE_CURVE ( 'NONE', #61245, #52121, #11778, .T. ) ;
#69339=ORIENTED_EDGE ( 'NONE', *, *, #8199, .F. ) ;
#69342=ADVANCED_FACE ( 'NONE', ( #27216 ), #5439, .T. ) ;
#69347=ORIENTED_EDGE ( 'NONE', *, *, #34921, .T. ) ;
#69348=ORIENTED_EDGE ( 'NONE', *, *, #52362, .T. ) ;
#69349=ORIENTED_EDGE ( 'NONE', *, *, #31789, .T. ) ;
#69350=CARTESIAN_POINT ( 'NONE',  ( 10.00000000000000000, 37.16516213103285082, -4.992566952384588141 ) ) ;
#69356=AXIS2_PLACEMENT_3D ( 'NONE', #72984, #38797, #61736 ) ;
#69363=ORIENTED_EDGE ( 'NONE', *, *, #25152, .T. ) ;
#69374=CARTESIAN_POINT ( 'NONE',  ( 5.000000000000000000, -22.48208911017525580, 35.47612816024516036 ) ) ;
#69375=DIRECTION ( 'NONE',  ( -1.000000000000000000, -0.000000000000000000, -0.000000000000000000 ) ) ;
#69385=CYLINDRICAL_SURFACE ( 'NONE', #45055, 16.00000000000000000 ) ;
#69386=DIRECTION ( 'NONE',  ( 0.000000000000000000, 0.000000000000000000, -1.000000000000000000 ) ) ;
#69405=ORIENTED_EDGE ( 'NONE', *, *, #49069, .F. ) ;
#69415=EDGE_LOOP ( 'NONE', ( #49996, #58635, #47780, #25578 ) ) ;
#69427=DIRECTION ( 'NONE',  ( -1.000000000000000000, -0.000000000000000000, 0.000000000000000000 ) ) ;
#69432=ADVANCED_FACE ( 'NONE', ( #52765 ), #41477, .T. ) ;
#69447=ORIENTED_EDGE ( 'NONE', *, *, #1499, .F. ) ;
#69449=CARTESIAN_POINT ( 'NONE',  ( 0.000000000000000000, -10.96151621346514382, 35.95386929396252640 ) ) ;
#69469=VECTOR ( 'NONE', #49608, 1000.000000000000000 ) ;
#69470=FACE_OUTER_BOUND ( 'NONE', #7208, .T. ) ;
#69476=ORIENTED_EDGE ( 'NONE', *, *, #61024, .F. ) ;
#69482=DIRECTION ( 'NONE',  ( -1.000000000000000000, 0.000000000000000000, 0.000000000000000000 ) ) ;
#69490=DIRECTION ( 'NONE',  ( -0.000000000000000000, 0.9945218953682731788, 0.1045284632676559550 ) ) ;
#69493=DIRECTION ( 'NONE',  ( -1.000000000000000000, 0.000000000000000000, 0.000000000000000000 ) ) ;
#69494=CARTESIAN_POINT ( 'NONE',  ( -3.000000000000000000, 22.07842321921481243, 8.187992925817422218 ) ) ;
#69497=EDGE_CURVE ( 'NONE', #29066, #21068, #19279, .T. ) ;
#69506=AXIS2_PLACEMENT_3D ( 'NONE', #49754, #56150, #32832 ) ;
#69507=FACE_OUTER_BOUND ( 'NONE', #22563, .T. ) ;
#69516=ORIENTED_EDGE ( 'NONE', *, *, #9400, .T. ) ;
#69533=CARTESIAN_POINT ( 'NONE',  ( 10.00000000000000000, -5.202137450156655518, 37.22597642581156663 ) ) ;
#69535=CARTESIAN_POINT ( 'NONE',  ( 10.00000000000000000, -37.48860685352290290, -0.8828120875904512665 ) ) ;
#69581=DIRECTION ( 'NONE',  ( 0.000000000000000000, -0.2079116908177664758, 0.9781476007338042455 ) ) ;
#69587=CARTESIAN_POINT ( 'NONE',  ( 10.00000000000000000, -35.92658777277517856, 10.74501242461269257 ) ) ;
#69589=DIRECTION ( 'NONE',  ( -1.000000000000000000, 0.000000000000000000, 0.000000000000000000 ) ) ;
#69591=PLANE ( 'NONE',  #74192 ) ;
#69596=VECTOR ( 'NONE', #1865, 1000.000000000000000 ) ;
#69599=VERTEX_POINT ( 'NONE', #43711 ) ;
#69607=CYLINDRICAL_SURFACE ( 'NONE', #43267, 42.00000000000000000 ) ;
#69615=CIRCLE ( 'NONE', #55234, 37.49900000000000233 ) ;
#69630=ORIENTED_EDGE ( 'NONE', *, *, #51533, .F. ) ;
#69633=AXIS2_PLACEMENT_3D ( 'NONE', #24720, #58190, #6691 ) ;
#69654=CARTESIAN_POINT ( 'NONE',  ( -3.000000000000000000, 16.83928648764945279, -16.46020748918028076 ) ) ;
#69659=LINE ( 'NONE', #29788, #47489 ) ;
#69671=LINE ( 'NONE', #35095, #37327 ) ;
#69672=DIRECTION ( 'NONE',  ( -1.000000000000000000, 0.000000000000000000, 0.000000000000000000 ) ) ;
#69679=EDGE_CURVE ( 'NONE', #41287, #25052, #51377, .T. ) ;
#69682=CARTESIAN_POINT ( 'NONE',  ( 0.000000000000000000, 37.58145647212453611, 0.6853352020791767529 ) ) ;
#69685=CARTESIAN_POINT ( 'NONE',  ( 0.000000000000000000, 20.85821328998756385, -10.92862929874494959 ) ) ;
#69686=EDGE_CURVE ( 'NONE', #18187, #22980, #15114, .T. ) ;
#69694=VECTOR ( 'NONE', #22913, 1000.000000000000000 ) ;
#69710=VERTEX_POINT ( 'NONE', #51180 ) ;
#69721=VERTEX_POINT ( 'NONE', #21488 ) ;
#69744=DIRECTION ( 'NONE',  ( 0.000000000000000000, 1.000000000000000000, 7.228014483236689653E-16 ) ) ;
#69745=CIRCLE ( 'NONE', #32539, 15.99999999999999467 ) ;
#69755=CARTESIAN_POINT ( 'NONE',  ( 10.00000000000000000, -21.40280677340345505, -36.13751322684441902 ) ) ;
#69758=EDGE_CURVE ( 'NONE', #13671, #68033, #28617, .T. ) ;
#69759=DIRECTION ( 'NONE',  ( -1.000000000000000000, 0.000000000000000000, 0.000000000000000000 ) ) ;
#69763=CARTESIAN_POINT ( 'NONE',  ( -3.000000000000000000, -11.95096189432312350, -23.69967320028773372 ) ) ;
#69775=AXIS2_PLACEMENT_3D ( 'NONE', #2509, #37427, #15213 ) ;
#69781=ADVANCED_FACE ( 'NONE', ( #27123 ), #50056, .T. ) ;
#69785=CIRCLE ( 'NONE', #68632, 16.00000000000000000 ) ;
#69806=DIRECTION ( 'NONE',  ( -1.000000000000000000, 0.000000000000000000, -0.000000000000000000 ) ) ;
#69839=CARTESIAN_POINT ( 'NONE',  ( 10.00000000000000000, 0.000000000000000000, 0.000000000000000000 ) ) ;
#69840=ORIENTED_EDGE ( 'NONE', *, *, #26837, .T. ) ;
#69841=EDGE_CURVE ( 'NONE', #66019, #68825, #53785, .T. ) ;
#69843=ORIENTED_EDGE ( 'NONE', *, *, #10166, .F. ) ;
#69845=AXIS2_PLACEMENT_3D ( 'NONE', #38579, #55495, #21258 ) ;
#69853=LINE ( 'NONE', #34917, #9206 ) ;
#69855=CARTESIAN_POINT ( 'NONE',  ( 0.000000000000000000, 26.50000000000000000, -1.500000000000001332 ) ) ;
#69857=EDGE_CURVE ( 'NONE', #26897, #56328, #69225, .T. ) ;
#69863=ADVANCED_FACE ( 'NONE', ( #58681 ), #69591, .F. ) ;
#69884=DIRECTION ( 'NONE',  ( -1.000000000000000000, -0.000000000000000000, 0.000000000000000000 ) ) ;
#69888=DIRECTION ( 'NONE',  ( 0.000000000000000000, 0.000000000000000000, -1.000000000000000000 ) ) ;
#69913=CARTESIAN_POINT ( 'NONE',  ( 0.000000000000000000, 2.663952781846149254, 41.91543099594818500 ) ) ;
#69914=EDGE_CURVE ( 'NONE', #66826, #71364, #17712, .T. ) ;
#69933=CARTESIAN_POINT ( 'NONE',  ( 10.00000000000000000, 0.000000000000000000, 0.000000000000000000 ) ) ;
#69937=CARTESIAN_POINT ( 'NONE',  ( 0.000000000000000000, 33.17418723428307459, 17.67226234102837878 ) ) ;
#69938=CARTESIAN_POINT ( 'NONE',  ( -3.000000000000000000, 0.000000000000000000, 0.000000000000000000 ) ) ;
#69947=VECTOR ( 'NONE', #11675, 999.9999999999998863 ) ;
#69948=DIRECTION ( 'NONE',  ( -1.000000000000000000, 0.000000000000000000, 0.000000000000000000 ) ) ;
#69949=DIRECTION ( 'NONE',  ( 0.000000000000000000, -0.9876883405951393247, 0.1564344650402205161 ) ) ;
#69959=CYLINDRICAL_SURFACE ( 'NONE', #16341, 21.00000000000000000 ) ;
#69994=EDGE_CURVE ( 'NONE', #73774, #29448, #25027, .T. ) ;
#70010=DIRECTION ( 'NONE',  ( -1.000000000000000000, 0.000000000000000000, 0.000000000000000000 ) ) ;
#70035=DIRECTION ( 'NONE',  ( 0.000000000000000000, -0.9876883405951358830, -0.1564344650402421932 ) ) ;
#70037=DIRECTION ( 'NONE',  ( -1.000000000000000000, 0.000000000000000000, -0.000000000000000000 ) ) ;
#70041=EDGE_CURVE ( 'NONE', #3791, #7308, #65073, .T. ) ;
#70046=DIRECTION ( 'NONE',  ( 0.000000000000000000, -0.5877852522924624790, -0.8090169943749553338 ) ) ;
#70056=VERTEX_POINT ( 'NONE', #10039 ) ;
#70057=DIRECTION ( 'NONE',  ( 0.000000000000000000, 0.000000000000000000, 1.000000000000000000 ) ) ;
#70065=VERTEX_POINT ( 'NONE', #72800 ) ;
#70076=EDGE_LOOP ( 'NONE', ( #30140, #15237, #29228, #56733 ) ) ;
#70087=DIRECTION ( 'NONE',  ( -1.000000000000000000, -0.000000000000000000, 0.000000000000000000 ) ) ;
#70113=DIRECTION ( 'NONE',  ( 0.000000000000000000, 0.000000000000000000, 1.000000000000000000 ) ) ;
#70140=ORIENTED_EDGE ( 'NONE', *, *, #58458, .F. ) ;
#70141=ORIENTED_EDGE ( 'NONE', *, *, #31977, .F. ) ;
#70145=DIRECTION ( 'NONE',  ( 0.000000000000000000, 0.8910065241883657894, 0.4539904997395509678 ) ) ;
#70151=CARTESIAN_POINT ( 'NONE',  ( 10.00000000000000000, 0.000000000000000000, 0.000000000000000000 ) ) ;
#70161=ORIENTED_EDGE ( 'NONE', *, *, #4948, .T. ) ;
#70170=EDGE_CURVE ( 'NONE', #23048, #50573, #64634, .T. ) ;
#70203=CARTESIAN_POINT ( 'NONE',  ( 0.000000000000000000, 37.58145647212453611, 16.68533520207917675 ) ) ;
#70214=FACE_OUTER_BOUND ( 'NONE', #26131, .T. ) ;
#70227=AXIS2_PLACEMENT_3D ( 'NONE', #44592, #33663, #38941 ) ;
#70235=CARTESIAN_POINT ( 'NONE',  ( 0.000000000000000000, -14.54903810567645372, -22.19967320028775504 ) ) ;
#70249=VECTOR ( 'NONE', #69482, 1000.000000000000000 ) ;
#70257=VERTEX_POINT ( 'NONE', #9486 ) ;
#70276=EDGE_CURVE ( 'NONE', #51144, #62438, #65914, .T. ) ;
#70279=DIRECTION ( 'NONE',  ( -0.000000000000000000, -0.9135454576426004225, -0.4067366430758009854 ) ) ;
#70281=CARTESIAN_POINT ( 'NONE',  ( 10.00000000000000000, 37.58145647212455032, -0.6853352020786441789 ) ) ;
#70286=CARTESIAN_POINT ( 'NONE',  ( -3.000000000000000000, -22.67460108101783334, 6.353146135317912169 ) ) ;
#70289=CARTESIAN_POINT ( 'NONE',  ( 10.00000000000000000, 0.000000000000000000, 0.000000000000000000 ) ) ;
#70293=DIRECTION ( 'NONE',  ( -0.000000000000000000, 0.4999999999999919509, 0.8660254037844432595 ) ) ;
#70354=CARTESIAN_POINT ( 'NONE',  ( -3.000000000000000000, 14.60985201121729737, -18.46759930825687945 ) ) ;
#70356=DIRECTION ( 'NONE',  ( 0.000000000000000000, -0.5877852522924624790, -0.8090169943749550008 ) ) ;
#70363=EDGE_CURVE ( 'NONE', #67004, #54905, #8175, .T. ) ;
#70364=VERTEX_POINT ( 'NONE', #60640 ) ;
#70376=LINE ( 'NONE', #58009, #33075 ) ;
#70377=DIRECTION ( 'NONE',  ( -1.000000000000000000, -0.000000000000000000, 0.000000000000000000 ) ) ;
#70389=CARTESIAN_POINT ( 'NONE',  ( 10.00000000000000000, 37.48860685352291000, -0.8828120875901940279 ) ) ;
#70393=CARTESIAN_POINT ( 'NONE',  ( -3.000000000000000000, 5.835314593368477354, 22.81335362449854642 ) ) ;
#70395=CARTESIAN_POINT ( 'NONE',  ( 10.00000000000000000, 0.000000000000000000, 0.000000000000000000 ) ) ;
#70416=CARTESIAN_POINT ( 'NONE',  ( -3.000000000000000000, 6.762365576493643893, -25.66652317338391853 ) ) ;
#70418=VERTEX_POINT ( 'NONE', #57217 ) ;
#70424=VERTEX_POINT ( 'NONE', #17355 ) ;
#70426=VERTEX_POINT ( 'NONE', #16992 ) ;
#70428=AXIS2_PLACEMENT_3D ( 'NONE', #68134, #46687, #62896 ) ;
#70442=ADVANCED_FACE ( 'NONE', ( #16242 ), #34641, .T. ) ;
#70446=PLANE ( 'NONE',  #26786 ) ;
#70460=CARTESIAN_POINT ( 'NONE',  ( 0.000000000000000000, -26.08949754953005495, -27.05870788708258701 ) ) ;
#70468=EDGE_LOOP ( 'NONE', ( #41783, #27774, #66101, #53450 ) ) ;
#70471=AXIS2_PLACEMENT_3D ( 'NONE', #1391, #65252, #42318 ) ;
#70474=DIRECTION ( 'NONE',  ( -1.000000000000000000, 0.000000000000000000, -0.000000000000000000 ) ) ;
#70479=CIRCLE ( 'NONE', #47688, 37.49900000000000944 ) ;
#70480=CARTESIAN_POINT ( 'NONE',  ( 0.000000000000000000, 22.74946021919133088, 29.81001611431016229 ) ) ;
#70482=DIRECTION ( 'NONE',  ( 1.000000000000000000, 0.000000000000000000, 0.000000000000000000 ) ) ;
#70492=CARTESIAN_POINT ( 'NONE',  ( -3.000000000000000000, 16.83928648764945279, -16.46020748918028076 ) ) ;
#70494=EDGE_CURVE ( 'NONE', #60846, #55130, #68500, .T. ) ;
#70496=EDGE_CURVE ( 'NONE', #35203, #23253, #10226, .T. ) ;
#70503=AXIS2_PLACEMENT_3D ( 'NONE', #40223, #9794, #49999 ) ;
#70506=CARTESIAN_POINT ( 'NONE',  ( -3.000000000000000000, 26.50000000000000355, 1.500000000000000000 ) ) ;
#70510=AXIS2_PLACEMENT_3D ( 'NONE', #66722, #38144, #32863 ) ;
#70518=DIRECTION ( 'NONE',  ( 1.000000000000000000, 0.000000000000000000, 0.000000000000000000 ) ) ;
#70530=CARTESIAN_POINT ( 'NONE',  ( 0.000000000000000000, -9.188173127307001309, -40.98264845739759465 ) ) ;
#70538=ORIENTED_EDGE ( 'NONE', *, *, #21222, .F. ) ;
#70544=DIRECTION ( 'NONE',  ( -1.000000000000000000, 0.000000000000000000, 0.000000000000000000 ) ) ;
#70554=DIRECTION ( 'NONE',  ( 0.000000000000000000, 0.000000000000000000, 1.000000000000000000 ) ) ;
#70564=CYLINDRICAL_SURFACE ( 'NONE', #72616, 37.49900000000000233 ) ;
#70587=VECTOR ( 'NONE', #23121, 999.9999999999998863 ) ;
#70590=DIRECTION ( 'NONE',  ( 0.000000000000000000, 1.000000000000000000, 7.228014483236689653E-16 ) ) ;
#70593=CARTESIAN_POINT ( 'NONE',  ( 0.000000000000000000, 23.50000000000000000, 1.499999999999997780 ) ) ;
#70596=LINE ( 'NONE', #43827, #28409 ) ;
#70625=ORIENTED_EDGE ( 'NONE', *, *, #48473, .F. ) ;
#70632=ORIENTED_EDGE ( 'NONE', *, *, #7147, .T. ) ;
#70640=ORIENTED_EDGE ( 'NONE', *, *, #66195, .F. ) ;
#70655=DIRECTION ( 'NONE',  ( -1.000000000000000000, -0.000000000000000000, -0.000000000000000000 ) ) ;
#70656=EDGE_CURVE ( 'NONE', #60846, #61246, #64339, .T. ) ;
#70682=EDGE_CURVE ( 'NONE', #18846, #42329, #19932, .T. ) ;
#70687=FACE_OUTER_BOUND ( 'NONE', #23748, .T. ) ;
#70695=ADVANCED_FACE ( 'NONE', ( #54526 ), #72537, .T. ) ;
#70699=EDGE_LOOP ( 'NONE', ( #46400, #30963, #65080, #69119 ) ) ;
#70713=ORIENTED_EDGE ( 'NONE', *, *, #4900, .F. ) ;
#70738=LINE ( 'NONE', #18867, #22858 ) ;
#70745=ORIENTED_EDGE ( 'NONE', *, *, #29923, .T. ) ;
#70748=DIRECTION ( 'NONE',  ( 0.000000000000000000, 0.9510565162951539753, -0.3090169943749460635 ) ) ;
#70754=DIRECTION ( 'NONE',  ( 0.000000000000000000, -0.6691306063588569053, -0.7431448254773954654 ) ) ;
#70760=EDGE_CURVE ( 'NONE', #35754, #63709, #72172, .T. ) ;
#70765=CARTESIAN_POINT ( 'NONE',  ( -3.000000000000000000, 18.84667830672605859, -18.68964196561243796 ) ) ;
#70767=FACE_OUTER_BOUND ( 'NONE', #27954, .T. ) ;
#70773=EDGE_CURVE ( 'NONE', #52874, #33020, #37617, .T. ) ;
#70776=DIRECTION ( 'NONE',  ( -1.000000000000000000, -0.000000000000000000, 0.000000000000000000 ) ) ;
#70804=AXIS2_PLACEMENT_3D ( 'NONE', #52175, #58944, #70554 ) ;
#70819=VERTEX_POINT ( 'NONE', #57131 ) ;
#70828=CARTESIAN_POINT ( 'NONE',  ( 0.000000000000000000, 0.000000000000000000, 0.000000000000000000 ) ) ;
#70830=LINE ( 'NONE', #2090, #9245 ) ;
#70836=VECTOR ( 'NONE', #29019, 1000.000000000000000 ) ;
#70841=LINE ( 'NONE', #2100, #51538 ) ;
#70869=VECTOR ( 'NONE', #28565, 1000.000000000000000 ) ;
#70893=PLANE ( 'NONE',  #24651 ) ;
#70895=ORIENTED_EDGE ( 'NONE', *, *, #12913, .T. ) ;
#70901=LINE ( 'NONE', #1793, #19492 ) ;
#70905=ORIENTED_EDGE ( 'NONE', *, *, #12964, .F. ) ;
#70917=VERTEX_POINT ( 'NONE', #50358 ) ;
#70920=FACE_OUTER_BOUND ( 'NONE', #35019, .T. ) ;
#70928=CARTESIAN_POINT ( 'NONE',  ( 10.00000000000000000, 0.000000000000000000, 0.000000000000000000 ) ) ;
#70932=ORIENTED_EDGE ( 'NONE', *, *, #40686, .T. ) ;
#70934=VERTEX_POINT ( 'NONE', #51474 ) ;
#70945=AXIS2_PLACEMENT_3D ( 'NONE', #56152, #11037, #67055 ) ;
#70955=CYLINDRICAL_SURFACE ( 'NONE', #11220, 42.00000000000000000 ) ;
#70959=CYLINDRICAL_SURFACE ( 'NONE', #25208, 16.00000000000000355 ) ;
#70962=CARTESIAN_POINT ( 'NONE',  ( -3.000000000000000000, -10.45096189432314837, -21.10159698893440350 ) ) ;
#70975=LINE ( 'NONE', #52212, #50368 ) ;
#70987=VERTEX_POINT ( 'NONE', #58595 ) ;
#71002=CIRCLE ( 'NONE', #36193, 16.00000000000000000 ) ;
#71011=ORIENTED_EDGE ( 'NONE', *, *, #28074, .T. ) ;
#71017=ADVANCED_FACE ( 'NONE', ( #69507 ), #57866, .T. ) ;
#71039=DIRECTION ( 'NONE',  ( -1.000000000000000000, -0.000000000000000000, -0.000000000000000000 ) ) ;
#71081=ADVANCED_FACE ( 'NONE', ( #46579 ), #40570, .T. ) ;
#71084=DIRECTION ( 'NONE',  ( -1.000000000000000000, 0.000000000000000000, 0.000000000000000000 ) ) ;
#71091=ORIENTED_EDGE ( 'NONE', *, *, #43825, .T. ) ;
#71099=CIRCLE ( 'NONE', #14657, 42.00000000000000000 ) ;
#71121=CARTESIAN_POINT ( 'NONE',  ( 0.000000000000000000, -19.89357724625003598, 12.59942793731059574 ) ) ;
#71122=VECTOR ( 'NONE', #35218, 1000.000000000000000 ) ;
#71123=CARTESIAN_POINT ( 'NONE',  ( 10.00000000000000000, 0.000000000000000000, 0.000000000000000000 ) ) ;
#71125=AXIS2_PLACEMENT_3D ( 'NONE', #16588, #40638, #458 ) ;
#71148=CARTESIAN_POINT ( 'NONE',  ( -3.000000000000000000, 18.84667830672579925, 18.68964196561269020 ) ) ;
#71152=CARTESIAN_POINT ( 'NONE',  ( -3.000000000000000000, 24.81905959214261514, 9.408202855044825341 ) ) ;
#71154=AXIS2_PLACEMENT_3D ( 'NONE', #56588, #51296, #34756 ) ;
#71161=ORIENTED_EDGE ( 'NONE', *, *, #28931, .F. ) ;
#71162=VECTOR ( 'NONE', #39014, 1000.000000000000000 ) ;
#71167=DIRECTION ( 'NONE',  ( 0.000000000000000000, 0.7071067811865439090, 0.7071067811865512365 ) ) ;
#71169=EDGE_LOOP ( 'NONE', ( #66769, #12456, #23502, #10244 ) ) ;
#71172=CARTESIAN_POINT ( 'NONE',  ( 0.000000000000000000, 0.000000000000000000, 0.000000000000000000 ) ) ;
#71174=ORIENTED_EDGE ( 'NONE', *, *, #23211, .F. ) ;
#71181=ORIENTED_EDGE ( 'NONE', *, *, #7478, .F. ) ;
#71195=CIRCLE ( 'NONE', #54420, 37.49900000000000944 ) ;
#71198=ORIENTED_EDGE ( 'NONE', *, *, #65438, .T. ) ;
#71221=VECTOR ( 'NONE', #40468, 1000.000000000000000 ) ;
#71223=CARTESIAN_POINT ( 'NONE',  ( 10.00000000000000000, -30.84782396557201878, -21.32104025579148399 ) ) ;
#71226=CIRCLE ( 'NONE', #65249, 37.49900000000000233 ) ;
#71227=CARTESIAN_POINT ( 'NONE',  ( -3.000000000000000000, -19.89357724625003598, 12.59942793731059574 ) ) ;
#71232=DIRECTION ( 'NONE',  ( 0.000000000000000000, 0.000000000000000000, 1.000000000000000000 ) ) ;
#71234=CARTESIAN_POINT ( 'NONE',  ( -3.000000000000000000, 0.000000000000000000, 0.000000000000000000 ) ) ;
#71249=ORIENTED_EDGE ( 'NONE', *, *, #53570, .T. ) ;
#71275=CYLINDRICAL_SURFACE ( 'NONE', #55463, 16.00000000000000000 ) ;
#71293=DIRECTION ( 'NONE',  ( -1.000000000000000000, 0.000000000000000000, -0.000000000000000000 ) ) ;
#71302=CIRCLE ( 'NONE', #43749, 42.00000000000000000 ) ;
#71306=DIRECTION ( 'NONE',  ( -1.000000000000000000, 0.000000000000000000, 0.000000000000000000 ) ) ;
#71314=CARTESIAN_POINT ( 'NONE',  ( -3.000000000000000000, -0.9646360437372163421, -23.52805723605591126 ) ) ;
#71321=VECTOR ( 'NONE', #52676, 999.9999999999998863 ) ;
#71322=CARTESIAN_POINT ( 'NONE',  ( 10.00000000000000000, -6.555932627142143865, -37.01155633439065440 ) ) ;
#71329=DIRECTION ( 'NONE',  ( -0.000000000000000000, 0.8090169943749426773, 0.5877852522924797984 ) ) ;
#71346=DIRECTION ( 'NONE',  ( 0.000000000000000000, 0.000000000000000000, 1.000000000000000000 ) ) ;
#71350=( NAMED_UNIT ( * ) SI_UNIT ( $, .STERADIAN. ) SOLID_ANGLE_UNIT ( ) );
#71364=VERTEX_POINT ( 'NONE', #73199 ) ;
#71372=ADVANCED_FACE ( 'NONE', ( #16817 ), #56679, .T. ) ;
#71412=PLANE ( 'NONE',  #36773 ) ;
#71423=AXIS2_PLACEMENT_3D ( 'NONE', #275, #69028, #17513 ) ;
#71430=AXIS2_PLACEMENT_3D ( 'NONE', #54800, #3330, #49524 ) ;
#71431=ADVANCED_FACE ( 'NONE', ( #59538 ), #36591, .F. ) ;
#71432=CIRCLE ( 'NONE', #60683, 15.99999999999999822 ) ;
#71450=VECTOR ( 'NONE', #51737, 1000.000000000000000 ) ;
#71456=ADVANCED_FACE ( 'NONE', ( #51382 ), #17545, .F. ) ;
#71461=ORIENTED_EDGE ( 'NONE', *, *, #47517, .F. ) ;
#71477=CARTESIAN_POINT ( 'NONE',  ( 0.000000000000000000, -36.88895765772637247, 6.736453364083436313 ) ) ;
#71492=VECTOR ( 'NONE', #38570, 1000.000000000000000 ) ;
#71495=ORIENTED_EDGE ( 'NONE', *, *, #16210, .T. ) ;
#71512=AXIS2_PLACEMENT_3D ( 'NONE', #53155, #47149, #70057 ) ;
#71518=CARTESIAN_POINT ( 'NONE',  ( 10.00000000000000000, 0.000000000000000000, 0.000000000000000000 ) ) ;
#71534=VERTEX_POINT ( 'NONE', #6790 ) ;
#71549=ADVANCED_FACE ( 'NONE', ( #27592 ), #29337, .T. ) ;
#71552=CIRCLE ( 'NONE', #57142, 16.00000000000000000 ) ;
#71560=VERTEX_POINT ( 'NONE', #45273 ) ;
#71562=EDGE_LOOP ( 'NONE', ( #54063, #37844, #66147, #35693 ) ) ;
#71569=DIRECTION ( 'NONE',  ( 0.000000000000000000, 0.5877852522924797984, -0.8090169943749426773 ) ) ;
#71576=EDGE_LOOP ( 'NONE', ( #53214, #54842, #43583, #74289 ) ) ;
#71601=DIRECTION ( 'NONE',  ( -1.000000000000000000, 0.000000000000000000, 0.000000000000000000 ) ) ;
#71635=EDGE_CURVE ( 'NONE', #12564, #13600, #61201, .T. ) ;
#71640=VECTOR ( 'NONE', #11226, 1000.000000000000000 ) ;
#71648=FACE_OUTER_BOUND ( 'NONE', #12029, .T. ) ;
#71655=CARTESIAN_POINT ( 'NONE',  ( 0.000000000000000000, 21.32104025579158701, -30.84782396557194772 ) ) ;
#71658=ORIENTED_EDGE ( 'NONE', *, *, #18994, .T. ) ;
#71685=DIRECTION ( 'NONE',  ( -1.000000000000000000, -0.000000000000000000, 0.000000000000000000 ) ) ;
#71707=ORIENTED_EDGE ( 'NONE', *, *, #6079, .T. ) ;
#71717=DIRECTION ( 'NONE',  ( -1.000000000000000000, -0.000000000000000000, -0.000000000000000000 ) ) ;
#71727=VERTEX_POINT ( 'NONE', #59045 ) ;
#71732=DIRECTION ( 'NONE',  ( 1.000000000000000000, 0.000000000000000000, -0.000000000000000000 ) ) ;
#71737=CARTESIAN_POINT ( 'NONE',  ( 10.00000000000000000, -35.38097989696503021, -12.42422080174676147 ) ) ;
#71739=ORIENTED_EDGE ( 'NONE', *, *, #38553, .T. ) ;
#71745=CARTESIAN_POINT ( 'NONE',  ( -3.000000000000000000, -22.67460108101783334, 6.353146135317912169 ) ) ;
#71753=FACE_OUTER_BOUND ( 'NONE', #33251, .T. ) ;
#71763=ORIENTED_EDGE ( 'NONE', *, *, #64343, .T. ) ;
#71769=CARTESIAN_POINT ( 'NONE',  ( 10.00000000000000000, -6.555932627142143865, -37.01155633439065440 ) ) ;
#71780=CYLINDRICAL_SURFACE ( 'NONE', #50288, 37.49900000000000233 ) ;
#71788=CARTESIAN_POINT ( 'NONE',  ( 10.00000000000000000, 17.80606268964585226, -33.00180498840028775 ) ) ;
#71839=ORIENTED_EDGE ( 'NONE', *, *, #67660, .F. ) ;
#71851=VECTOR ( 'NONE', #15560, 1000.000000000000000 ) ;
#71857=VECTOR ( 'NONE', #26122, 1000.000000000000227 ) ;
#71859=CARTESIAN_POINT ( 'NONE',  ( 0.000000000000000000, -16.65560815589383381, -38.55633173627028754 ) ) ;
#71863=CIRCLE ( 'NONE', #11807, 42.00000000000000000 ) ;
#71865=ORIENTED_EDGE ( 'NONE', *, *, #54722, .F. ) ;
#71868=EDGE_CURVE ( 'NONE', #61246, #65031, #3368, .T. ) ;
#71879=AXIS2_PLACEMENT_3D ( 'NONE', #26252, #60854, #20625 ) ;
#71888=CIRCLE ( 'NONE', #74316, 42.00000000000000000 ) ;
#71889=DIRECTION ( 'NONE',  ( -1.000000000000000000, 0.000000000000000000, 0.000000000000000000 ) ) ;
#71898=EDGE_CURVE ( 'NONE', #5103, #57712, #3637, .T. ) ;
#71907=ORIENTED_EDGE ( 'NONE', *, *, #546, .T. ) ;
#71910=ORIENTED_EDGE ( 'NONE', *, *, #43748, .F. ) ;
#71926=CIRCLE ( 'NONE', #49135, 42.00000000000000000 ) ;
#71937=CARTESIAN_POINT ( 'NONE',  ( 10.00000000000000000, 30.80686688397010542, 21.53537804866092387 ) ) ;
#71945=ORIENTED_EDGE ( 'NONE', *, *, #66053, .F. ) ;
#71957=ORIENTED_EDGE ( 'NONE', *, *, #52288, .T. ) ;
#71996=AXIS2_PLACEMENT_3D ( 'NONE', #17141, #40076, #28407 ) ;
#72003=LINE ( 'NONE', #49447, #6832 ) ;
#72012=DIRECTION ( 'NONE',  ( 0.000000000000000000, 0.5877852522924684742, 0.8090169943749506709 ) ) ;
#72015=EDGE_LOOP ( 'NONE', ( #44936, #50406, #63929, #8312 ) ) ;
#72016=ORIENTED_EDGE ( 'NONE', *, *, #8397, .F. ) ;
#72019=DIRECTION ( 'NONE',  ( 0.000000000000000000, 0.000000000000000000, 1.000000000000000000 ) ) ;
#72030=ORIENTED_EDGE ( 'NONE', *, *, #20488, .T. ) ;
#72039=EDGE_CURVE ( 'NONE', #32534, #66402, #13210, .T. ) ;
#72045=FACE_OUTER_BOUND ( 'NONE', #12289, .T. ) ;
#72059=ORIENTED_EDGE ( 'NONE', *, *, #25235, .T. ) ;
#72064=VECTOR ( 'NONE', #24745, 1000.000000000000000 ) ;
#72069=FACE_OUTER_BOUND ( 'NONE', #54852, .T. ) ;
#72084=LINE ( 'NONE', #20593, #45031 ) ;
#72086=DIRECTION ( 'NONE',  ( -1.000000000000000000, 0.000000000000000000, 0.000000000000000000 ) ) ;
#72096=EDGE_LOOP ( 'NONE', ( #16787, #69447, #69843, #51686 ) ) ;
#72101=SURFACE_SIDE_STYLE ('',( #43923 ) ) ;
#72103=ORIENTED_EDGE ( 'NONE', *, *, #32592, .T. ) ;
#72111=ORIENTED_EDGE ( 'NONE', *, *, #9585, .F. ) ;
#72112=CARTESIAN_POINT ( 'NONE',  ( 10.00000000000000000, -21.53537804866058991, -30.80686688397033635 ) ) ;
#72134=ORIENTED_EDGE ( 'NONE', *, *, #17925, .F. ) ;
#72143=DIRECTION ( 'NONE',  ( 0.000000000000000000, 0.4539904997395477482, -0.8910065241883673437 ) ) ;
#72148=DIRECTION ( 'NONE',  ( -1.000000000000000000, -0.000000000000000000, 0.000000000000000000 ) ) ;
#72150=VECTOR ( 'NONE', #53658, 1000.000000000000227 ) ;
#72172=LINE ( 'NONE', #60189, #67100 ) ;
#72184=EDGE_CURVE ( 'NONE', #32720, #66019, #10846, .T. ) ;
#72192=AXIS2_PLACEMENT_3D ( 'NONE', #47110, #909, #23796 ) ;
#72195=AXIS2_PLACEMENT_3D ( 'NONE', #8143, #31068, #35602 ) ;
#72200=ORIENTED_EDGE ( 'NONE', *, *, #14170, .F. ) ;
#72226=FACE_OUTER_BOUND ( 'NONE', #53713, .T. ) ;
#72237=CARTESIAN_POINT ( 'NONE',  ( 5.000000000000000000, -35.47612816024506088, -22.48208911017539435 ) ) ;
#72250=ORIENTED_EDGE ( 'NONE', *, *, #53131, .F. ) ;
#72264=DIRECTION ( 'NONE',  ( -1.000000000000000000, 0.000000000000000000, -0.000000000000000000 ) ) ;
#72267=EDGE_LOOP ( 'NONE', ( #73556, #65523, #55923, #7404 ) ) ;
#72276=ORIENTED_EDGE ( 'NONE', *, *, #40309, .T. ) ;
#72281=DIRECTION ( 'NONE',  ( 0.000000000000000000, -0.9945218953682730678, -0.1045284632676570791 ) ) ;
#72285=ORIENTED_EDGE ( 'NONE', *, *, #33025, .T. ) ;
#72290=ORIENTED_EDGE ( 'NONE', *, *, #6160, .T. ) ;
#72314=LINE ( 'NONE', #60320, #60538 ) ;
#72315=CARTESIAN_POINT ( 'NONE',  ( 0.000000000000000000, 0.000000000000000000, 0.000000000000000000 ) ) ;
#72323=ORIENTED_EDGE ( 'NONE', *, *, #45361, .T. ) ;
#72334=DIRECTION ( 'NONE',  ( 1.000000000000000000, 0.000000000000000000, 0.000000000000000000 ) ) ;
#72355=LINE ( 'NONE', #60356, #31339 ) ;
#72361=FACE_OUTER_BOUND ( 'NONE', #2339, .T. ) ;
#72363=CARTESIAN_POINT ( 'NONE',  ( 5.000000000000000000, -21.40280677340398086, 36.13751322684410638 ) ) ;
#72373=ORIENTED_EDGE ( 'NONE', *, *, #65767, .T. ) ;
#72379=CARTESIAN_POINT ( 'NONE',  ( -10.00000000000000000, 0.000000000000000000, 0.000000000000000000 ) ) ;
#72405=ORIENTED_EDGE ( 'NONE', *, *, #51546, .F. ) ;
#72417=VECTOR ( 'NONE', #14645, 1000.000000000000000 ) ;
#72434=LINE ( 'NONE', #8559, #50615 ) ;
#72436=CARTESIAN_POINT ( 'NONE',  ( 0.000000000000000000, 0.000000000000000000, 0.000000000000000000 ) ) ;
#72442=ORIENTED_EDGE ( 'NONE', *, *, #9864, .T. ) ;
#72449=EDGE_CURVE ( 'NONE', #61705, #66826, #32477, .T. ) ;
#72471=ORIENTED_EDGE ( 'NONE', *, *, #48346, .T. ) ;
#72487=AXIS2_PLACEMENT_3D ( 'NONE', #5603, #51817, #51437 ) ;
#72503=VECTOR ( 'NONE', #46979, 1000.000000000000000 ) ;
#72513=DIRECTION ( 'NONE',  ( 0.000000000000000000, 0.3090169943749482839, -0.9510565162951533091 ) ) ;
#72514=CARTESIAN_POINT ( 'NONE',  ( 10.00000000000000000, -37.58145647212455032, 0.6853352020789044152 ) ) ;
#72521=CARTESIAN_POINT ( 'NONE',  ( -3.000000000000000000, -23.29833615347109443, 3.418703333116492438 ) ) ;
#72522=CARTESIAN_POINT ( 'NONE',  ( 0.000000000000000000, 10.41901085202078292, 40.68715046381932865 ) ) ;
#72526=EDGE_CURVE ( 'NONE', #13949, #34086, #61155, .T. ) ;
#72528=CARTESIAN_POINT ( 'NONE',  ( 0.000000000000000000, 0.000000000000000000, 0.000000000000000000 ) ) ;
#72537=CYLINDRICAL_SURFACE ( 'NONE', #58684, 37.49900000000000233 ) ;
#72539=LINE ( 'NONE', #38723, #14984 ) ;
#72543=CARTESIAN_POINT ( 'NONE',  ( 10.00000000000000000, 10.96151621346540317, -35.95386929396244113 ) ) ;
#72544=DIRECTION ( 'NONE',  ( 1.000000000000000000, 0.000000000000000000, 0.000000000000000000 ) ) ;
#72554=VERTEX_POINT ( 'NONE', #10756 ) ;
#72568=CIRCLE ( 'NONE', #6541, 42.00000000000000000 ) ;
#72572=ORIENTED_EDGE ( 'NONE', *, *, #3350, .T. ) ;
#72593=LINE ( 'NONE', #71121, #40342 ) ;
#72594=DIRECTION ( 'NONE',  ( 0.000000000000000000, 0.8090169943749486725, -0.5877852522924713607 ) ) ;
#72595=ORIENTED_EDGE ( 'NONE', *, *, #48346, .F. ) ;
#72598=DIRECTION ( 'NONE',  ( 0.000000000000000000, 0.9510565162951521989, 0.3090169943749515591 ) ) ;
#72605=ORIENTED_EDGE ( 'NONE', *, *, #60467, .F. ) ;
#72606=AXIS2_PLACEMENT_3D ( 'NONE', #16191, #33469, #56428 ) ;
#72616=AXIS2_PLACEMENT_3D ( 'NONE', #54410, #71685, #13801 ) ;
#72620=CARTESIAN_POINT ( 'NONE',  ( 5.000000000000000000, 41.91543099594818500, 2.663952781846291362 ) ) ;
#72623=ORIENTED_EDGE ( 'NONE', *, *, #24354, .F. ) ;
#72625=DIRECTION ( 'NONE',  ( -1.000000000000000000, 0.000000000000000000, 0.000000000000000000 ) ) ;
#72635=CARTESIAN_POINT ( 'NONE',  ( 10.00000000000000000, 36.13751322684419165, 21.40280677340384230 ) ) ;
#72644=EDGE_LOOP ( 'NONE', ( #44616, #13342, #48170, #42255 ) ) ;
#72645=ORIENTED_EDGE ( 'NONE', *, *, #4377, .F. ) ;
#72649=EDGE_CURVE ( 'NONE', #51709, #5557, #4388, .T. ) ;
#72657=ORIENTED_EDGE ( 'NONE', *, *, #52444, .T. ) ;
#72678=DIRECTION ( 'NONE',  ( 0.000000000000000000, -0.3090169943749349057, -0.9510565162951577500 ) ) ;
#72685=VECTOR ( 'NONE', #43731, 1000.000000000000000 ) ;
#72686=ORIENTED_EDGE ( 'NONE', *, *, #1588, .F. ) ;
#72695=ORIENTED_EDGE ( 'NONE', *, *, #4784, .F. ) ;
#72705=ADVANCED_FACE ( 'NONE', ( #41450 ), #65139, .F. ) ;
#72717=VECTOR ( 'NONE', #54656, 1000.000000000000114 ) ;
#72718=CIRCLE ( 'NONE', #23535, 15.99999999999999822 ) ;
#72726=AXIS2_PLACEMENT_3D ( 'NONE', #2760, #66252, #49308 ) ;
#72727=LINE ( 'NONE', #44182, #59649 ) ;
#72734=ORIENTED_EDGE ( 'NONE', *, *, #42342, .F. ) ;
#72737=FACE_OUTER_BOUND ( 'NONE', #16382, .T. ) ;
#72738=EDGE_CURVE ( 'NONE', #48910, #67887, #30160, .T. ) ;
#72739=DIRECTION ( 'NONE',  ( -1.000000000000000000, 0.000000000000000000, 0.000000000000000000 ) ) ;
#72752=CARTESIAN_POINT ( 'NONE',  ( -10.00000000000000000, 0.000000000000000000, 0.000000000000000000 ) ) ;
#72759=VERTEX_POINT ( 'NONE', #12503 ) ;
#72766=FACE_OUTER_BOUND ( 'NONE', #72644, .T. ) ;
#72794=DIRECTION ( 'NONE',  ( 0.000000000000000000, 0.000000000000000000, 1.000000000000000000 ) ) ;
#72800=CARTESIAN_POINT ( 'NONE',  ( 10.00000000000000000, -9.188173127307003085, -40.98264845739760176 ) ) ;
#72809=LINE ( 'NONE', #32224, #23478 ) ;
#72823=VECTOR ( 'NONE', #68399, 1000.000000000000000 ) ;
#72827=LINE ( 'NONE', #54093, #36899 ) ;
#72829=VERTEX_POINT ( 'NONE', #3835 ) ;
#72870=ADVANCED_FACE ( 'NONE', ( #72226 ), #43325, .T. ) ;
#72878=AXIS2_PLACEMENT_3D ( 'NONE', #40368, #63315, #62196 ) ;
#72879=DIRECTION ( 'NONE',  ( -1.000000000000000000, 0.000000000000000000, -0.000000000000000000 ) ) ;
#72880=DIRECTION ( 'NONE',  ( 0.000000000000000000, -0.4999999999999913403, -0.8660254037844435926 ) ) ;
#72884=DIRECTION ( 'NONE',  ( 0.000000000000000000, 0.000000000000000000, 1.000000000000000000 ) ) ;
#72891=AXIS2_PLACEMENT_3D ( 'NONE', #74143, #22654, #32616 ) ;
#72894=VECTOR ( 'NONE', #23234, 1000.000000000000227 ) ;
#72906=CARTESIAN_POINT ( 'NONE',  ( 10.00000000000000000, -10.96151621346514382, 35.95386929396252640 ) ) ;
#72908=ORIENTED_EDGE ( 'NONE', *, *, #23881, .T. ) ;
#72918=ORIENTED_EDGE ( 'NONE', *, *, #61890, .T. ) ;
#72920=VECTOR ( 'NONE', #55976, 1000.000000000000114 ) ;
#72947=VECTOR ( 'NONE', #61734, 1000.000000000000000 ) ;
#72974=CARTESIAN_POINT ( 'NONE',  ( 10.00000000000000000, -35.53030884539077050, -12.26510123303296851 ) ) ;
#72983=AXIS2_PLACEMENT_3D ( 'NONE', #2027, #36554, #66262 ) ;
#72984=CARTESIAN_POINT ( 'NONE',  ( 10.00000000000000000, 0.000000000000000000, 0.000000000000000000 ) ) ;
#72993=CARTESIAN_POINT ( 'NONE',  ( 10.00000000000000000, 0.000000000000000000, 0.000000000000000000 ) ) ;
#72995=CARTESIAN_POINT ( 'NONE',  ( 10.00000000000000000, 26.08949754953024325, 27.05870788708241648 ) ) ;
#72999=AXIS2_PLACEMENT_3D ( 'NONE', #21264, #61893, #33292 ) ;
#73027=ORIENTED_EDGE ( 'NONE', *, *, #69994, .T. ) ;
#73044=EDGE_CURVE ( 'NONE', #53287, #59768, #46830, .T. ) ;
#73052=CARTESIAN_POINT ( 'NONE',  ( 10.00000000000000000, 41.91543099594818500, -2.663952781846293139 ) ) ;
#73058=EDGE_CURVE ( 'NONE', #51144, #1695, #42047, .T. ) ;
#73068=DIRECTION ( 'NONE',  ( -1.000000000000000000, 0.000000000000000000, -0.000000000000000000 ) ) ;
#73071=DIRECTION ( 'NONE',  ( 0.000000000000000000, -0.9781476007338040235, -0.2079116908177671419 ) ) ;
#73080=DIRECTION ( 'NONE',  ( -1.000000000000000000, -0.000000000000000000, 0.000000000000000000 ) ) ;
#73085=EDGE_CURVE ( 'NONE', #6668, #67004, #69615, .T. ) ;
#73086=EDGE_CURVE ( 'NONE', #10014, #39132, #50139, .T. ) ;
#73116=ORIENTED_EDGE ( 'NONE', *, *, #41866, .F. ) ;
#73124=ORIENTED_EDGE ( 'NONE', *, *, #53208, .T. ) ;
#73125=VERTEX_POINT ( 'NONE', #22334 ) ;
#73149=AXIS2_PLACEMENT_3D ( 'NONE', #66823, #3323, #37889 ) ;
#73155=ORIENTED_EDGE ( 'NONE', *, *, #13261, .F. ) ;
#73163=EDGE_CURVE ( 'NONE', #42446, #68977, #33607, .T. ) ;
#73164=DIRECTION ( 'NONE',  ( 0.000000000000000000, 0.9876883405951381034, -0.1564344650402276216 ) ) ;
#73199=CARTESIAN_POINT ( 'NONE',  ( 0.000000000000000000, 9.188173127307290855, 40.98264845739752360 ) ) ;
#73200=VECTOR ( 'NONE', #3202, 1000.000000000000000 ) ;
#73212=ORIENTED_EDGE ( 'NONE', *, *, #65767, .F. ) ;
#73229=DIRECTION ( 'NONE',  ( 0.000000000000000000, 0.000000000000000000, 1.000000000000000000 ) ) ;
#73245=EDGE_LOOP ( 'NONE', ( #60910, #30888, #46438, #64297 ) ) ;
#73246=VERTEX_POINT ( 'NONE', #35815 ) ;
#73254=LINE ( 'NONE', #22139, #24279 ) ;
#73260=VECTOR ( 'NONE', #23538, 1000.000000000000000 ) ;
#73269=DIRECTION ( 'NONE',  ( 0.000000000000000000, -0.5877852522924801315, 0.8090169943749421222 ) ) ;
#73275=DIRECTION ( 'NONE',  ( -1.000000000000000000, 0.000000000000000000, 0.000000000000000000 ) ) ;
#73277=LINE ( 'NONE', #39085, #42174 ) ;
#73284=DIRECTION ( 'NONE',  ( -1.000000000000000000, 0.000000000000000000, 0.000000000000000000 ) ) ;
#73286=CYLINDRICAL_SURFACE ( 'NONE', #51462, 42.00000000000000000 ) ;
#73307=CARTESIAN_POINT ( 'NONE',  ( 10.00000000000000000, -27.05870788708213226, -26.08949754953053102 ) ) ;
#73309=EDGE_CURVE ( 'NONE', #19670, #66145, #29073, .T. ) ;
#73321=CIRCLE ( 'NONE', #6115, 16.00000000000000000 ) ;
#73344=CARTESIAN_POINT ( 'NONE',  ( 10.00000000000000000, 0.000000000000000000, 0.000000000000000000 ) ) ;
#73345=DIRECTION ( 'NONE',  ( 0.000000000000000000, 0.6691306063588563502, 0.7431448254773960205 ) ) ;
#73359=AXIS2_PLACEMENT_3D ( 'NONE', #6952, #52830, #57735 ) ;
#73386=DIRECTION ( 'NONE',  ( 0.000000000000000000, -0.8660254037844437036, 0.4999999999999913403 ) ) ;
#73398=EDGE_LOOP ( 'NONE', ( #46546, #53947, #9405, #2111 ) ) ;
#73417=AXIS2_PLACEMENT_3D ( 'NONE', #63956, #832, #47029 ) ;
#73420=DIRECTION ( 'NONE',  ( -1.000000000000000000, 0.000000000000000000, 0.000000000000000000 ) ) ;
#73421=FACE_OUTER_BOUND ( 'NONE', #53668, .T. ) ;
#73450=CYLINDRICAL_SURFACE ( 'NONE', #55566, 16.00000000000000000 ) ;
#73456=CARTESIAN_POINT ( 'NONE',  ( 10.00000000000000000, 0.000000000000000000, 0.000000000000000000 ) ) ;
#73462=AXIS2_PLACEMENT_3D ( 'NONE', #68694, #39000, #63422 ) ;
#73487=ORIENTED_EDGE ( 'NONE', *, *, #32496, .T. ) ;
#73492=CARTESIAN_POINT ( 'NONE',  ( 5.000000000000000000, 31.52238457039599595, 27.75498641678753842 ) ) ;
#73504=CARTESIAN_POINT ( 'NONE',  ( 10.00000000000000000, -10.74501242461308159, 35.92658777277507909 ) ) ;
#73526=CARTESIAN_POINT ( 'NONE',  ( 10.00000000000000000, -12.26510123303284594, 35.53030884539080603 ) ) ;
#73538=EDGE_LOOP ( 'NONE', ( #24361, #41685, #13412, #33823 ) ) ;
#73539=DIRECTION ( 'NONE',  ( -1.000000000000000000, 0.000000000000000000, 0.000000000000000000 ) ) ;
#73556=ORIENTED_EDGE ( 'NONE', *, *, #15969, .F. ) ;
#73584=ORIENTED_EDGE ( 'NONE', *, *, #55930, .T. ) ;
#73610=DIRECTION ( 'NONE',  ( -1.000000000000000000, 0.000000000000000000, -0.000000000000000000 ) ) ;
#73617=DIRECTION ( 'NONE',  ( 0.000000000000000000, 0.000000000000000000, 1.000000000000000000 ) ) ;
#73631=CARTESIAN_POINT ( 'NONE',  ( -10.00000000000000000, 0.000000000000000000, 0.000000000000000000 ) ) ;
#73648=VECTOR ( 'NONE', #26398, 1000.000000000000000 ) ;
#73657=FACE_OUTER_BOUND ( 'NONE', #17596, .T. ) ;
#73664=ORIENTED_EDGE ( 'NONE', *, *, #28272, .F. ) ;
#73667=ADVANCED_FACE ( 'NONE', ( #52562 ), #59320, .T. ) ;
#73675=EDGE_CURVE ( 'NONE', #62190, #13857, #36012, .T. ) ;
#73678=CYLINDRICAL_SURFACE ( 'NONE', #27366, 16.00000000000000000 ) ;
#73679=AXIS2_PLACEMENT_3D ( 'NONE', #65648, #54002, #14499 ) ;
#73696=AXIS2_PLACEMENT_3D ( 'NONE', #60539, #38336, #61644 ) ;
#73715=DIRECTION ( 'NONE',  ( -1.000000000000000000, -0.000000000000000000, -0.000000000000000000 ) ) ;
#73731=FACE_OUTER_BOUND ( 'NONE', #51339, .T. ) ;
#73746=CYLINDRICAL_SURFACE ( 'NONE', #48523, 42.00000000000000000 ) ;
#73774=VERTEX_POINT ( 'NONE', #43534 ) ;
#73782=ORIENTED_EDGE ( 'NONE', *, *, #55183, .T. ) ;
#73787=CARTESIAN_POINT ( 'NONE',  ( 10.00000000000000000, 0.000000000000000000, 0.000000000000000000 ) ) ;
#73798=FACE_OUTER_BOUND ( 'NONE', #67146, .T. ) ;
#73799=AXIS2_PLACEMENT_3D ( 'NONE', #34553, #45491, #39844 ) ;
#73809=DIRECTION ( 'NONE',  ( 1.000000000000000000, -0.000000000000000000, -0.000000000000000000 ) ) ;
#73839=DIRECTION ( 'NONE',  ( -1.000000000000000000, 0.000000000000000000, -0.000000000000000000 ) ) ;
#73847=EDGE_CURVE ( 'NONE', #39991, #67442, #32586, .T. ) ;
#73855=VECTOR ( 'NONE', #65723, 999.9999999999998863 ) ;
#73860=VECTOR ( 'NONE', #29247, 1000.000000000000000 ) ;
#73866=CARTESIAN_POINT ( 'NONE',  ( 10.00000000000000000, -33.00180498840060039, 17.80606268964528027 ) ) ;
#73894=EDGE_CURVE ( 'NONE', #26343, #69721, #6156, .T. ) ;
#73901=CARTESIAN_POINT ( 'NONE',  ( -3.000000000000000000, -13.04903810567675038, 19.60159698893425428 ) ) ;
#73925=CARTESIAN_POINT ( 'NONE',  ( 10.00000000000000000, 0.000000000000000000, 0.000000000000000000 ) ) ;
#73934=ORIENTED_EDGE ( 'NONE', *, *, #632, .F. ) ;
#73937=CIRCLE ( 'NONE', #41526, 37.49900000000000944 ) ;
#73951=DIRECTION ( 'NONE',  ( 1.000000000000000000, 0.000000000000000000, 0.000000000000000000 ) ) ;
#73967=DIRECTION ( 'NONE',  ( -0.000000000000000000, -0.7431448254773870277, -0.6691306063588662312 ) ) ;
#73976=CIRCLE ( 'NONE', #41570, 16.00000000000000000 ) ;
#73980=ORIENTED_EDGE ( 'NONE', *, *, #66629, .T. ) ;
#73995=DIRECTION ( 'NONE',  ( 1.000000000000000000, -0.000000000000000000, 0.000000000000000000 ) ) ;
#74003=DIRECTION ( 'NONE',  ( 0.000000000000000000, -0.9781476007338070211, 0.2079116908177532363 ) ) ;
#74014=CARTESIAN_POINT ( 'NONE',  ( 10.00000000000000000, 0.6853352020790449695, 37.58145647212454321 ) ) ;
#74026=CIRCLE ( 'NONE', #49974, 16.00000000000000000 ) ;
#74033=CYLINDRICAL_SURFACE ( 'NONE', #57589, 16.00000000000000000 ) ;
#74035=DIRECTION ( 'NONE',  ( 0.000000000000000000, 0.9510565162951503115, 0.3090169943749573878 ) ) ;
#74050=VERTEX_POINT ( 'NONE', #61923 ) ;
#74053=DIRECTION ( 'NONE',  ( 0.000000000000000000, 0.8910065241883688980, -0.4539904997395445840 ) ) ;
#74076=CARTESIAN_POINT ( 'NONE',  ( 10.00000000000000000, 6.555932627142952995, -37.01155633439051940 ) ) ;
#74078=DIRECTION ( 'NONE',  ( -1.000000000000000000, -0.000000000000000000, 0.000000000000000000 ) ) ;
#74089=AXIS2_PLACEMENT_3D ( 'NONE', #5267, #56388, #56763 ) ;
#74107=CYLINDRICAL_SURFACE ( 'NONE', #26790, 37.49900000000000233 ) ;
#74122=VECTOR ( 'NONE', #62827, 1000.000000000000000 ) ;
#74126=VECTOR ( 'NONE', #7890, 1000.000000000000000 ) ;
#74136=CARTESIAN_POINT ( 'NONE',  ( 0.000000000000000000, -35.53030884539094103, 12.26510123303246935 ) ) ;
#74141=VECTOR ( 'NONE', #32238, 1000.000000000000000 ) ;
#74143=CARTESIAN_POINT ( 'NONE',  ( 10.00000000000000000, -17.67226234102801286, -33.17418723428327354 ) ) ;
#74145=ORIENTED_EDGE ( 'NONE', *, *, #22924, .F. ) ;
#74147=AXIS2_PLACEMENT_3D ( 'NONE', #3904, #44861, #9524 ) ;
#74166=DIRECTION ( 'NONE',  ( 0.000000000000000000, -1.000000000000000000, -1.047444401652940007E-14 ) ) ;
#74167=EDGE_CURVE ( 'NONE', #64121, #48813, #23540, .T. ) ;
#74177=AXIS2_PLACEMENT_3D ( 'NONE', #1154, #11633, #69888 ) ;
#74185=DIRECTION ( 'NONE',  ( 1.000000000000000000, -0.000000000000000000, 0.000000000000000000 ) ) ;
#74191=ORIENTED_EDGE ( 'NONE', *, *, #72738, .F. ) ;
#74192=AXIS2_PLACEMENT_3D ( 'NONE', #68862, #30461, #53410 ) ;
#74201=ORIENTED_EDGE ( 'NONE', *, *, #16571, .T. ) ;
#74212=CIRCLE ( 'NONE', #45405, 16.00000000000000000 ) ;
#74226=CIRCLE ( 'NONE', #41815, 42.00000000000000000 ) ;
#74230=CARTESIAN_POINT ( 'NONE',  ( 10.00000000000000000, 30.84782396557248418, -21.32104025579081252 ) ) ;
#74236=DIRECTION ( 'NONE',  ( 0.000000000000000000, -0.1564344650402380854, 0.9876883405951365491 ) ) ;
#74246=VERTEX_POINT ( 'NONE', #47215 ) ;
#74263=CARTESIAN_POINT ( 'NONE',  ( 0.000000000000000000, -26.23277895567245821, -4.042438405570103477 ) ) ;
#74280=VERTEX_POINT ( 'NONE', #26497 ) ;
#74289=ORIENTED_EDGE ( 'NONE', *, *, #52948, .T. ) ;
#74312=CARTESIAN_POINT ( 'NONE',  ( 10.00000000000000000, -17.80606268964516659, -33.00180498840066434 ) ) ;
#74316=AXIS2_PLACEMENT_3D ( 'NONE', #43357, #33147, #3503 ) ;
#74317=ORIENTED_EDGE ( 'NONE', *, *, #58055, .F. ) ;
#74318=AXIS2_PLACEMENT_3D ( 'NONE', #10705, #28359, #12179 ) ;
#74319=LINE ( 'NONE', #29181, #17463 ) ;
#74320=CARTESIAN_POINT ( 'NONE',  ( 0.000000000000000000, -3.948201729842038432, -23.21447184625298021 ) ) ;
#74321=DIRECTION ( 'NONE',  ( 0.000000000000000000, -0.8090169943749504489, 0.5877852522924689183 ) ) ;
#74327=EDGE_CURVE ( 'NONE', #20728, #60846, #72355, .T. ) ;
ENDSEC;
END-ISO-10303-21;
